ISO-10303-21;
HEADER;
FILE_DESCRIPTION (('STEP AP214'),
    '1' );
FILE_NAME ('big gear_ISO - Spur gear 2M 80T 20PA 10FW ---S80A75H50L20.0N.step',
    '2026-10-08T09:53:37',
    ( '' ),
    ( '' ),
    'SwSTEP 2.0',
    'SolidWorks 2026',
    '' );
FILE_SCHEMA (( 'AUTOMOTIVE_DESIGN' ));
ENDSEC;

DATA;
#3=EDGE_LOOP ( 'NONE', ( #16003, #47116, #6301, #7133 ) ) ;
#7=DIRECTION ( 'NONE',  ( 0.000000000000000000, 0.7071067811865487940, -0.7071067811865462405 ) ) ;
#21=AXIS2_PLACEMENT_3D ( 'NONE', #73803, #50119, #22316 ) ;
#22=FACE_OUTER_BOUND ( 'NONE', #9056, .T. ) ;
#28=ORIENTED_EDGE ( 'NONE', *, *, #17747, .T. ) ;
#31=CARTESIAN_POINT ( 'NONE',  ( 10.00000000000000000, 69.42325613327439271, 34.44570377933623462 ) ) ;
#42=AXIS2_PLACEMENT_3D ( 'NONE', #21315, #43177, #8581 ) ;
#43=ADVANCED_FACE ( 'NONE', ( #33760 ), #72489, .F. ) ;
#58=ORIENTED_EDGE ( 'NONE', *, *, #67325, .F. ) ;
#62=DIRECTION ( 'NONE',  ( -1.000000000000000000, 0.000000000000000000, 0.000000000000000000 ) ) ;
#66=EDGE_CURVE ( 'NONE', #32419, #45509, #49931, .T. ) ;
#69=ORIENTED_EDGE ( 'NONE', *, *, #12987, .T. ) ;
#70=VERTEX_POINT ( 'NONE', #39037 ) ;
#76=AXIS2_PLACEMENT_3D ( 'NONE', #48493, #31191, #42490 ) ;
#77=ORIENTED_EDGE ( 'NONE', *, *, #22870, .F. ) ;
#111=DIRECTION ( 'NONE',  ( 1.000000000000000000, 0.000000000000000000, 0.000000000000000000 ) ) ;
#115=DIRECTION ( 'NONE',  ( 0.000000000000000000, 0.000000000000000000, 1.000000000000000000 ) ) ;
#125=CARTESIAN_POINT ( 'NONE',  ( 5.000000000000000000, 27.74655509720779634, -77.16300072079631889 ) ) ;
#126=EDGE_CURVE ( 'NONE', #13140, #57222, #72120, .T. ) ;
#131=EDGE_LOOP ( 'NONE', ( #13994, #39252, #24769, #61767 ) ) ;
#133=AXIS2_PLACEMENT_3D ( 'NONE', #60527, #9005, #21768 ) ;
#148=ADVANCED_FACE ( 'NONE', ( #73604 ), #38668, .T. ) ;
#155=ORIENTED_EDGE ( 'NONE', *, *, #25637, .T. ) ;
#179=FACE_OUTER_BOUND ( 'NONE', #56512, .T. ) ;
#183=CARTESIAN_POINT ( 'NONE',  ( 0.000000000000000000, 0.000000000000000000, 0.000000000000000000 ) ) ;
#199=CARTESIAN_POINT ( 'NONE',  ( 10.00000000000000000, 0.000000000000000000, 0.000000000000000000 ) ) ;
#201=DIRECTION ( 'NONE',  ( 0.000000000000000000, -0.7071067811865537900, 0.7071067811865413555 ) ) ;
#202=CARTESIAN_POINT ( 'NONE',  ( 0.000000000000000000, -5.256550761633411284, 77.32052557432838569 ) ) ;
#204=VECTOR ( 'NONE', #39459, 1000.000000000000000 ) ;
#209=EDGE_LOOP ( 'NONE', ( #50770, #39177, #69553, #21845 ) ) ;
#213=EDGE_CURVE ( 'NONE', #29240, #35405, #33215, .T. ) ;
#226=DIRECTION ( 'NONE',  ( 0.000000000000000000, 0.9238795325112877377, -0.3826834323650873948 ) ) ;
#239=ORIENTED_EDGE ( 'NONE', *, *, #34376, .F. ) ;
#242=VECTOR ( 'NONE', #15932, 1000.000000000000000 ) ;
#247=DIRECTION ( 'NONE',  ( -1.000000000000000000, -0.000000000000000000, 0.000000000000000000 ) ) ;
#258=ADVANCED_FACE ( 'NONE', ( #18534 ), #30184, .T. ) ;
#271=DIRECTION ( 'NONE',  ( -1.000000000000000000, -0.000000000000000000, 0.000000000000000000 ) ) ;
#272=ORIENTED_EDGE ( 'NONE', *, *, #49233, .T. ) ;
#274=FACE_OUTER_BOUND ( 'NONE', #69340, .T. ) ;
#278=VERTEX_POINT ( 'NONE', #26397 ) ;
#286=DIRECTION ( 'NONE',  ( -1.000000000000000000, 0.000000000000000000, 0.000000000000000000 ) ) ;
#292=CIRCLE ( 'NONE', #31463, 31.99999999999998934 ) ;
#301=EDGE_CURVE ( 'NONE', #16264, #8951, #60626, .T. ) ;
#310=CARTESIAN_POINT ( 'NONE',  ( 10.00000000000000000, -46.21855187248583974, -62.20884554314070414 ) ) ;
#311=DIRECTION ( 'NONE',  ( -1.000000000000000000, 0.000000000000000000, 0.000000000000000000 ) ) ;
#327=ORIENTED_EDGE ( 'NONE', *, *, #16062, .T. ) ;
#328=ORIENTED_EDGE ( 'NONE', *, *, #66153, .T. ) ;
#330=EDGE_CURVE ( 'NONE', #45876, #49292, #56024, .T. ) ;
#335=DIRECTION ( 'NONE',  ( 0.000000000000000000, -0.8090169943749403458, -0.5877852522924830181 ) ) ;
#340=CIRCLE ( 'NONE', #62732, 82.00000000000000000 ) ;
#342=CARTESIAN_POINT ( 'NONE',  ( 10.00000000000000000, 2.946379043147425492, -75.11764819372145041 ) ) ;
#348=ORIENTED_EDGE ( 'NONE', *, *, #27313, .T. ) ;
#349=CARTESIAN_POINT ( 'NONE',  ( 10.00000000000000000, -55.19960302592104284, 51.03279382321070301 ) ) ;
#350=DIRECTION ( 'NONE',  ( -1.000000000000000000, 0.000000000000000000, 0.000000000000000000 ) ) ;
#352=DIRECTION ( 'NONE',  ( -1.000000000000000000, 0.000000000000000000, -0.000000000000000000 ) ) ;
#356=AXIS2_PLACEMENT_3D ( 'NONE', #18436, #58663, #43973 ) ;
#367=DIRECTION ( 'NONE',  ( 0.000000000000000000, 0.000000000000000000, 1.000000000000000000 ) ) ;
#369=DIRECTION ( 'NONE',  ( -1.000000000000000000, 0.000000000000000000, 0.000000000000000000 ) ) ;
#371=DIRECTION ( 'NONE',  ( 0.000000000000000000, 0.000000000000000000, 1.000000000000000000 ) ) ;
#374=CYLINDRICAL_SURFACE ( 'NONE', #42423, 31.99999999999999289 ) ;
#376=DIRECTION ( 'NONE',  ( 0.000000000000000000, -0.9238795325112906243, 0.3826834323650805114 ) ) ;
#380=CARTESIAN_POINT ( 'NONE',  ( 5.000000000000002665, -22.90783923731575911, -78.73519480814978522 ) ) ;
#382=EDGE_CURVE ( 'NONE', #38466, #29678, #65248, .T. ) ;
#406=EDGE_LOOP ( 'NONE', ( #60664, #29067, #49767, #42385 ) ) ;
#416=CARTESIAN_POINT ( 'NONE',  ( 10.00000000000000000, -10.30890764327324227, -81.34940948281347062 ) ) ;
#421=CYLINDRICAL_SURFACE ( 'NONE', #34708, 82.00000000000000000 ) ;
#427=ORIENTED_EDGE ( 'NONE', *, *, #61045, .F. ) ;
#432=ORIENTED_EDGE ( 'NONE', *, *, #15187, .T. ) ;
#434=ORIENTED_EDGE ( 'NONE', *, *, #33411, .T. ) ;
#436=DIRECTION ( 'NONE',  ( 0.000000000000000000, 0.000000000000000000, 1.000000000000000000 ) ) ;
#442=ORIENTED_EDGE ( 'NONE', *, *, #24306, .T. ) ;
#446=AXIS2_PLACEMENT_3D ( 'NONE', #16807, #39746, #40855 ) ;
#447=CARTESIAN_POINT ( 'NONE',  ( 0.000000000000000000, 41.19522573413731692, 65.64334221924924861 ) ) ;
#455=CIRCLE ( 'NONE', #66471, 31.99999999999999289 ) ;
#464=VERTEX_POINT ( 'NONE', #40275 ) ;
#473=CARTESIAN_POINT ( 'NONE',  ( 0.000000000000000000, -26.02418014898260878, -70.52718814184285634 ) ) ;
#479=DIRECTION ( 'NONE',  ( 0.000000000000000000, 0.000000000000000000, 1.000000000000000000 ) ) ;
#489=ORIENTED_EDGE ( 'NONE', *, *, #30011, .F. ) ;
#490=AXIS2_PLACEMENT_3D ( 'NONE', #21064, #31973, #50001 ) ;
#494=CIRCLE ( 'NONE', #59269, 31.99999999999999289 ) ;
#503=VERTEX_POINT ( 'NONE', #39168 ) ;
#504=LINE ( 'NONE', #32888, #943 ) ;
#512=ORIENTED_EDGE ( 'NONE', *, *, #65758, .T. ) ;
#539=CARTESIAN_POINT ( 'NONE',  ( 10.00000000000000000, 70.53064760720316428, -26.01480285779861035 ) ) ;
#542=AXIS2_PLACEMENT_3D ( 'NONE', #63998, #53079, #24500 ) ;
#543=ORIENTED_EDGE ( 'NONE', *, *, #58749, .F. ) ;
#551=AXIS2_PLACEMENT_3D ( 'NONE', #66850, #8604, #71359 ) ;
#559=CARTESIAN_POINT ( 'NONE',  ( 10.00000000000000000, 50.23322058963440639, -64.81221759200288091 ) ) ;
#564=AXIS2_PLACEMENT_3D ( 'NONE', #54816, #60474, #3712 ) ;
#598=ORIENTED_EDGE ( 'NONE', *, *, #41493, .T. ) ;
#609=DIRECTION ( 'NONE',  ( -1.000000000000000000, -0.000000000000000000, -0.000000000000000000 ) ) ;
#616=EDGE_CURVE ( 'NONE', #5747, #25646, #18544, .T. ) ;
#623=CIRCLE ( 'NONE', #39007, 77.49899999999999523 ) ;
#627=EDGE_LOOP ( 'NONE', ( #39309, #43860, #42175, #54202, #70134, #50291 ) ) ;
#631=EDGE_LOOP ( 'NONE', ( #18780, #16378, #8241, #67951 ) ) ;
#639=ORIENTED_EDGE ( 'NONE', *, *, #74332, .F. ) ;
#641=DIRECTION ( 'NONE',  ( 0.000000000000000000, 0.000000000000000000, 1.000000000000000000 ) ) ;
#642=AXIS2_PLACEMENT_3D ( 'NONE', #45335, #55858, #4749 ) ;
#643=LINE ( 'NONE', #23906, #4726 ) ;
#647=LINE ( 'NONE', #69041, #51696 ) ;
#654=AXIS2_PLACEMENT_3D ( 'NONE', #45899, #28211, #35347 ) ;
#662=EDGE_CURVE ( 'NONE', #8349, #73763, #13173, .T. ) ;
#664=EDGE_CURVE ( 'NONE', #39348, #15750, #53376, .T. ) ;
#675=DIRECTION ( 'NONE',  ( 0.000000000000000000, 0.07845909572783797692, 0.9969173337331285190 ) ) ;
#676=AXIS2_PLACEMENT_3D ( 'NONE', #2122, #58480, #24642 ) ;
#684=CARTESIAN_POINT ( 'NONE',  ( 5.000000000000000000, -50.23322058963393744, 64.81221759200325039 ) ) ;
#688=VERTEX_POINT ( 'NONE', #70670 ) ;
#711=ADVANCED_FACE ( 'NONE', ( #59052 ), #836, .T. ) ;
#722=EDGE_CURVE ( 'NONE', #29955, #52790, #71225, .T. ) ;
#734=ORIENTED_EDGE ( 'NONE', *, *, #67580, .F. ) ;
#754=DIRECTION ( 'NONE',  ( -1.000000000000000000, -0.000000000000000000, 0.000000000000000000 ) ) ;
#755=ORIENTED_EDGE ( 'NONE', *, *, #11773, .T. ) ;
#760=DIRECTION ( 'NONE',  ( 0.000000000000000000, 0.000000000000000000, 1.000000000000000000 ) ) ;
#763=AXIS2_PLACEMENT_3D ( 'NONE', #36619, #70444, #32081 ) ;
#768=EDGE_LOOP ( 'NONE', ( #52256, #54474, #28723, #42542 ) ) ;
#777=LINE ( 'NONE', #12011, #7121 ) ;
#788=ORIENTED_EDGE ( 'NONE', *, *, #22355, .T. ) ;
#789=DIRECTION ( 'NONE',  ( -1.000000000000000000, -0.000000000000000000, 0.000000000000000000 ) ) ;
#793=EDGE_CURVE ( 'NONE', #67190, #11833, #21029, .T. ) ;
#795=( LENGTH_UNIT ( ) NAMED_UNIT ( * ) SI_UNIT ( .MILLI., .METRE. ) );
#796=ORIENTED_EDGE ( 'NONE', *, *, #32317, .T. ) ;
#808=VERTEX_POINT ( 'NONE', #66179 ) ;
#828=CARTESIAN_POINT ( 'NONE',  ( 10.00000000000000000, -56.15606465355001120, 59.75363087400054951 ) ) ;
#835=ORIENTED_EDGE ( 'NONE', *, *, #23203, .F. ) ;
#836=CYLINDRICAL_SURFACE ( 'NONE', #58045, 31.99999999999999289 ) ;
#842=AXIS2_PLACEMENT_3D ( 'NONE', #18020, #1510, #46224 ) ;
#848=CARTESIAN_POINT ( 'NONE',  ( 0.000000000000000000, 33.71516098798740302, 74.74816331893443078 ) ) ;
#849=DIRECTION ( 'NONE',  ( 0.000000000000000000, 0.000000000000000000, -1.000000000000000000 ) ) ;
#859=ORIENTED_EDGE ( 'NONE', *, *, #57057, .T. ) ;
#864=ORIENTED_EDGE ( 'NONE', *, *, #47800, .T. ) ;
#874=FACE_OUTER_BOUND ( 'NONE', #50101, .T. ) ;
#875=EDGE_CURVE ( 'NONE', #39002, #36881, #2684, .T. ) ;
#876=ORIENTED_EDGE ( 'NONE', *, *, #60456, .T. ) ;
#889=VECTOR ( 'NONE', #37456, 1000.000000000000000 ) ;
#899=ORIENTED_EDGE ( 'NONE', *, *, #27993, .F. ) ;
#902=CARTESIAN_POINT ( 'NONE',  ( 0.000000000000000000, -36.73666225445845157, -65.58780272294114866 ) ) ;
#905=CARTESIAN_POINT ( 'NONE',  ( 10.00000000000000000, 36.72794159290334903, -65.59268652807170952 ) ) ;
#906=LINE ( 'NONE', #57272, #26039 ) ;
#908=CARTESIAN_POINT ( 'NONE',  ( 10.00000000000000000, -73.44644590900043113, -24.73286445877782924 ) ) ;
#910=CARTESIAN_POINT ( 'NONE',  ( 10.00000000000000000, 0.000000000000000000, 0.000000000000000000 ) ) ;
#915=EDGE_CURVE ( 'NONE', #15157, #3606, #40196, .T. ) ;
#931=CARTESIAN_POINT ( 'NONE',  ( 10.00000000000000000, -51.02545421589363883, 55.20638768913742922 ) ) ;
#932=DIRECTION ( 'NONE',  ( 0.000000000000000000, -0.07845909572785234043, 0.9969173337331274087 ) ) ;
#934=AXIS2_PLACEMENT_3D ( 'NONE', #72701, #48316, #9575 ) ;
#938=DIRECTION ( 'NONE',  ( -1.000000000000000000, 0.000000000000000000, -0.000000000000000000 ) ) ;
#942=DIRECTION ( 'NONE',  ( -1.000000000000000000, -0.000000000000000000, 0.000000000000000000 ) ) ;
#943=VECTOR ( 'NONE', #9608, 1000.000000000000000 ) ;
#946=ORIENTED_EDGE ( 'NONE', *, *, #71700, .T. ) ;
#950=ORIENTED_EDGE ( 'NONE', *, *, #54751, .F. ) ;
#961=VERTEX_POINT ( 'NONE', #4894 ) ;
#968=VERTEX_POINT ( 'NONE', #27411 ) ;
#971=EDGE_CURVE ( 'NONE', #30219, #19199, #14467, .T. ) ;
#975=VERTEX_POINT ( 'NONE', #17260 ) ;
#978=CIRCLE ( 'NONE', #22565, 82.00000000000000000 ) ;
#991=VERTEX_POINT ( 'NONE', #21780 ) ;
#1002=CIRCLE ( 'NONE', #15377, 32.00000000000000000 ) ;
#1005=AXIS2_PLACEMENT_3D ( 'NONE', #19392, #42340, #53993 ) ;
#1006=CIRCLE ( 'NONE', #63389, 31.99999999999999289 ) ;
#1009=CARTESIAN_POINT ( 'NONE',  ( 5.000000000000002665, -2.543863470248944214, 81.96053171279901051 ) ) ;
#1017=CARTESIAN_POINT ( 'NONE',  ( 5.000000000000000000, -40.65526001592664329, 71.21200624218782593 ) ) ;
#1019=CARTESIAN_POINT ( 'NONE',  ( 10.00000000000000000, -8.830959090342926032, 74.65491531819115778 ) ) ;
#1039=DIRECTION ( 'NONE',  ( -1.000000000000000000, 0.000000000000000000, -0.000000000000000000 ) ) ;
#1047=EDGE_CURVE ( 'NONE', #70648, #50470, #62474, .T. ) ;
#1052=CARTESIAN_POINT ( 'NONE',  ( 0.000000000000000000, -11.30684508768395524, 76.66974797899831628 ) ) ;
#1056=CARTESIAN_POINT ( 'NONE',  ( 0.000000000000000000, -59.03342792756297541, 46.54456581323783126 ) ) ;
#1076=VERTEX_POINT ( 'NONE', #53317 ) ;
#1085=CIRCLE ( 'NONE', #9393, 31.99999999999999289 ) ;
#1096=DIRECTION ( 'NONE',  ( 0.000000000000000000, 0.9723699203976756689, 0.2334453638559093047 ) ) ;
#1117=DIRECTION ( 'NONE',  ( -1.000000000000000000, -0.000000000000000000, -0.000000000000000000 ) ) ;
#1121=DIRECTION ( 'NONE',  ( 0.000000000000000000, 0.000000000000000000, 1.000000000000000000 ) ) ;
#1124=AXIS2_PLACEMENT_3D ( 'NONE', #51978, #64384, #59114 ) ;
#1136=AXIS2_PLACEMENT_3D ( 'NONE', #65708, #35636, #14189 ) ;
#1139=ADVANCED_FACE ( 'NONE', ( #34923 ), #47315, .T. ) ;
#1142=VERTEX_POINT ( 'NONE', #18355 ) ;
#1159=VERTEX_POINT ( 'NONE', #63877 ) ;
#1172=ORIENTED_EDGE ( 'NONE', *, *, #5947, .F. ) ;
#1188=DIRECTION ( 'NONE',  ( 0.000000000000000000, 0.000000000000000000, 1.000000000000000000 ) ) ;
#1190=CARTESIAN_POINT ( 'NONE',  ( 10.00000000000000000, 63.18004540533029001, 44.88180994100400767 ) ) ;
#1192=VERTEX_POINT ( 'NONE', #59329 ) ;
#1198=AXIS2_PLACEMENT_3D ( 'NONE', #56876, #45224, #10253 ) ;
#1211=DIRECTION ( 'NONE',  ( -1.000000000000000000, 0.000000000000000000, -0.000000000000000000 ) ) ;
#1212=VECTOR ( 'NONE', #3746, 1000.000000000000000 ) ;
#1216=CIRCLE ( 'NONE', #54036, 82.00000000000000000 ) ;
#1221=AXIS2_PLACEMENT_3D ( 'NONE', #72653, #50483, #50850 ) ;
#1222=CIRCLE ( 'NONE', #10785, 77.49899999999999523 ) ;
#1228=FACE_OUTER_BOUND ( 'NONE', #28220, .T. ) ;
#1232=ADVANCED_FACE ( 'NONE', ( #2956 ), #31484, .T. ) ;
#1241=AXIS2_PLACEMENT_3D ( 'NONE', #63682, #1665, #13266 ) ;
#1247=ORIENTED_EDGE ( 'NONE', *, *, #5534, .T. ) ;
#1248=CIRCLE ( 'NONE', #19220, 31.99999999999999645 ) ;
#1249=DIRECTION ( 'NONE',  ( 0.000000000000000000, -0.07845909572783058006, -0.9969173337331290741 ) ) ;
#1255=VERTEX_POINT ( 'NONE', #66093 ) ;
#1256=DIRECTION ( 'NONE',  ( 0.000000000000000000, 0.3090169943749412895, 0.9510565162951556406 ) ) ;
#1267=AXIS2_PLACEMENT_3D ( 'NONE', #4310, #67439, #33213 ) ;
#1284=CARTESIAN_POINT ( 'NONE',  ( 0.000000000000000000, 22.90783923731629912, 78.73519480814962890 ) ) ;
#1288=CARTESIAN_POINT ( 'NONE',  ( 5.000000000000000000, -64.81221759200379040, 50.23322058963324110 ) ) ;
#1289=DIRECTION ( 'NONE',  ( -1.000000000000000000, -0.000000000000000000, -0.000000000000000000 ) ) ;
#1292=DIRECTION ( 'NONE',  ( 0.000000000000000000, 0.5224985647159500202, -0.8526401643540915121 ) ) ;
#1300=CARTESIAN_POINT ( 'NONE',  ( 0.000000000000000000, -71.27951684758046724, 30.41916302227088309 ) ) ;
#1319=AXIS2_PLACEMENT_3D ( 'NONE', #14732, #21472, #56073 ) ;
#1322=DIRECTION ( 'NONE',  ( -1.000000000000000000, 0.000000000000000000, 0.000000000000000000 ) ) ;
#1329=ORIENTED_EDGE ( 'NONE', *, *, #18478, .F. ) ;
#1336=CARTESIAN_POINT ( 'NONE',  ( 0.000000000000000000, -72.35432306680498016, 20.40083707022857951 ) ) ;
#1338=ORIENTED_EDGE ( 'NONE', *, *, #32822, .T. ) ;
#1342=EDGE_CURVE ( 'NONE', #44951, #8568, #15304, .T. ) ;
#1351=VERTEX_POINT ( 'NONE', #8565 ) ;
#1378=DIRECTION ( 'NONE',  ( 1.000000000000000000, -0.000000000000000000, 0.000000000000000000 ) ) ;
#1379=ORIENTED_EDGE ( 'NONE', *, *, #46496, .F. ) ;
#1382=AXIS2_PLACEMENT_3D ( 'NONE', #31665, #27412, #42591 ) ;
#1396=CARTESIAN_POINT ( 'NONE',  ( 10.00000000000000000, -59.46389618801999433, 49.70050353004867816 ) ) ;
#1397=DIRECTION ( 'NONE',  ( 0.000000000000000000, 0.000000000000000000, -1.000000000000000000 ) ) ;
#1410=AXIS2_PLACEMENT_3D ( 'NONE', #22614, #38047, #49679 ) ;
#1413=VECTOR ( 'NONE', #13421, 1000.000000000000000 ) ;
#1419=DIRECTION ( 'NONE',  ( 1.000000000000000000, 0.000000000000000000, 0.000000000000000000 ) ) ;
#1437=ORIENTED_EDGE ( 'NONE', *, *, #10127, .T. ) ;
#1440=CARTESIAN_POINT ( 'NONE',  ( 0.000000000000000000, 59.46389618801963195, 49.70050353004911159 ) ) ;
#1450=VERTEX_POINT ( 'NONE', #33321 ) ;
#1453=ORIENTED_EDGE ( 'NONE', *, *, #6036, .T. ) ;
#1460=CARTESIAN_POINT ( 'NONE',  ( 10.00000000000000000, 54.21277698773675979, 55.38113227695801299 ) ) ;
#1462=ORIENTED_EDGE ( 'NONE', *, *, #50315, .F. ) ;
#1463=VERTEX_POINT ( 'NONE', #51007 ) ;
#1468=ORIENTED_EDGE ( 'NONE', *, *, #34535, .F. ) ;
#1476=AXIS2_PLACEMENT_3D ( 'NONE', #15646, #9993, #43498 ) ;
#1484=CARTESIAN_POINT ( 'NONE',  ( 10.00000000000000000, 73.72996012237460661, -14.67089635893632504 ) ) ;
#1496=VERTEX_POINT ( 'NONE', #33711 ) ;
#1502=VECTOR ( 'NONE', #20654, 1000.000000000000000 ) ;
#1510=DIRECTION ( 'NONE',  ( -1.000000000000000000, -0.000000000000000000, 0.000000000000000000 ) ) ;
#1514=AXIS2_PLACEMENT_3D ( 'NONE', #60420, #67529, #38211 ) ;
#1519=DIRECTION ( 'NONE',  ( -1.000000000000000000, -0.000000000000000000, 0.000000000000000000 ) ) ;
#1520=ORIENTED_EDGE ( 'NONE', *, *, #9260, .T. ) ;
#1522=VERTEX_POINT ( 'NONE', #24563 ) ;
#1526=DIRECTION ( 'NONE',  ( -1.000000000000000000, 0.000000000000000000, 0.000000000000000000 ) ) ;
#1532=DIRECTION ( 'NONE',  ( 0.000000000000000000, 0.000000000000000000, 1.000000000000000000 ) ) ;
#1544=ORIENTED_EDGE ( 'NONE', *, *, #14957, .F. ) ;
#1549=ORIENTED_EDGE ( 'NONE', *, *, #875, .F. ) ;
#1552=ORIENTED_EDGE ( 'NONE', *, *, #14097, .T. ) ;
#1557=CARTESIAN_POINT ( 'NONE',  ( 0.000000000000000000, -46.54456581323847786, 59.03342792756247093 ) ) ;
#1560=EDGE_CURVE ( 'NONE', #10604, #44963, #42510, .T. ) ;
#1565=FACE_OUTER_BOUND ( 'NONE', #2977, .T. ) ;
#1574=CIRCLE ( 'NONE', #2798, 82.00000000000000000 ) ;
#1579=AXIS2_PLACEMENT_3D ( 'NONE', #26390, #49313, #35370 ) ;
#1592=ADVANCED_FACE ( 'NONE', ( #19648 ), #13277, .T. ) ;
#1593=EDGE_CURVE ( 'NONE', #24805, #16594, #19640, .T. ) ;
#1604=EDGE_CURVE ( 'NONE', #60490, #17740, #70780, .T. ) ;
#1612=ORIENTED_EDGE ( 'NONE', *, *, #35372, .F. ) ;
#1618=DIRECTION ( 'NONE',  ( -1.000000000000000000, 0.000000000000000000, 0.000000000000000000 ) ) ;
#1623=AXIS2_PLACEMENT_3D ( 'NONE', #10219, #44069, #38428 ) ;
#1629=CARTESIAN_POINT ( 'NONE',  ( 0.000000000000000000, -81.96053171279903893, 2.543863470248094227 ) ) ;
#1630=AXIS2_PLACEMENT_3D ( 'NONE', #62392, #51090, #33800 ) ;
#1634=CARTESIAN_POINT ( 'NONE',  ( 10.00000000000000000, 55.16347631943041563, 60.67117009219156643 ) ) ;
#1635=CARTESIAN_POINT ( 'NONE',  ( 10.00000000000000000, -75.11764819372145041, -2.946379043147127064 ) ) ;
#1644=CARTESIAN_POINT ( 'NONE',  ( 0.000000000000000000, -20.40083707022935400, 72.35432306680478121 ) ) ;
#1646=LINE ( 'NONE', #7251, #29630 ) ;
#1651=DIRECTION ( 'NONE',  ( -1.000000000000000000, -0.000000000000000000, 0.000000000000000000 ) ) ;
#1655=VERTEX_POINT ( 'NONE', #42974 ) ;
#1665=DIRECTION ( 'NONE',  ( -1.000000000000000000, -0.000000000000000000, -0.000000000000000000 ) ) ;
#1691=LINE ( 'NONE', #47509, #19176 ) ;
#1693=ORIENTED_EDGE ( 'NONE', *, *, #12824, .T. ) ;
#1696=CIRCLE ( 'NONE', #5272, 77.49899999999999523 ) ;
#1699=ORIENTED_EDGE ( 'NONE', *, *, #61480, .F. ) ;
#1706=CARTESIAN_POINT ( 'NONE',  ( 0.000000000000000000, 18.89407956138256139, 75.16055320797038064 ) ) ;
#1708=ORIENTED_EDGE ( 'NONE', *, *, #60623, .F. ) ;
#1710=ORIENTED_EDGE ( 'NONE', *, *, #25380, .T. ) ;
#1715=CARTESIAN_POINT ( 'NONE',  ( 0.000000000000000000, -46.53671651293907274, -59.03961581697448935 ) ) ;
#1717=CARTESIAN_POINT ( 'NONE',  ( 10.00000000000000000, 2.956366410621684260, -75.11725578898465017 ) ) ;
#1727=VERTEX_POINT ( 'NONE', #72262 ) ;
#1738=DIRECTION ( 'NONE',  ( -1.000000000000000000, 0.000000000000000000, 0.000000000000000000 ) ) ;
#1743=ORIENTED_EDGE ( 'NONE', *, *, #72785, .T. ) ;
#1753=DIRECTION ( 'NONE',  ( 0.000000000000000000, 0.1564344650402311743, -0.9876883405951377704 ) ) ;
#1756=DIRECTION ( 'NONE',  ( 1.000000000000000000, 0.000000000000000000, -0.000000000000000000 ) ) ;
#1760=CYLINDRICAL_SURFACE ( 'NONE', #50839, 31.99999999999998579 ) ;
#1768=DIRECTION ( 'NONE',  ( 0.000000000000000000, 0.8090169943749486725, -0.5877852522924713607 ) ) ;
#1769=ORIENTED_EDGE ( 'NONE', *, *, #39831, .T. ) ;
#1774=EDGE_CURVE ( 'NONE', #14718, #17127, #24477, .T. ) ;
#1777=VERTEX_POINT ( 'NONE', #67745 ) ;
#1783=FACE_OUTER_BOUND ( 'NONE', #22087, .T. ) ;
#1789=CARTESIAN_POINT ( 'NONE',  ( 10.00000000000000000, -59.03342792756297541, 46.54456581323783126 ) ) ;
#1797=AXIS2_PLACEMENT_3D ( 'NONE', #45062, #34888, #6326 ) ;
#1801=EDGE_LOOP ( 'NONE', ( #7477, #67129, #5153, #54165 ) ) ;
#1805=DIRECTION ( 'NONE',  ( -1.000000000000000000, -0.000000000000000000, 0.000000000000000000 ) ) ;
#1808=EDGE_CURVE ( 'NONE', #1450, #35339, #6452, .T. ) ;
#1817=CARTESIAN_POINT ( 'NONE',  ( 0.000000000000000000, 0.000000000000000000, 0.000000000000000000 ) ) ;
#1821=LINE ( 'NONE', #57824, #26304 ) ;
#1838=EDGE_LOOP ( 'NONE', ( #45044, #16033, #19530, #9739 ) ) ;
#1840=AXIS2_PLACEMENT_3D ( 'NONE', #8394, #31311, #54263 ) ;
#1860=CARTESIAN_POINT ( 'NONE',  ( 10.00000000000000000, 72.35160999960817207, 20.41045688087850607 ) ) ;
#1868=CIRCLE ( 'NONE', #11433, 77.49899999999998101 ) ;
#1870=VERTEX_POINT ( 'NONE', #51564 ) ;
#1872=ADVANCED_FACE ( 'NONE', ( #62495 ), #10974, .T. ) ;
#1881=ORIENTED_EDGE ( 'NONE', *, *, #2771, .F. ) ;
#1884=CIRCLE ( 'NONE', #53482, 31.99999999999999289 ) ;
#1890=LINE ( 'NONE', #47346, #22174 ) ;
#1893=EDGE_CURVE ( 'NONE', #8568, #25521, #46500, .T. ) ;
#1895=FACE_OUTER_BOUND ( 'NONE', #3899, .T. ) ;
#1905=EDGE_CURVE ( 'NONE', #70889, #60073, #66898, .T. ) ;
#1910=EDGE_LOOP ( 'NONE', ( #3819, #45720, #14057, #17027 ) ) ;
#1911=ORIENTED_EDGE ( 'NONE', *, *, #47294, .F. ) ;
#1924=DIRECTION ( 'NONE',  ( -1.000000000000000000, -0.000000000000000000, 0.000000000000000000 ) ) ;
#1928=DIRECTION ( 'NONE',  ( -1.000000000000000000, 0.000000000000000000, 0.000000000000000000 ) ) ;
#1932=LINE ( 'NONE', #66533, #72366 ) ;
#1934=DIRECTION ( 'NONE',  ( -1.000000000000000000, 0.000000000000000000, 0.000000000000000000 ) ) ;
#1936=EDGE_CURVE ( 'NONE', #52599, #67382, #12842, .T. ) ;
#1948=AXIS2_PLACEMENT_3D ( 'NONE', #24843, #15317, #26966 ) ;
#1955=ORIENTED_EDGE ( 'NONE', *, *, #41345, .F. ) ;
#1961=CARTESIAN_POINT ( 'NONE',  ( 0.000000000000000000, 74.74816331893477184, -33.71516098798660011 ) ) ;
#1975=ORIENTED_EDGE ( 'NONE', *, *, #24507, .T. ) ;
#1984=AXIS2_PLACEMENT_3D ( 'NONE', #62555, #51246, #68559 ) ;
#1988=VERTEX_POINT ( 'NONE', #47042 ) ;
#1990=DIRECTION ( 'NONE',  ( 0.000000000000000000, 0.9876883405951383255, -0.1564344650402277048 ) ) ;
#1996=DIRECTION ( 'NONE',  ( -1.000000000000000000, 0.000000000000000000, 0.000000000000000000 ) ) ;
#2003=AXIS2_PLACEMENT_3D ( 'NONE', #29705, #11677, #35720 ) ;
#2007=ORIENTED_EDGE ( 'NONE', *, *, #24640, .F. ) ;
#2009=DIRECTION ( 'NONE',  ( -1.000000000000000000, 0.000000000000000000, 0.000000000000000000 ) ) ;
#2021=EDGE_LOOP ( 'NONE', ( #17016, #33841, #35931, #24776 ) ) ;
#2030=DIRECTION ( 'NONE',  ( -1.000000000000000000, 0.000000000000000000, 0.000000000000000000 ) ) ;
#2045=FACE_OUTER_BOUND ( 'NONE', #57394, .T. ) ;
#2053=DIRECTION ( 'NONE',  ( -1.000000000000000000, 0.000000000000000000, -0.000000000000000000 ) ) ;
#2056=AXIS2_PLACEMENT_3D ( 'NONE', #16139, #55245, #56751 ) ;
#2062=VERTEX_POINT ( 'NONE', #7916 ) ;
#2063=ADVANCED_FACE ( 'NONE', ( #53774 ), #58313, .T. ) ;
#2068=ORIENTED_EDGE ( 'NONE', *, *, #40560, .T. ) ;
#2074=ORIENTED_EDGE ( 'NONE', *, *, #59970, .F. ) ;
#2078=EDGE_LOOP ( 'NONE', ( #30248, #40135, #17651, #51121 ) ) ;
#2079=EDGE_LOOP ( 'NONE', ( #37265, #53284, #7770, #56109, #46056, #15253, #7415, #10741, #69066, #67673, #71670, #46050, #43374, #4538, #44452, #24396, #18336, #73012, #54371, #51399, #946, #46681, #68084, #73961, #4087, #66512, #46789, #442, #49864, #6338, #14821, #27894, #59131, #432, #15444, #38036, #48524, #49811, #63474, #26894, #25539, #17845, #43872, #29144, #71066, #17562, #35576, #67128, #57657, #23744, #3378, #27674, #18021, #12442, #12234, #3800, #9150, #54194, #59427, #56072, #40987, #68664, #2358, #43484, #43759, #58285, #28502, #45416, #50992, #35661, #60771, #19743, #55794, #65399, #27890, #56212, #61400, #4556, #50837, #70109, #44689, #37173, #24917, #59550, #37282, #28651, #19231, #47601, #15000, #38098, #58513, #68055, #25251, #28373, #46599, #22576, #42531, #434, #61779, #54813, #15266, #65561, #60486, #57251, #47705, #38090, #29757, #57667, #11073, #58859, #13621, #69004, #12022, #36213, #43798, #4217, #12655, #12756, #59190, #66801, #57240, #69, #27134, #14994, #59249, #53333, #3893, #36726, #49288, #60840, #8035, #55465, #28404, #46044, #41631, #56160, #41586, #19582, #40971, #48923, #50114, #19983, #52635, #21752, #26907, #42618, #14236, #4628, #70848, #19527, #53743, #31439, #27462, #58998, #45908, #13024, #39879, #44558, #5199, #64715, #12833, #59645, #6645, #69283, #61104, #19061, #67994, #58092, #69652, #17365, #23244, #7017, #61219, #40804, #20997, #6960, #50190, #27147, #26043, #9876, #40576, #55946, #5829, #3628, #8856, #69190, #49898, #46136, #4193, #38210, #27379, #33074, #3069, #20694, #12572, #33160, #54472, #52174, #18776, #60471, #17004, #61129, #37492, #40499, #10851, #35171, #24709, #55275, #67502, #31918, #47791, #60656, #31793, #64921, #33681, #51892, #69801, #52506, #45648, #23160, #56813, #44086, #55599, #28465, #13559, #66348, #10591, #7570, #23479, #1693, #53517, #72106, #53887, #68456, #13610, #70420, #51126, #30172, #67862, #55827, #28964, #62255, #66294, #58609, #14227, #22808, #12046, #11367, #36690, #13984, #23449, #34423, #73489, #34949, #71550, #1710, #36056, #38083, #59841, #2854, #12904, #35959, #3430, #23148, #39877, #2451, #28847, #30330, #43656, #71342, #22655, #64837, #19482, #9119, #48455, #72782, #74066, #42116, #1955, #61141, #14073, #63269, #69262, #14424, #38840, #40585, #68237, #59308, #43235, #30506, #55448, #24906, #15408, #2463, #57876, #68064, #39870, #34815, #47962, #73863, #7779, #15569, #46416, #788, #21760, #71920, #44402, #27819, #48821, #33205, #18682, #52998, #68888, #47792, #40908, #40238, #7749, #45807, #59379, #46984, #24077, #67036, #74172, #16112, #5862 ) ) ;
#2086=CARTESIAN_POINT ( 'NONE',  ( 10.00000000000000000, -54.21277698773715059, 55.38113227695762930 ) ) ;
#2087=FACE_OUTER_BOUND ( 'NONE', #66940, .T. ) ;
#2089=EDGE_CURVE ( 'NONE', #65194, #3728, #37418, .T. ) ;
#2098=FACE_OUTER_BOUND ( 'NONE', #23322, .T. ) ;
#2108=LINE ( 'NONE', #47928, #14368 ) ;
#2122=CARTESIAN_POINT ( 'NONE',  ( 0.000000000000000000, -62.50884508063395373, -41.76106447765554464 ) ) ;
#2126=DIRECTION ( 'NONE',  ( -1.000000000000000000, 0.000000000000000000, 0.000000000000000000 ) ) ;
#2128=LINE ( 'NONE', #12254, #7315 ) ;
#2131=AXIS2_PLACEMENT_3D ( 'NONE', #4098, #37188, #72118 ) ;
#2136=VERTEX_POINT ( 'NONE', #73283 ) ;
#2143=ORIENTED_EDGE ( 'NONE', *, *, #26142, .T. ) ;
#2152=ORIENTED_EDGE ( 'NONE', *, *, #9221, .F. ) ;
#2153=CIRCLE ( 'NONE', #54916, 77.49899999999999523 ) ;
#2159=CYLINDRICAL_SURFACE ( 'NONE', #33991, 32.00000000000000000 ) ;
#2161=CYLINDRICAL_SURFACE ( 'NONE', #44701, 77.49899999999999523 ) ;
#2168=EDGE_LOOP ( 'NONE', ( #30262, #12321, #9359, #63638 ) ) ;
#2169=VERTEX_POINT ( 'NONE', #37245 ) ;
#2174=CARTESIAN_POINT ( 'NONE',  ( 10.00000000000000000, 76.69515212746057387, -29.01471420065480089 ) ) ;
#2182=CARTESIAN_POINT ( 'NONE',  ( 0.000000000000000000, -10.30890764327441822, 81.34940948281332851 ) ) ;
#2194=EDGE_CURVE ( 'NONE', #58172, #67479, #30195, .T. ) ;
#2219=CARTESIAN_POINT ( 'NONE',  ( 10.00000000000000000, 40.65526001592612459, 71.21200624218811015 ) ) ;
#2222=CARTESIAN_POINT ( 'NONE',  ( 0.000000000000000000, 75.16055320797057959, -18.89407956138176914 ) ) ;
#2236=CARTESIAN_POINT ( 'NONE',  ( 10.00000000000000000, -55.20638768913797634, 51.02545421589302777 ) ) ;
#2243=ORIENTED_EDGE ( 'NONE', *, *, #9495, .F. ) ;
#2251=AXIS2_PLACEMENT_3D ( 'NONE', #31758, #14848, #42685 ) ;
#2263=ADVANCED_FACE ( 'NONE', ( #10505 ), #63510, .T. ) ;
#2272=ORIENTED_EDGE ( 'NONE', *, *, #68865, .F. ) ;
#2278=AXIS2_PLACEMENT_3D ( 'NONE', #66936, #15819, #38749 ) ;
#2280=ORIENTED_EDGE ( 'NONE', *, *, #62245, .F. ) ;
#2281=DIRECTION ( 'NONE',  ( -1.000000000000000000, 0.000000000000000000, -0.000000000000000000 ) ) ;
#2292=DIRECTION ( 'NONE',  ( 0.000000000000000000, 0.9969173337331281859, -0.07845909572784168229 ) ) ;
#2300=CYLINDRICAL_SURFACE ( 'NONE', #76, 82.00000000000000000 ) ;
#2303=CARTESIAN_POINT ( 'NONE',  ( 10.00000000000000000, 65.64334221924909230, 41.19522573413756561 ) ) ;
#2304=VECTOR ( 'NONE', #20815, 1000.000000000000000 ) ;
#2331=EDGE_CURVE ( 'NONE', #38213, #8802, #40450, .T. ) ;
#2335=ORIENTED_EDGE ( 'NONE', *, *, #52197, .T. ) ;
#2358=ORIENTED_EDGE ( 'NONE', *, *, #34277, .T. ) ;
#2359=DIRECTION ( 'NONE',  ( 1.000000000000000000, 0.000000000000000000, 0.000000000000000000 ) ) ;
#2364=AXIS2_PLACEMENT_3D ( 'NONE', #9678, #43903, #15309 ) ;
#2383=EDGE_LOOP ( 'NONE', ( #10793, #2879, #10748, #24982 ) ) ;
#2385=DIRECTION ( 'NONE',  ( 0.000000000000000000, 0.000000000000000000, 1.000000000000000000 ) ) ;
#2393=CARTESIAN_POINT ( 'NONE',  ( 10.00000000000000000, 0.000000000000000000, 0.000000000000000000 ) ) ;
#2407=EDGE_LOOP ( 'NONE', ( #7210, #21070, #63186, #27827 ) ) ;
#2413=DIRECTION ( 'NONE',  ( -1.000000000000000000, 0.000000000000000000, 0.000000000000000000 ) ) ;
#2424=LINE ( 'NONE', #24211, #31417 ) ;
#2429=AXIS2_PLACEMENT_3D ( 'NONE', #58772, #30182, #64785 ) ;
#2443=ORIENTED_EDGE ( 'NONE', *, *, #32516, .F. ) ;
#2448=VECTOR ( 'NONE', #71191, 1000.000000000000000 ) ;
#2451=ORIENTED_EDGE ( 'NONE', *, *, #40250, .T. ) ;
#2452=ORIENTED_EDGE ( 'NONE', *, *, #42883, .T. ) ;
#2461=ORIENTED_EDGE ( 'NONE', *, *, #25863, .T. ) ;
#2463=ORIENTED_EDGE ( 'NONE', *, *, #9082, .T. ) ;
#2470=CARTESIAN_POINT ( 'NONE',  ( 10.00000000000000000, 0.000000000000000000, 0.000000000000000000 ) ) ;
#2476=AXIS2_PLACEMENT_3D ( 'NONE', #9904, #31717, #71941 ) ;
#2480=DIRECTION ( 'NONE',  ( -1.000000000000000000, -0.000000000000000000, 0.000000000000000000 ) ) ;
#2482=DIRECTION ( 'NONE',  ( 0.000000000000000000, 0.000000000000000000, 1.000000000000000000 ) ) ;
#2484=VECTOR ( 'NONE', #12704, 1000.000000000000000 ) ;
#2487=CIRCLE ( 'NONE', #21635, 32.00000000000000711 ) ;
#2492=FACE_OUTER_BOUND ( 'NONE', #52801, .T. ) ;
#2507=FACE_OUTER_BOUND ( 'NONE', #72844, .T. ) ;
#2512=AXIS2_PLACEMENT_3D ( 'NONE', #8401, #1039, #71159 ) ;
#2520=ORIENTED_EDGE ( 'NONE', *, *, #39666, .F. ) ;
#2521=EDGE_CURVE ( 'NONE', #14991, #24836, #69662, .T. ) ;
#2522=CARTESIAN_POINT ( 'NONE',  ( 5.000000000000000000, -56.15606465354917276, -59.75363087400133111 ) ) ;
#2530=ORIENTED_EDGE ( 'NONE', *, *, #43715, .F. ) ;
#2558=ORIENTED_EDGE ( 'NONE', *, *, #6028, .T. ) ;
#2565=CARTESIAN_POINT ( 'NONE',  ( 10.00000000000000000, 0.000000000000000000, 0.000000000000000000 ) ) ;
#2584=EDGE_CURVE ( 'NONE', #70598, #34383, #43273, .T. ) ;
#2585=DIRECTION ( 'NONE',  ( -1.000000000000000000, 0.000000000000000000, -0.000000000000000000 ) ) ;
#2588=EDGE_CURVE ( 'NONE', #49292, #19761, #72634, .T. ) ;
#2591=DIRECTION ( 'NONE',  ( -1.000000000000000000, -0.000000000000000000, 0.000000000000000000 ) ) ;
#2599=PRODUCT_DEFINITION_CONTEXT ( 'detailed design', #26332, 'design' ) ;
#2601=ORIENTED_EDGE ( 'NONE', *, *, #24062, .F. ) ;
#2603=CIRCLE ( 'NONE', #23016, 82.00000000000000000 ) ;
#2609=ORIENTED_EDGE ( 'NONE', *, *, #47878, .F. ) ;
#2610=AXIS2_PLACEMENT_3D ( 'NONE', #25220, #48146, #13187 ) ;
#2613=FACE_OUTER_BOUND ( 'NONE', #73912, .T. ) ;
#2619=CARTESIAN_POINT ( 'NONE',  ( 10.00000000000000000, -74.74816331893453025, 33.71516098798714722 ) ) ;
#2626=CIRCLE ( 'NONE', #15789, 31.99999999999999289 ) ;
#2630=ORIENTED_EDGE ( 'NONE', *, *, #67247, .T. ) ;
#2631=CARTESIAN_POINT ( 'NONE',  ( 0.000000000000000000, 0.000000000000000000, 0.000000000000000000 ) ) ;
#2652=ORIENTED_EDGE ( 'NONE', *, *, #47022, .F. ) ;
#2655=ORIENTED_EDGE ( 'NONE', *, *, #22354, .T. ) ;
#2673=ADVANCED_FACE ( 'NONE', ( #21310 ), #9679, .T. ) ;
#2676=CARTESIAN_POINT ( 'NONE',  ( 10.00000000000000000, 77.49459641780886443, -0.8261519478433788644 ) ) ;
#2683=ADVANCED_FACE ( 'NONE', ( #10046 ), #55913, .T. ) ;
#2684=LINE ( 'NONE', #60176, #47258 ) ;
#2690=DIRECTION ( 'NONE',  ( -1.000000000000000000, 0.000000000000000000, 0.000000000000000000 ) ) ;
#2703=EDGE_LOOP ( 'NONE', ( #42664, #9447, #53288, #40165 ) ) ;
#2706=ORIENTED_EDGE ( 'NONE', *, *, #48892, .T. ) ;
#2715=ORIENTED_EDGE ( 'NONE', *, *, #48309, .T. ) ;
#2716=VERTEX_POINT ( 'NONE', #60819 ) ;
#2735=VERTEX_POINT ( 'NONE', #34839 ) ;
#2743=CARTESIAN_POINT ( 'NONE',  ( 10.00000000000000000, 66.50666863322000211, 39.78640506895629869 ) ) ;
#2750=AXIS2_PLACEMENT_3D ( 'NONE', #51429, #69825, #23260 ) ;
#2753=DIRECTION ( 'NONE',  ( 1.000000000000000000, -0.000000000000000000, 0.000000000000000000 ) ) ;
#2764=DIRECTION ( 'NONE',  ( 0.000000000000000000, -1.000000000000000000, -1.047444401652940007E-14 ) ) ;
#2769=CARTESIAN_POINT ( 'NONE',  ( 10.00000000000000000, 72.35432306680455383, 20.40083707023012494 ) ) ;
#2770=DIRECTION ( 'NONE',  ( 0.000000000000000000, 0.9510565162951521989, 0.3090169943749515591 ) ) ;
#2771=EDGE_CURVE ( 'NONE', #41920, #17282, #12242, .T. ) ;
#2782=EDGE_CURVE ( 'NONE', #44699, #57645, #37233, .T. ) ;
#2787=VERTEX_POINT ( 'NONE', #73194 ) ;
#2788=CARTESIAN_POINT ( 'NONE',  ( 10.00000000000000000, -77.49459641780886443, 0.8261519478428377417 ) ) ;
#2789=CARTESIAN_POINT ( 'NONE',  ( 10.00000000000000000, -62.20884554314051940, 46.21855187248608132 ) ) ;
#2795=FACE_OUTER_BOUND ( 'NONE', #71475, .T. ) ;
#2796=DIRECTION ( 'NONE',  ( 1.000000000000000000, -0.000000000000000000, -0.000000000000000000 ) ) ;
#2798=AXIS2_PLACEMENT_3D ( 'NONE', #44666, #50650, #28092 ) ;
#2799=DIRECTION ( 'NONE',  ( 0.000000000000000000, 0.000000000000000000, 1.000000000000000000 ) ) ;
#2805=ORIENTED_EDGE ( 'NONE', *, *, #18353, .F. ) ;
#2815=EDGE_CURVE ( 'NONE', #73400, #54114, #21592, .T. ) ;
#2823=DIRECTION ( 'NONE',  ( -1.000000000000000000, 0.000000000000000000, -0.000000000000000000 ) ) ;
#2836=CARTESIAN_POINT ( 'NONE',  ( 10.00000000000000000, 0.000000000000000000, 0.000000000000000000 ) ) ;
#2844=DIRECTION ( 'NONE',  ( 0.000000000000000000, 0.000000000000000000, -1.000000000000000000 ) ) ;
#2854=ORIENTED_EDGE ( 'NONE', *, *, #39839, .T. ) ;
#2864=DIRECTION ( 'NONE',  ( -1.000000000000000000, 0.000000000000000000, -0.000000000000000000 ) ) ;
#2871=ORIENTED_EDGE ( 'NONE', *, *, #7905, .F. ) ;
#2877=AXIS2_PLACEMENT_3D ( 'NONE', #16872, #21757, #29236 ) ;
#2878=FACE_OUTER_BOUND ( 'NONE', #21917, .T. ) ;
#2879=ORIENTED_EDGE ( 'NONE', *, *, #37598, .T. ) ;
#2885=VERTEX_POINT ( 'NONE', #22837 ) ;
#2888=DIRECTION ( 'NONE',  ( 0.000000000000000000, 0.000000000000000000, 1.000000000000000000 ) ) ;
#2891=CIRCLE ( 'NONE', #60511, 32.00000000000000000 ) ;
#2898=ORIENTED_EDGE ( 'NONE', *, *, #29089, .F. ) ;
#2900=EDGE_LOOP ( 'NONE', ( #16411, #48435, #30762, #25608 ) ) ;
#2905=EDGE_CURVE ( 'NONE', #68809, #19857, #17741, .T. ) ;
#2908=DIRECTION ( 'NONE',  ( -1.000000000000000000, -0.000000000000000000, -0.000000000000000000 ) ) ;
#2931=CYLINDRICAL_SURFACE ( 'NONE', #60054, 31.99999999999999289 ) ;
#2941=DIRECTION ( 'NONE',  ( 0.000000000000000000, -0.5224985647159379187, -0.8526401643540989506 ) ) ;
#2954=CIRCLE ( 'NONE', #6527, 31.99999999999998934 ) ;
#2956=FACE_OUTER_BOUND ( 'NONE', #24596, .T. ) ;
#2958=DIRECTION ( 'NONE',  ( 0.000000000000000000, 0.000000000000000000, -1.000000000000000000 ) ) ;
#2959=VERTEX_POINT ( 'NONE', #11566 ) ;
#2968=CARTESIAN_POINT ( 'NONE',  ( 10.00000000000000000, 20.41045688087930898, -72.35160999960793049 ) ) ;
#2969=CYLINDRICAL_SURFACE ( 'NONE', #31130, 31.99999999999999289 ) ;
#2977=EDGE_LOOP ( 'NONE', ( #29074, #48341, #59458, #63020 ) ) ;
#2982=CARTESIAN_POINT ( 'NONE',  ( 10.00000000000000000, 8.830959090343430518, -74.65491531819107252 ) ) ;
#2983=VERTEX_POINT ( 'NONE', #56337 ) ;
#2989=VERTEX_POINT ( 'NONE', #10461 ) ;
#2992=EDGE_CURVE ( 'NONE', #23616, #17390, #35761, .T. ) ;
#3001=CIRCLE ( 'NONE', #37811, 77.49900000000000944 ) ;
#3003=VECTOR ( 'NONE', #38102, 1000.000000000000000 ) ;
#3004=EDGE_LOOP ( 'NONE', ( #18199, #49944, #33070, #14403 ) ) ;
#3030=AXIS2_PLACEMENT_3D ( 'NONE', #47815, #37293, #43313 ) ;
#3040=DIRECTION ( 'NONE',  ( -1.000000000000000000, 0.000000000000000000, 0.000000000000000000 ) ) ;
#3042=DIRECTION ( 'NONE',  ( 0.000000000000000000, 0.7604059656000323741, -0.6494480483301819929 ) ) ;
#3054=AXIS2_PLACEMENT_3D ( 'NONE', #56998, #55872, #38586 ) ;
#3069=ORIENTED_EDGE ( 'NONE', *, *, #73929, .F. ) ;
#3080=DIRECTION ( 'NONE',  ( 0.000000000000000000, 0.000000000000000000, 1.000000000000000000 ) ) ;
#3097=DIRECTION ( 'NONE',  ( -1.000000000000000000, 0.000000000000000000, 0.000000000000000000 ) ) ;
#3111=FACE_OUTER_BOUND ( 'NONE', #7678, .T. ) ;
#3113=DIRECTION ( 'NONE',  ( -1.000000000000000000, 0.000000000000000000, -0.000000000000000000 ) ) ;
#3114=CARTESIAN_POINT ( 'NONE',  ( 10.00000000000000000, -74.18225833017913828, 34.94270380257611919 ) ) ;
#3115=AXIS2_PLACEMENT_3D ( 'NONE', #27651, #44207, #67132 ) ;
#3116=CYLINDRICAL_SURFACE ( 'NONE', #52674, 31.99999999999999289 ) ;
#3131=CARTESIAN_POINT ( 'NONE',  ( 10.00000000000000000, 12.93880638057426502, -76.41127070299258150 ) ) ;
#3134=DIRECTION ( 'NONE',  ( -1.000000000000000000, -0.000000000000000000, 0.000000000000000000 ) ) ;
#3147=EDGE_CURVE ( 'NONE', #37997, #28262, #3390, .T. ) ;
#3152=SURFACE_STYLE_USAGE ( .BOTH. , #60287 ) ;
#3153=ORIENTED_EDGE ( 'NONE', *, *, #48309, .F. ) ;
#3171=CIRCLE ( 'NONE', #27161, 82.00000000000000000 ) ;
#3184=CARTESIAN_POINT ( 'NONE',  ( 0.000000000000000000, 0.000000000000000000, 0.000000000000000000 ) ) ;
#3198=ORIENTED_EDGE ( 'NONE', *, *, #7259, .F. ) ;
#3204=CARTESIAN_POINT ( 'NONE',  ( 10.00000000000000000, -58.39081064771787766, 50.95692526931307498 ) ) ;
#3217=AXIS2_PLACEMENT_3D ( 'NONE', #63207, #69202, #47015 ) ;
#3223=AXIS2_PLACEMENT_3D ( 'NONE', #73039, #21545, #15918 ) ;
#3231=EDGE_CURVE ( 'NONE', #21174, #44951, #29813, .T. ) ;
#3239=CARTESIAN_POINT ( 'NONE',  ( 10.00000000000000000, -51.29473840253178452, -63.97538442413483750 ) ) ;
#3257=EDGE_CURVE ( 'NONE', #43589, #21187, #37020, .T. ) ;
#3259=DIRECTION ( 'NONE',  ( 0.000000000000000000, -0.5224985647159560154, 0.8526401643540879594 ) ) ;
#3261=AXIS2_PLACEMENT_3D ( 'NONE', #32711, #72563, #62054 ) ;
#3280=CIRCLE ( 'NONE', #32050, 77.49899999999999523 ) ;
#3287=CYLINDRICAL_SURFACE ( 'NONE', #69048, 32.00000000000000000 ) ;
#3290=DIRECTION ( 'NONE',  ( -1.000000000000000000, -0.000000000000000000, 0.000000000000000000 ) ) ;
#3295=AXIS2_PLACEMENT_3D ( 'NONE', #5928, #35579, #35949 ) ;
#3305=CARTESIAN_POINT ( 'NONE',  ( 5.000000000000000000, 56.15606465355042332, -59.75363087400017292 ) ) ;
#3310=CARTESIAN_POINT ( 'NONE',  ( 10.00000000000000000, -80.28980883073768382, 16.65972982744906972 ) ) ;
#3321=ORIENTED_EDGE ( 'NONE', *, *, #25537, .F. ) ;
#3326=CIRCLE ( 'NONE', #44190, 32.00000000000000000 ) ;
#3332=DIRECTION ( 'NONE',  ( 0.000000000000000000, 0.9510565162951544194, -0.3090169943749446757 ) ) ;
#3338=VERTEX_POINT ( 'NONE', #66056 ) ;
#3348=DIRECTION ( 'NONE',  ( 0.000000000000000000, 0.5877852522924685852, 0.8090169943749507819 ) ) ;
#3359=DIRECTION ( 'NONE',  ( -1.000000000000000000, 0.000000000000000000, 0.000000000000000000 ) ) ;
#3367=EDGE_LOOP ( 'NONE', ( #6658, #24611, #8874, #51856 ) ) ;
#3369=VERTEX_POINT ( 'NONE', #22028 ) ;
#3378=ORIENTED_EDGE ( 'NONE', *, *, #63066, .F. ) ;
#3381=EDGE_LOOP ( 'NONE', ( #68818, #29763, #35375, #48631 ) ) ;
#3383=DIRECTION ( 'NONE',  ( 0.000000000000000000, -0.9969173337331287410, 0.07845909572783495156 ) ) ;
#3390=CIRCLE ( 'NONE', #15380, 77.49900000000002365 ) ;
#3406=DIRECTION ( 'NONE',  ( 0.000000000000000000, 0.000000000000000000, 1.000000000000000000 ) ) ;
#3408=FACE_OUTER_BOUND ( 'NONE', #15745, .T. ) ;
#3420=ORIENTED_EDGE ( 'NONE', *, *, #4156, .F. ) ;
#3423=DIRECTION ( 'NONE',  ( 0.000000000000000000, 0.000000000000000000, 1.000000000000000000 ) ) ;
#3424=ORIENTED_EDGE ( 'NONE', *, *, #36379, .F. ) ;
#3427=ORIENTED_EDGE ( 'NONE', *, *, #42184, .T. ) ;
#3429=CIRCLE ( 'NONE', #56287, 31.99999999999999645 ) ;
#3430=ORIENTED_EDGE ( 'NONE', *, *, #68282, .F. ) ;
#3432=ORIENTED_EDGE ( 'NONE', *, *, #69590, .F. ) ;
#3437=ORIENTED_EDGE ( 'NONE', *, *, #44984, .F. ) ;
#3446=ORIENTED_EDGE ( 'NONE', *, *, #45007, .F. ) ;
#3460=CARTESIAN_POINT ( 'NONE',  ( 5.000000000000002665, 22.90783923731629912, 78.73519480814962890 ) ) ;
#3462=EDGE_LOOP ( 'NONE', ( #44510, #51328, #29841, #41810 ) ) ;
#3472=AXIS2_PLACEMENT_3D ( 'NONE', #10217, #62491, #33511 ) ;
#3491=AXIS2_PLACEMENT_3D ( 'NONE', #40604, #16936, #5666 ) ;
#3497=VECTOR ( 'NONE', #72553, 1000.000000000000000 ) ;
#3516=SURFACE_STYLE_FILL_AREA ( #32785 ) ;
#3525=AXIS2_PLACEMENT_3D ( 'NONE', #7787, #30705, #352 ) ;
#3527=LINE ( 'NONE', #26053, #73000 ) ;
#3537=EDGE_LOOP ( 'NONE', ( #43275, #49723, #49201, #1769 ) ) ;
#3542=AXIS2_PLACEMENT_3D ( 'NONE', #20647, #60510, #54854 ) ;
#3546=VERTEX_POINT ( 'NONE', #46825 ) ;
#3557=CARTESIAN_POINT ( 'NONE',  ( 5.000000000000002665, 44.99326035066052043, 68.55367621811159040 ) ) ;
#3563=EDGE_LOOP ( 'NONE', ( #62760, #42019, #42563, #74132 ) ) ;
#3577=DIRECTION ( 'NONE',  ( 0.000000000000000000, 0.000000000000000000, 1.000000000000000000 ) ) ;
#3583=AXIS2_PLACEMENT_3D ( 'NONE', #69198, #34986, #16576 ) ;
#3584=ORIENTED_EDGE ( 'NONE', *, *, #2089, .T. ) ;
#3588=CIRCLE ( 'NONE', #71971, 77.49899999999999523 ) ;
#3593=DIRECTION ( 'NONE',  ( -1.000000000000000000, -0.000000000000000000, 0.000000000000000000 ) ) ;
#3596=FACE_OUTER_BOUND ( 'NONE', #73753, .T. ) ;
#3597=DIRECTION ( 'NONE',  ( -1.000000000000000000, 0.000000000000000000, -0.000000000000000000 ) ) ;
#3606=VERTEX_POINT ( 'NONE', #69738 ) ;
#3607=CYLINDRICAL_SURFACE ( 'NONE', #16067, 77.49899999999999523 ) ;
#3619=EDGE_LOOP ( 'NONE', ( #32437, #43961, #12188, #63772 ) ) ;
#3622=LINE ( 'NONE', #64911, #16461 ) ;
#3628=ORIENTED_EDGE ( 'NONE', *, *, #36380, .T. ) ;
#3629=ORIENTED_EDGE ( 'NONE', *, *, #43544, .F. ) ;
#3631=ORIENTED_EDGE ( 'NONE', *, *, #67763, .T. ) ;
#3640=DIRECTION ( 'NONE',  ( -1.000000000000000000, -0.000000000000000000, -0.000000000000000000 ) ) ;
#3647=ORIENTED_EDGE ( 'NONE', *, *, #5984, .T. ) ;
#3650=CYLINDRICAL_SURFACE ( 'NONE', #24652, 77.49899999999999523 ) ;
#3659=VECTOR ( 'NONE', #29771, 1000.000000000000000 ) ;
#3665=CARTESIAN_POINT ( 'NONE',  ( 10.00000000000000000, 0.000000000000000000, 0.000000000000000000 ) ) ;
#3669=CARTESIAN_POINT ( 'NONE',  ( 10.00000000000000000, -36.73666225445845157, -65.58780272294114866 ) ) ;
#3699=EDGE_CURVE ( 'NONE', #63343, #24857, #63791, .T. ) ;
#3707=EDGE_LOOP ( 'NONE', ( #55650, #35318, #18488, #33643 ) ) ;
#3712=DIRECTION ( 'NONE',  ( 0.000000000000000000, 0.000000000000000000, 1.000000000000000000 ) ) ;
#3714=CYLINDRICAL_SURFACE ( 'NONE', #5094, 77.49899999999999523 ) ;
#3721=CARTESIAN_POINT ( 'NONE',  ( 10.00000000000000000, -6.903761155838323837, 77.19088730480521576 ) ) ;
#3728=VERTEX_POINT ( 'NONE', #14813 ) ;
#3734=CIRCLE ( 'NONE', #36122, 31.99999999999998934 ) ;
#3743=DIRECTION ( 'NONE',  ( -1.000000000000000000, 0.000000000000000000, 0.000000000000000000 ) ) ;
#3746=DIRECTION ( 'NONE',  ( -1.000000000000000000, 0.000000000000000000, 0.000000000000000000 ) ) ;
#3755=DIRECTION ( 'NONE',  ( -1.000000000000000000, -0.000000000000000000, -0.000000000000000000 ) ) ;
#3756=AXIS2_PLACEMENT_3D ( 'NONE', #18711, #48399, #64586 ) ;
#3760=AXIS2_PLACEMENT_3D ( 'NONE', #41274, #46179, #1096 ) ;
#3765=CARTESIAN_POINT ( 'NONE',  ( 0.000000000000000000, -31.46837873495025306, 68.27212725128265447 ) ) ;
#3772=ADVANCED_FACE ( 'NONE', ( #2098 ), #26463, .T. ) ;
#3793=DIRECTION ( 'NONE',  ( -1.000000000000000000, 0.000000000000000000, 0.000000000000000000 ) ) ;
#3798=ORIENTED_EDGE ( 'NONE', *, *, #38873, .F. ) ;
#3800=ORIENTED_EDGE ( 'NONE', *, *, #45855, .T. ) ;
#3816=CARTESIAN_POINT ( 'NONE',  ( 0.000000000000000000, 3.894527615417891830, 81.90746397400390322 ) ) ;
#3819=ORIENTED_EDGE ( 'NONE', *, *, #29963, .F. ) ;
#3828=EDGE_CURVE ( 'NONE', #25432, #11811, #30985, .T. ) ;
#3833=ORIENTED_EDGE ( 'NONE', *, *, #21695, .T. ) ;
#3838=DIRECTION ( 'NONE',  ( 0.000000000000000000, -0.2334453638558921240, -0.9723699203976797767 ) ) ;
#3843=LINE ( 'NONE', #60249, #15107 ) ;
#3846=VERTEX_POINT ( 'NONE', #60331 ) ;
#3848=CARTESIAN_POINT ( 'NONE',  ( 10.00000000000000000, -75.11725578898470701, 2.956366410620372864 ) ) ;
#3850=CIRCLE ( 'NONE', #5088, 82.00000000000000000 ) ;
#3853=FACE_OUTER_BOUND ( 'NONE', #12917, .T. ) ;
#3859=CIRCLE ( 'NONE', #68690, 77.49899999999999523 ) ;
#3873=DIRECTION ( 'NONE',  ( -1.000000000000000000, -0.000000000000000000, 0.000000000000000000 ) ) ;
#3880=DIRECTION ( 'NONE',  ( 0.000000000000000000, -0.9238795325112822976, -0.3826834323651006065 ) ) ;
#3881=EDGE_LOOP ( 'NONE', ( #65203, #38921, #68388, #512 ) ) ;
#3891=DIRECTION ( 'NONE',  ( -1.000000000000000000, -0.000000000000000000, 0.000000000000000000 ) ) ;
#3893=ORIENTED_EDGE ( 'NONE', *, *, #2331, .T. ) ;
#3899=EDGE_LOOP ( 'NONE', ( #61490, #28946, #72561, #15672 ) ) ;
#3906=VERTEX_POINT ( 'NONE', #61433 ) ;
#3907=EDGE_CURVE ( 'NONE', #72957, #57222, #31340, .T. ) ;
#3910=VECTOR ( 'NONE', #47247, 1000.000000000000000 ) ;
#3913=AXIS2_PLACEMENT_3D ( 'NONE', #26014, #54957, #50429 ) ;
#3922=DIRECTION ( 'NONE',  ( -1.000000000000000000, 0.000000000000000000, -0.000000000000000000 ) ) ;
#3930=ORIENTED_EDGE ( 'NONE', *, *, #18930, .T. ) ;
#3935=CARTESIAN_POINT ( 'NONE',  ( 10.00000000000000000, 66.50666863322055633, -39.78640506895536078 ) ) ;
#3936=LINE ( 'NONE', #31362, #55736 ) ;
#3941=ORIENTED_EDGE ( 'NONE', *, *, #25151, .F. ) ;
#3947=FACE_OUTER_BOUND ( 'NONE', #45265, .T. ) ;
#3950=ORIENTED_EDGE ( 'NONE', *, *, #64499, .F. ) ;
#3960=CARTESIAN_POINT ( 'NONE',  ( 5.000000000000002665, 8.966570791700698706, 81.50828551894228724 ) ) ;
#3961=DIRECTION ( 'NONE',  ( -1.000000000000000000, -0.000000000000000000, -0.000000000000000000 ) ) ;
#3975=VERTEX_POINT ( 'NONE', #39612 ) ;
#3983=DIRECTION ( 'NONE',  ( 0.000000000000000000, -0.5224985647159380298, -0.8526401643540988395 ) ) ;
#3986=CARTESIAN_POINT ( 'NONE',  ( 10.00000000000000000, -73.73191006444561424, -14.66109333815538918 ) ) ;
#4010=DIRECTION ( 'NONE',  ( -1.000000000000000000, -0.000000000000000000, 0.000000000000000000 ) ) ;
#4016=ORIENTED_EDGE ( 'NONE', *, *, #50828, .T. ) ;
#4025=ORIENTED_EDGE ( 'NONE', *, *, #32418, .T. ) ;
#4032=EDGE_CURVE ( 'NONE', #66307, #24726, #2626, .T. ) ;
#4034=CYLINDRICAL_SURFACE ( 'NONE', #19186, 82.00000000000000000 ) ;
#4035=CYLINDRICAL_SURFACE ( 'NONE', #45006, 82.00000000000000000 ) ;
#4038=VERTEX_POINT ( 'NONE', #1284 ) ;
#4045=CARTESIAN_POINT ( 'NONE',  ( 0.000000000000000000, 59.03342792756328095, -46.54456581323744757 ) ) ;
#4052=DIRECTION ( 'NONE',  ( 0.000000000000000000, 0.000000000000000000, 1.000000000000000000 ) ) ;
#4066=EDGE_CURVE ( 'NONE', #38196, #69125, #18510, .T. ) ;
#4068=CARTESIAN_POINT ( 'NONE',  ( 10.00000000000000000, 0.000000000000000000, 0.000000000000000000 ) ) ;
#4071=ORIENTED_EDGE ( 'NONE', *, *, #71960, .F. ) ;
#4087=ORIENTED_EDGE ( 'NONE', *, *, #33857, .T. ) ;
#4092=DIRECTION ( 'NONE',  ( -1.000000000000000000, 0.000000000000000000, -0.000000000000000000 ) ) ;
#4097=EDGE_LOOP ( 'NONE', ( #8400, #30258, #58601, #31056 ) ) ;
#4098=CARTESIAN_POINT ( 'NONE',  ( 10.00000000000000000, 26.01480285779933510, -70.53064760720289428 ) ) ;
#4099=AXIS2_PLACEMENT_3D ( 'NONE', #48912, #30144, #57462 ) ;
#4100=ORIENTED_EDGE ( 'NONE', *, *, #45139, .F. ) ;
#4114=DIRECTION ( 'NONE',  ( -1.000000000000000000, 0.000000000000000000, 0.000000000000000000 ) ) ;
#4116=ORIENTED_EDGE ( 'NONE', *, *, #60967, .F. ) ;
#4119=CIRCLE ( 'NONE', #46126, 82.00000000000000000 ) ;
#4124=EDGE_CURVE ( 'NONE', #464, #73769, #58993, .T. ) ;
#4125=AXIS2_PLACEMENT_3D ( 'NONE', #11430, #27616, #22735 ) ;
#4127=CARTESIAN_POINT ( 'NONE',  ( 0.000000000000000000, 0.000000000000000000, 0.000000000000000000 ) ) ;
#4128=CARTESIAN_POINT ( 'NONE',  ( 10.00000000000000000, 0.000000000000000000, 0.000000000000000000 ) ) ;
#4131=AXIS2_PLACEMENT_3D ( 'NONE', #11065, #55812, #33988 ) ;
#4135=CYLINDRICAL_SURFACE ( 'NONE', #54173, 82.00000000000000000 ) ;
#4137=CYLINDRICAL_SURFACE ( 'NONE', #71660, 32.00000000000000000 ) ;
#4138=DIRECTION ( 'NONE',  ( 0.000000000000000000, -0.3090169943749349057, -0.9510565162951577500 ) ) ;
#4143=AXIS2_PLACEMENT_3D ( 'NONE', #45244, #21544, #27177 ) ;
#4145=DIRECTION ( 'NONE',  ( -1.000000000000000000, 0.000000000000000000, -0.000000000000000000 ) ) ;
#4149=CARTESIAN_POINT ( 'NONE',  ( 10.00000000000000000, 0.000000000000000000, 0.000000000000000000 ) ) ;
#4150=CARTESIAN_POINT ( 'NONE',  ( 10.00000000000000000, -71.91182617369167929, -28.89263327155822481 ) ) ;
#4152=DIRECTION ( 'NONE',  ( 0.000000000000000000, 0.000000000000000000, 1.000000000000000000 ) ) ;
#4153=CIRCLE ( 'NONE', #20932, 82.00000000000000000 ) ;
#4156=EDGE_CURVE ( 'NONE', #21857, #16649, #22997, .T. ) ;
#4161=ORIENTED_EDGE ( 'NONE', *, *, #67886, .F. ) ;
#4175=ORIENTED_EDGE ( 'NONE', *, *, #3231, .F. ) ;
#4178=VERTEX_POINT ( 'NONE', #31274 ) ;
#4193=ORIENTED_EDGE ( 'NONE', *, *, #31760, .F. ) ;
#4217=ORIENTED_EDGE ( 'NONE', *, *, #66382, .T. ) ;
#4225=ORIENTED_EDGE ( 'NONE', *, *, #52828, .F. ) ;
#4228=CIRCLE ( 'NONE', #47413, 31.99999999999998934 ) ;
#4239=LINE ( 'NONE', #50063, #59899 ) ;
#4240=VECTOR ( 'NONE', #48745, 1000.000000000000000 ) ;
#4244=ORIENTED_EDGE ( 'NONE', *, *, #37598, .F. ) ;
#4246=DIRECTION ( 'NONE',  ( -1.000000000000000000, 0.000000000000000000, 0.000000000000000000 ) ) ;
#4252=LINE ( 'NONE', #15508, #23496 ) ;
#4255=DIRECTION ( 'NONE',  ( -1.000000000000000000, -0.000000000000000000, 0.000000000000000000 ) ) ;
#4259=ORIENTED_EDGE ( 'NONE', *, *, #30626, .T. ) ;
#4261=AXIS2_PLACEMENT_3D ( 'NONE', #73789, #4288, #50495 ) ;
#4264=EDGE_LOOP ( 'NONE', ( #29324, #56595, #9271, #5112 ) ) ;
#4268=EDGE_CURVE ( 'NONE', #42280, #23222, #27805, .T. ) ;
#4269=ORIENTED_EDGE ( 'NONE', *, *, #12824, .F. ) ;
#4278=EDGE_LOOP ( 'NONE', ( #38221, #4962, #18769, #45811 ) ) ;
#4285=DIRECTION ( 'NONE',  ( 0.000000000000000000, 0.000000000000000000, 1.000000000000000000 ) ) ;
#4288=DIRECTION ( 'NONE',  ( -1.000000000000000000, 0.000000000000000000, 0.000000000000000000 ) ) ;
#4295=ORIENTED_EDGE ( 'NONE', *, *, #19924, .F. ) ;
#4298=AXIS2_PLACEMENT_3D ( 'NONE', #3665, #44891, #34704 ) ;
#4310=CARTESIAN_POINT ( 'NONE',  ( 0.000000000000000000, 0.000000000000000000, 0.000000000000000000 ) ) ;
#4314=CARTESIAN_POINT ( 'NONE',  ( 10.00000000000000000, -55.20638768913724448, -51.02545421589383068 ) ) ;
#4325=FACE_OUTER_BOUND ( 'NONE', #33187, .T. ) ;
#4332=FACE_OUTER_BOUND ( 'NONE', #71681, .T. ) ;
#4337=CARTESIAN_POINT ( 'NONE',  ( 10.00000000000000000, -46.21855187248583974, -62.20884554314070414 ) ) ;
#4355=DIRECTION ( 'NONE',  ( 0.000000000000000000, 0.8910065241883657894, 0.4539904997395510788 ) ) ;
#4362=VERTEX_POINT ( 'NONE', #447 ) ;
#4366=ADVANCED_FACE ( 'NONE', ( #68469 ), #74087, .T. ) ;
#4375=VERTEX_POINT ( 'NONE', #22981 ) ;
#4386=DIRECTION ( 'NONE',  ( -1.000000000000000000, -0.000000000000000000, -0.000000000000000000 ) ) ;
#4396=CIRCLE ( 'NONE', #17571, 82.00000000000000000 ) ;
#4410=DIRECTION ( 'NONE',  ( 0.000000000000000000, 0.000000000000000000, 1.000000000000000000 ) ) ;
#4414=DIRECTION ( 'NONE',  ( 0.000000000000000000, -0.5877852522924802425, 0.8090169943749422332 ) ) ;
#4422=EDGE_CURVE ( 'NONE', #11744, #36763, #50613, .T. ) ;
#4432=DIRECTION ( 'NONE',  ( 0.000000000000000000, 0.8526401643540936215, -0.5224985647159469115 ) ) ;
#4433=AXIS2_PLACEMENT_3D ( 'NONE', #64364, #12838, #11365 ) ;
#4435=DIRECTION ( 'NONE',  ( 0.000000000000000000, -0.9238795325112906243, 0.3826834323650805114 ) ) ;
#4439=AXIS2_PLACEMENT_3D ( 'NONE', #30977, #609, #58086 ) ;
#4443=FACE_OUTER_BOUND ( 'NONE', #55082, .T. ) ;
#4460=CARTESIAN_POINT ( 'NONE',  ( 0.000000000000000000, -3.894527615417340272, -81.90746397400393164 ) ) ;
#4468=CARTESIAN_POINT ( 'NONE',  ( 0.000000000000000000, 0.000000000000000000, 0.000000000000000000 ) ) ;
#4490=LINE ( 'NONE', #15001, #50657 ) ;
#4494=CARTESIAN_POINT ( 'NONE',  ( 10.00000000000000000, 0.000000000000000000, 0.000000000000000000 ) ) ;
#4500=ADVANCED_FACE ( 'NONE', ( #63940 ), #35362, .T. ) ;
#4504=DIRECTION ( 'NONE',  ( 0.000000000000000000, 0.000000000000000000, 1.000000000000000000 ) ) ;
#4508=CYLINDRICAL_SURFACE ( 'NONE', #5942, 31.99999999999999289 ) ;
#4516=DIRECTION ( 'NONE',  ( -1.000000000000000000, 0.000000000000000000, 0.000000000000000000 ) ) ;
#4517=VECTOR ( 'NONE', #28646, 1000.000000000000000 ) ;
#4528=EDGE_LOOP ( 'NONE', ( #12096, #4752, #50982, #43232 ) ) ;
#4538=ORIENTED_EDGE ( 'NONE', *, *, #61867, .T. ) ;
#4552=VERTEX_POINT ( 'NONE', #8639 ) ;
#4556=ORIENTED_EDGE ( 'NONE', *, *, #26728, .T. ) ;
#4561=DIRECTION ( 'NONE',  ( 0.000000000000000000, 0.000000000000000000, 1.000000000000000000 ) ) ;
#4566=ORIENTED_EDGE ( 'NONE', *, *, #65697, .F. ) ;
#4572=ADVANCED_FACE ( 'NONE', ( #53387 ), #7888, .T. ) ;
#4576=VERTEX_POINT ( 'NONE', #54134 ) ;
#4577=CARTESIAN_POINT ( 'NONE',  ( 10.00000000000000000, 0.000000000000000000, 0.000000000000000000 ) ) ;
#4580=DIRECTION ( 'NONE',  ( 0.000000000000000000, 8.881784197001252323E-16, 1.000000000000000000 ) ) ;
#4584=DIRECTION ( 'NONE',  ( 0.000000000000000000, -0.9876883405951359940, -0.1564344650402420267 ) ) ;
#4594=DIRECTION ( 'NONE',  ( -1.000000000000000000, -0.000000000000000000, 0.000000000000000000 ) ) ;
#4595=LINE ( 'NONE', #44062, #43459 ) ;
#4597=ORIENTED_EDGE ( 'NONE', *, *, #71131, .T. ) ;
#4602=DIRECTION ( 'NONE',  ( -1.000000000000000000, -0.000000000000000000, 0.000000000000000000 ) ) ;
#4612=EDGE_CURVE ( 'NONE', #52257, #7655, #14637, .T. ) ;
#4619=CIRCLE ( 'NONE', #38245, 31.99999999999999289 ) ;
#4625=EDGE_CURVE ( 'NONE', #63684, #13514, #39903, .T. ) ;
#4628=ORIENTED_EDGE ( 'NONE', *, *, #34209, .T. ) ;
#4643=ORIENTED_EDGE ( 'NONE', *, *, #52705, .T. ) ;
#4645=DIRECTION ( 'NONE',  ( -1.000000000000000000, 0.000000000000000000, -0.000000000000000000 ) ) ;
#4647=CIRCLE ( 'NONE', #61088, 31.99999999999999289 ) ;
#4648=ORIENTED_EDGE ( 'NONE', *, *, #28854, .F. ) ;
#4653=ORIENTED_EDGE ( 'NONE', *, *, #69543, .F. ) ;
#4665=ORIENTED_EDGE ( 'NONE', *, *, #33113, .T. ) ;
#4668=ORIENTED_EDGE ( 'NONE', *, *, #30390, .T. ) ;
#4671=CARTESIAN_POINT ( 'NONE',  ( 0.000000000000000000, 12.93880638057313703, 76.41127070299276625 ) ) ;
#4680=VERTEX_POINT ( 'NONE', #27775 ) ;
#4689=LINE ( 'NONE', #15941, #27928 ) ;
#4700=CYLINDRICAL_SURFACE ( 'NONE', #54500, 31.99999999999999289 ) ;
#4703=EDGE_CURVE ( 'NONE', #12767, #38196, #66297, .T. ) ;
#4704=VECTOR ( 'NONE', #44882, 1000.000000000000000 ) ;
#4709=VECTOR ( 'NONE', #60900, 1000.000000000000000 ) ;
#4717=VECTOR ( 'NONE', #6370, 1000.000000000000000 ) ;
#4721=EDGE_CURVE ( 'NONE', #63684, #72004, #4490, .T. ) ;
#4726=VECTOR ( 'NONE', #73917, 1000.000000000000000 ) ;
#4733=CIRCLE ( 'NONE', #37140, 77.49900000000000944 ) ;
#4737=CARTESIAN_POINT ( 'NONE',  ( 10.00000000000000000, 70.53064760720316428, -26.01480285779861035 ) ) ;
#4742=ORIENTED_EDGE ( 'NONE', *, *, #39248, .F. ) ;
#4749=DIRECTION ( 'NONE',  ( 0.000000000000000000, 0.000000000000000000, 1.000000000000000000 ) ) ;
#4750=CARTESIAN_POINT ( 'NONE',  ( 0.000000000000000000, 0.000000000000000000, 0.000000000000000000 ) ) ;
#4751=CARTESIAN_POINT ( 'NONE',  ( 0.000000000000000000, -77.19088730480518734, -6.903761155838607166 ) ) ;
#4752=ORIENTED_EDGE ( 'NONE', *, *, #36804, .T. ) ;
#4755=CYLINDRICAL_SURFACE ( 'NONE', #12267, 31.99999999999999289 ) ;
#4766=EDGE_CURVE ( 'NONE', #30680, #18834, #38651, .T. ) ;
#4770=CARTESIAN_POINT ( 'NONE',  ( 10.00000000000000000, -34.94270380257693631, 74.18225833017875459 ) ) ;
#4773=DIRECTION ( 'NONE',  ( -1.000000000000000000, 0.000000000000000000, 0.000000000000000000 ) ) ;
#4795=CARTESIAN_POINT ( 'NONE',  ( 10.00000000000000000, -14.66109333815513160, 73.73191006444567108 ) ) ;
#4799=DIRECTION ( 'NONE',  ( -1.000000000000000000, -0.000000000000000000, 0.000000000000000000 ) ) ;
#4803=EDGE_CURVE ( 'NONE', #17390, #70908, #9740, .T. ) ;
#4822=ORIENTED_EDGE ( 'NONE', *, *, #8818, .T. ) ;
#4824=LINE ( 'NONE', #21711, #40453 ) ;
#4831=ORIENTED_EDGE ( 'NONE', *, *, #62916, .T. ) ;
#4835=EDGE_LOOP ( 'NONE', ( #72208, #13219, #66492, #60132 ) ) ;
#4848=ORIENTED_EDGE ( 'NONE', *, *, #49124, .F. ) ;
#4850=EDGE_LOOP ( 'NONE', ( #36781, #6697, #23042, #734 ) ) ;
#4854=VERTEX_POINT ( 'NONE', #69477 ) ;
#4858=ADVANCED_FACE ( 'NONE', ( #11225 ), #28889, .T. ) ;
#4859=LINE ( 'NONE', #40159, #28726 ) ;
#4869=ORIENTED_EDGE ( 'NONE', *, *, #31668, .T. ) ;
#4878=CARTESIAN_POINT ( 'NONE',  ( 10.00000000000000000, 0.000000000000000000, 0.000000000000000000 ) ) ;
#4890=CARTESIAN_POINT ( 'NONE',  ( 10.00000000000000000, 51.03279382321088065, 55.19960302592086521 ) ) ;
#4894=CARTESIAN_POINT ( 'NONE',  ( 10.00000000000000000, 73.44644590900094272, -24.73286445877628026 ) ) ;
#4903=AXIS2_PLACEMENT_3D ( 'NONE', #40235, #68815, #57903 ) ;
#4906=DIRECTION ( 'NONE',  ( -1.000000000000000000, 0.000000000000000000, -0.000000000000000000 ) ) ;
#4909=ORIENTED_EDGE ( 'NONE', *, *, #68184, .F. ) ;
#4917=AXIS2_PLACEMENT_3D ( 'NONE', #69766, #19370, #29165 ) ;
#4921=CIRCLE ( 'NONE', #34910, 82.00000000000000000 ) ;
#4923=LINE ( 'NONE', #23669, #14876 ) ;
#4924=ORIENTED_EDGE ( 'NONE', *, *, #29692, .F. ) ;
#4926=FACE_OUTER_BOUND ( 'NONE', #14042, .T. ) ;
#4928=DIRECTION ( 'NONE',  ( 0.000000000000000000, -0.1564344650402381687, 0.9876883405951365491 ) ) ;
#4930=CARTESIAN_POINT ( 'NONE',  ( 10.00000000000000000, 36.72794159290241822, 65.59268652807223532 ) ) ;
#4932=EDGE_CURVE ( 'NONE', #65643, #65194, #63129, .T. ) ;
#4935=VERTEX_POINT ( 'NONE', #46189 ) ;
#4939=LINE ( 'NONE', #54933, #37867 ) ;
#4943=ADVANCED_FACE ( 'NONE', ( #35268 ), #58196, .T. ) ;
#4950=VERTEX_POINT ( 'NONE', #29604 ) ;
#4962=ORIENTED_EDGE ( 'NONE', *, *, #18672, .F. ) ;
#4977=DIRECTION ( 'NONE',  ( -1.000000000000000000, 0.000000000000000000, 0.000000000000000000 ) ) ;
#4979=AXIS2_PLACEMENT_3D ( 'NONE', #45562, #10573, #21864 ) ;
#4983=EDGE_LOOP ( 'NONE', ( #43169, #58255, #2871, #36329 ) ) ;
#4986=CARTESIAN_POINT ( 'NONE',  ( 0.000000000000000000, -11.30684508768284680, -76.66974797899850103 ) ) ;
#4987=VERTEX_POINT ( 'NONE', #20837 ) ;
#4990=AXIS2_PLACEMENT_3D ( 'NONE', #28690, #5421, #60790 ) ;
#4996=ORIENTED_EDGE ( 'NONE', *, *, #33929, .T. ) ;
#4999=DIRECTION ( 'NONE',  ( 0.000000000000000000, 0.9969173337331281859, -0.07845909572784180719 ) ) ;
#5001=EDGE_CURVE ( 'NONE', #59827, #71846, #68716, .T. ) ;
#5015=ORIENTED_EDGE ( 'NONE', *, *, #35075, .F. ) ;
#5017=LINE ( 'NONE', #33182, #46791 ) ;
#5021=ORIENTED_EDGE ( 'NONE', *, *, #5621, .F. ) ;
#5046=CARTESIAN_POINT ( 'NONE',  ( 10.00000000000000000, 36.73666225445894185, 65.58780272294090707 ) ) ;
#5051=ORIENTED_EDGE ( 'NONE', *, *, #50820, .T. ) ;
#5059=DIRECTION ( 'NONE',  ( 0.000000000000000000, 0.000000000000000000, -1.000000000000000000 ) ) ;
#5065=ORIENTED_EDGE ( 'NONE', *, *, #45505, .F. ) ;
#5068=LINE ( 'NONE', #63313, #58589 ) ;
#5088=AXIS2_PLACEMENT_3D ( 'NONE', #4494, #54864, #20657 ) ;
#5094=AXIS2_PLACEMENT_3D ( 'NONE', #26607, #67585, #39391 ) ;
#5099=ADVANCED_FACE ( 'NONE', ( #2492 ), #38129, .T. ) ;
#5100=ORIENTED_EDGE ( 'NONE', *, *, #58569, .F. ) ;
#5104=FACE_OUTER_BOUND ( 'NONE', #9949, .T. ) ;
#5107=DIRECTION ( 'NONE',  ( -1.000000000000000000, 0.000000000000000000, -0.000000000000000000 ) ) ;
#5109=ORIENTED_EDGE ( 'NONE', *, *, #59353, .T. ) ;
#5112=ORIENTED_EDGE ( 'NONE', *, *, #49124, .T. ) ;
#5118=CARTESIAN_POINT ( 'NONE',  ( 10.00000000000000000, 0.000000000000000000, 0.000000000000000000 ) ) ;
#5122=ORIENTED_EDGE ( 'NONE', *, *, #31292, .F. ) ;
#5143=AXIS2_PLACEMENT_3D ( 'NONE', #51445, #58854, #7 ) ;
#5149=CIRCLE ( 'NONE', #68782, 31.99999999999998934 ) ;
#5151=ORIENTED_EDGE ( 'NONE', *, *, #48297, .F. ) ;
#5153=ORIENTED_EDGE ( 'NONE', *, *, #59149, .T. ) ;
#5155=AXIS2_PLACEMENT_3D ( 'NONE', #20479, #19357, #42310 ) ;
#5165=CARTESIAN_POINT ( 'NONE',  ( 5.000000000000000000, 74.74816331893430288, 33.71516098798768013 ) ) ;
#5169=CARTESIAN_POINT ( 'NONE',  ( 10.00000000000000178, 12.24744871391589207, -2.500000000000000000 ) ) ;
#5170=ORIENTED_EDGE ( 'NONE', *, *, #10122, .F. ) ;
#5171=LINE ( 'NONE', #34454, #8829 ) ;
#5173=CARTESIAN_POINT ( 'NONE',  ( 0.000000000000000000, -41.76106447765443619, -62.50884508063471401 ) ) ;
#5176=CYLINDRICAL_SURFACE ( 'NONE', #28241, 77.49899999999999523 ) ;
#5181=CARTESIAN_POINT ( 'NONE',  ( 10.00000000000000000, 17.28742895386084655, 75.54627589209950145 ) ) ;
#5189=CARTESIAN_POINT ( 'NONE',  ( 10.00000000000000000, 11.30684508768452545, -76.66974797899825944 ) ) ;
#5194=CARTESIAN_POINT ( 'NONE',  ( 0.000000000000000000, 0.000000000000000000, 0.000000000000000000 ) ) ;
#5199=ORIENTED_EDGE ( 'NONE', *, *, #1774, .T. ) ;
#5205=CARTESIAN_POINT ( 'NONE',  ( 0.000000000000000000, 0.000000000000000000, 0.000000000000000000 ) ) ;
#5206=EDGE_LOOP ( 'NONE', ( #33260, #1437, #57752, #63829 ) ) ;
#5226=CARTESIAN_POINT ( 'NONE',  ( 0.000000000000000000, 0.000000000000000000, 0.000000000000000000 ) ) ;
#5231=CARTESIAN_POINT ( 'NONE',  ( 0.000000000000000000, 0.000000000000000000, 0.000000000000000000 ) ) ;
#5246=CIRCLE ( 'NONE', #72447, 82.00000000000000000 ) ;
#5252=CYLINDRICAL_SURFACE ( 'NONE', #51971, 31.99999999999999289 ) ;
#5253=DIRECTION ( 'NONE',  ( 0.000000000000000000, 0.2334453638558990907, 0.9723699203976781114 ) ) ;
#5256=AXIS2_PLACEMENT_3D ( 'NONE', #22374, #15983, #10725 ) ;
#5269=CARTESIAN_POINT ( 'NONE',  ( 0.000000000000000000, 0.000000000000000000, 0.000000000000000000 ) ) ;
#5272=AXIS2_PLACEMENT_3D ( 'NONE', #12852, #53824, #32641 ) ;
#5277=ORIENTED_EDGE ( 'NONE', *, *, #6145, .T. ) ;
#5278=EDGE_CURVE ( 'NONE', #71840, #7986, #25890, .T. ) ;
#5280=EDGE_CURVE ( 'NONE', #32631, #19363, #55951, .T. ) ;
#5286=ORIENTED_EDGE ( 'NONE', *, *, #66475, .F. ) ;
#5297=LINE ( 'NONE', #68056, #47341 ) ;
#5300=ORIENTED_EDGE ( 'NONE', *, *, #126, .F. ) ;
#5303=ORIENTED_EDGE ( 'NONE', *, *, #28509, .T. ) ;
#5306=ORIENTED_EDGE ( 'NONE', *, *, #30784, .T. ) ;
#5314=FACE_OUTER_BOUND ( 'NONE', #25079, .T. ) ;
#5339=AXIS2_PLACEMENT_3D ( 'NONE', #7437, #47652, #70555 ) ;
#5353=VECTOR ( 'NONE', #32779, 1000.000000000000000 ) ;
#5356=LINE ( 'NONE', #74121, #59792 ) ;
#5358=CARTESIAN_POINT ( 'NONE',  ( 0.000000000000000000, 0.000000000000000000, 0.000000000000000000 ) ) ;
#5370=EDGE_CURVE ( 'NONE', #49109, #15896, #69667, .T. ) ;
#5375=CARTESIAN_POINT ( 'NONE',  ( 10.00000000000000000, -2.956366410621191765, 75.11725578898467859 ) ) ;
#5378=EDGE_LOOP ( 'NONE', ( #48113, #10172, #24183, #42277 ) ) ;
#5381=ORIENTED_EDGE ( 'NONE', *, *, #15027, .T. ) ;
#5395=VERTEX_POINT ( 'NONE', #64779 ) ;
#5399=CIRCLE ( 'NONE', #70187, 82.00000000000000000 ) ;
#5401=LINE ( 'NONE', #23776, #16340 ) ;
#5404=CARTESIAN_POINT ( 'NONE',  ( 10.00000000000000000, -78.73519480814938731, -22.90783923731713756 ) ) ;
#5413=CARTESIAN_POINT ( 'NONE',  ( 10.00000000000000000, -35.91791733033426226, -68.67312586195033930 ) ) ;
#5420=CARTESIAN_POINT ( 'NONE',  ( 10.00000000000000000, 46.54456581323805153, 59.03342792756280488 ) ) ;
#5421=DIRECTION ( 'NONE',  ( -1.000000000000000000, 0.000000000000000000, 0.000000000000000000 ) ) ;
#5428=CARTESIAN_POINT ( 'NONE',  ( 5.000000000000002665, -78.73519480814971416, 22.90783923731600069 ) ) ;
#5432=FACE_OUTER_BOUND ( 'NONE', #20715, .T. ) ;
#5456=EDGE_CURVE ( 'NONE', #16527, #66304, #66259, .T. ) ;
#5465=VERTEX_POINT ( 'NONE', #47840 ) ;
#5470=AXIS2_PLACEMENT_3D ( 'NONE', #69128, #51825, #371 ) ;
#5477=CARTESIAN_POINT ( 'NONE',  ( 10.00000000000000000, -65.64334221924882229, -41.19522573413803457 ) ) ;
#5480=VECTOR ( 'NONE', #50881, 1000.000000000000000 ) ;
#5487=CIRCLE ( 'NONE', #13871, 77.49900000000000944 ) ;
#5495=DIRECTION ( 'NONE',  ( 0.000000000000000000, 0.000000000000000000, 1.000000000000000000 ) ) ;
#5506=VERTEX_POINT ( 'NONE', #43698 ) ;
#5511=VERTEX_POINT ( 'NONE', #60618 ) ;
#5514=DIRECTION ( 'NONE',  ( -1.000000000000000000, 0.000000000000000000, -0.000000000000000000 ) ) ;
#5515=CYLINDRICAL_SURFACE ( 'NONE', #11441, 31.99999999999999289 ) ;
#5529=EDGE_CURVE ( 'NONE', #8511, #24726, #3171, .T. ) ;
#5534=EDGE_CURVE ( 'NONE', #59559, #60502, #42220, .T. ) ;
#5546=VECTOR ( 'NONE', #20690, 1000.000000000000000 ) ;
#5553=DIRECTION ( 'NONE',  ( -1.000000000000000000, 0.000000000000000000, -0.000000000000000000 ) ) ;
#5561=DIRECTION ( 'NONE',  ( 0.000000000000000000, -0.8910065241883722287, 0.4539904997395383668 ) ) ;
#5564=DIRECTION ( 'NONE',  ( 1.000000000000000000, 0.000000000000000000, 0.000000000000000000 ) ) ;
#5572=VERTEX_POINT ( 'NONE', #48219 ) ;
#5580=DIRECTION ( 'NONE',  ( 0.000000000000000000, 0.000000000000000000, 1.000000000000000000 ) ) ;
#5591=FACE_OUTER_BOUND ( 'NONE', #64787, .T. ) ;
#5606=ORIENTED_EDGE ( 'NONE', *, *, #73133, .T. ) ;
#5613=CARTESIAN_POINT ( 'NONE',  ( 10.00000000000000000, 34.44570377933598593, 69.42325613327452061 ) ) ;
#5618=CARTESIAN_POINT ( 'NONE',  ( 0.000000000000000000, 0.000000000000000000, 0.000000000000000000 ) ) ;
#5621=EDGE_CURVE ( 'NONE', #64515, #2735, #47583, .T. ) ;
#5625=AXIS2_PLACEMENT_3D ( 'NONE', #18427, #63572, #63942 ) ;
#5628=CARTESIAN_POINT ( 'NONE',  ( 10.00000000000000000, 59.46389618802034960, -49.70050353004825894 ) ) ;
#5647=VERTEX_POINT ( 'NONE', #16218 ) ;
#5648=ORIENTED_EDGE ( 'NONE', *, *, #69208, .F. ) ;
#5649=AXIS2_PLACEMENT_3D ( 'NONE', #5375, #57609, #33917 ) ;
#5652=ORIENTED_EDGE ( 'NONE', *, *, #64410, .T. ) ;
#5658=DIRECTION ( 'NONE',  ( 1.000000000000000000, 0.000000000000000000, -0.000000000000000000 ) ) ;
#5666=DIRECTION ( 'NONE',  ( 0.000000000000000000, 0.000000000000000000, -1.000000000000000000 ) ) ;
#5684=CARTESIAN_POINT ( 'NONE',  ( 10.00000000000000000, -55.16347631943084195, 60.67117009219116852 ) ) ;
#5702=AXIS2_PLACEMENT_3D ( 'NONE', #22111, #39409, #63101 ) ;
#5723=CARTESIAN_POINT ( 'NONE',  ( 10.00000000000000000, -76.66974797899830207, -11.30684508768422170 ) ) ;
#5734=EDGE_CURVE ( 'NONE', #66703, #56916, #40268, .T. ) ;
#5738=ORIENTED_EDGE ( 'NONE', *, *, #35004, .F. ) ;
#5741=CARTESIAN_POINT ( 'NONE',  ( 0.000000000000000000, 0.000000000000000000, 0.000000000000000000 ) ) ;
#5746=LINE ( 'NONE', #51954, #4517 ) ;
#5747=VERTEX_POINT ( 'NONE', #23355 ) ;
#5767=CARTESIAN_POINT ( 'NONE',  ( 10.00000000000000000, 80.28980883073757013, 16.65972982744963460 ) ) ;
#5774=ORIENTED_EDGE ( 'NONE', *, *, #38944, .F. ) ;
#5786=CARTESIAN_POINT ( 'NONE',  ( 10.00000000000000000, 0.000000000000000000, 0.000000000000000000 ) ) ;
#5788=ORIENTED_EDGE ( 'NONE', *, *, #65963, .F. ) ;
#5794=CARTESIAN_POINT ( 'NONE',  ( 10.00000000000000000, 0.000000000000000000, 0.000000000000000000 ) ) ;
#5799=DIRECTION ( 'NONE',  ( -1.000000000000000000, -0.000000000000000000, 0.000000000000000000 ) ) ;
#5815=DIRECTION ( 'NONE',  ( 0.000000000000000000, 0.9723699203976756689, 0.2334453638559095268 ) ) ;
#5820=EDGE_CURVE ( 'NONE', #17228, #10249, #30755, .T. ) ;
#5821=ADVANCED_FACE ( 'NONE', ( #68852 ), #40639, .T. ) ;
#5829=ORIENTED_EDGE ( 'NONE', *, *, #9776, .T. ) ;
#5833=VECTOR ( 'NONE', #37229, 1000.000000000000000 ) ;
#5834=ORIENTED_EDGE ( 'NONE', *, *, #70421, .T. ) ;
#5836=CIRCLE ( 'NONE', #57456, 77.49900000000002365 ) ;
#5844=ORIENTED_EDGE ( 'NONE', *, *, #37965, .T. ) ;
#5845=VERTEX_POINT ( 'NONE', #30088 ) ;
#5847=DIRECTION ( 'NONE',  ( -1.000000000000000000, 0.000000000000000000, -0.000000000000000000 ) ) ;
#5848=CIRCLE ( 'NONE', #19021, 31.99999999999998934 ) ;
#5855=CIRCLE ( 'NONE', #67066, 82.00000000000000000 ) ;
#5856=DIRECTION ( 'NONE',  ( -1.000000000000000000, 0.000000000000000000, 0.000000000000000000 ) ) ;
#5862=ORIENTED_EDGE ( 'NONE', *, *, #65859, .T. ) ;
#5866=VERTEX_POINT ( 'NONE', #828 ) ;
#5869=PRODUCT_DEFINITION ( 'UNKNOWN', '', #69968, #2599 ) ;
#5880=ORIENTED_EDGE ( 'NONE', *, *, #301, .T. ) ;
#5888=CIRCLE ( 'NONE', #59917, 31.99999999999999289 ) ;
#5890=VECTOR ( 'NONE', #47492, 1000.000000000000000 ) ;
#5891=CARTESIAN_POINT ( 'NONE',  ( 10.00000000000000000, -44.88180994100421373, 63.18004540533011948 ) ) ;
#5897=CARTESIAN_POINT ( 'NONE',  ( 0.000000000000000000, 51.03279382321088065, 55.19960302592086521 ) ) ;
#5903=DIRECTION ( 'NONE',  ( 0.000000000000000000, -0.9510565162951499785, -0.3090169943749582204 ) ) ;
#5911=DIRECTION ( 'NONE',  ( -1.000000000000000000, 0.000000000000000000, 0.000000000000000000 ) ) ;
#5915=CARTESIAN_POINT ( 'NONE',  ( 10.00000000000000000, 0.000000000000000000, 0.000000000000000000 ) ) ;
#5918=DIRECTION ( 'NONE',  ( -1.000000000000000000, 0.000000000000000000, 0.000000000000000000 ) ) ;
#5926=VECTOR ( 'NONE', #28580, 1000.000000000000000 ) ;
#5928=CARTESIAN_POINT ( 'NONE',  ( 10.00000000000000000, 0.000000000000000000, 0.000000000000000000 ) ) ;
#5933=DIRECTION ( 'NONE',  ( -1.000000000000000000, -0.000000000000000000, 0.000000000000000000 ) ) ;
#5936=EDGE_CURVE ( 'NONE', #26543, #32443, #52400, .T. ) ;
#5941=ORIENTED_EDGE ( 'NONE', *, *, #61992, .T. ) ;
#5942=AXIS2_PLACEMENT_3D ( 'NONE', #15017, #55618, #27790 ) ;
#5947=EDGE_CURVE ( 'NONE', #68980, #27978, #25200, .T. ) ;
#5948=CARTESIAN_POINT ( 'NONE',  ( 10.00000000000000000, 0.000000000000000000, 0.000000000000000000 ) ) ;
#5953=CARTESIAN_POINT ( 'NONE',  ( 10.00000000000000000, 2.956366410620650420, 75.11725578898469280 ) ) ;
#5969=CIRCLE ( 'NONE', #44364, 31.99999999999999645 ) ;
#5973=VERTEX_POINT ( 'NONE', #70663 ) ;
#5983=DIRECTION ( 'NONE',  ( 0.000000000000000000, 0.000000000000000000, 1.000000000000000000 ) ) ;
#5984=EDGE_CURVE ( 'NONE', #11648, #29034, #52453, .T. ) ;
#5987=ORIENTED_EDGE ( 'NONE', *, *, #8309, .F. ) ;
#5988=FACE_OUTER_BOUND ( 'NONE', #39421, .T. ) ;
#5994=DIRECTION ( 'NONE',  ( -1.000000000000000000, 0.000000000000000000, -0.000000000000000000 ) ) ;
#6003=CARTESIAN_POINT ( 'NONE',  ( 10.00000000000000000, 0.000000000000000000, 0.000000000000000000 ) ) ;
#6013=CYLINDRICAL_SURFACE ( 'NONE', #28351, 77.49899999999999523 ) ;
#6026=ORIENTED_EDGE ( 'NONE', *, *, #50909, .F. ) ;
#6028=EDGE_CURVE ( 'NONE', #1496, #49408, #36837, .T. ) ;
#6033=FACE_OUTER_BOUND ( 'NONE', #25542, .T. ) ;
#6035=DIRECTION ( 'NONE',  ( 0.000000000000000000, 0.000000000000000000, -1.000000000000000000 ) ) ;
#6036=EDGE_CURVE ( 'NONE', #39875, #73588, #14023, .T. ) ;
#6040=ORIENTED_EDGE ( 'NONE', *, *, #33252, .T. ) ;
#6044=CIRCLE ( 'NONE', #51645, 31.99999999999999289 ) ;
#6056=CARTESIAN_POINT ( 'NONE',  ( 0.000000000000000000, 36.72794159290334903, -65.59268652807170952 ) ) ;
#6059=VERTEX_POINT ( 'NONE', #33412 ) ;
#6062=FACE_OUTER_BOUND ( 'NONE', #16947, .T. ) ;
#6070=CIRCLE ( 'NONE', #32428, 77.49899999999999523 ) ;
#6072=FACE_OUTER_BOUND ( 'NONE', #13134, .T. ) ;
#6076=AXIS2_PLACEMENT_3D ( 'NONE', #52485, #39188, #50824 ) ;
#6078=DIRECTION ( 'NONE',  ( -1.000000000000000000, 0.000000000000000000, 0.000000000000000000 ) ) ;
#6083=EDGE_CURVE ( 'NONE', #70179, #69749, #66839, .T. ) ;
#6089=DIRECTION ( 'NONE',  ( -1.000000000000000000, -0.000000000000000000, 0.000000000000000000 ) ) ;
#6093=ORIENTED_EDGE ( 'NONE', *, *, #48448, .F. ) ;
#6100=AXIS2_PLACEMENT_3D ( 'NONE', #62365, #33015, #28488 ) ;
#6109=EDGE_CURVE ( 'NONE', #51433, #29098, #23645, .T. ) ;
#6130=ADVANCED_FACE ( 'NONE', ( #45095 ), #4137, .T. ) ;
#6145=EDGE_CURVE ( 'NONE', #73479, #34939, #53643, .T. ) ;
#6155=FACE_OUTER_BOUND ( 'NONE', #2168, .T. ) ;
#6159=AXIS2_PLACEMENT_3D ( 'NONE', #19725, #26483, #49775 ) ;
#6164=ORIENTED_EDGE ( 'NONE', *, *, #38786, .F. ) ;
#6178=AXIS2_PLACEMENT_3D ( 'NONE', #33588, #39989, #39246 ) ;
#6189=CARTESIAN_POINT ( 'NONE',  ( 10.00000000000000000, -26.02418014898359289, 70.52718814184250107 ) ) ;
#6190=CARTESIAN_POINT ( 'NONE',  ( 10.00000000000000000, 14.66109333815460225, 73.73191006444577056 ) ) ;
#6195=ORIENTED_EDGE ( 'NONE', *, *, #30449, .T. ) ;
#6196=CARTESIAN_POINT ( 'NONE',  ( 10.00000000000000000, 44.88180994100468268, -63.18004540532978552 ) ) ;
#6199=EDGE_CURVE ( 'NONE', #73126, #5572, #48859, .T. ) ;
#6200=DIRECTION ( 'NONE',  ( -1.000000000000000000, 0.000000000000000000, 0.000000000000000000 ) ) ;
#6202=EDGE_CURVE ( 'NONE', #19951, #15157, #54815, .T. ) ;
#6207=ORIENTED_EDGE ( 'NONE', *, *, #27418, .T. ) ;
#6211=ORIENTED_EDGE ( 'NONE', *, *, #34277, .F. ) ;
#6212=ORIENTED_EDGE ( 'NONE', *, *, #16970, .T. ) ;
#6216=ORIENTED_EDGE ( 'NONE', *, *, #34103, .T. ) ;
#6238=ORIENTED_EDGE ( 'NONE', *, *, #37519, .T. ) ;
#6265=DIRECTION ( 'NONE',  ( 0.000000000000000000, 0.000000000000000000, 1.000000000000000000 ) ) ;
#6270=AXIS2_PLACEMENT_3D ( 'NONE', #15564, #55412, #38864 ) ;
#6282=CYLINDRICAL_SURFACE ( 'NONE', #9649, 31.99999999999998579 ) ;
#6289=ORIENTED_EDGE ( 'NONE', *, *, #15644, .F. ) ;
#6300=ORIENTED_EDGE ( 'NONE', *, *, #51850, .F. ) ;
#6301=ORIENTED_EDGE ( 'NONE', *, *, #63241, .T. ) ;
#6304=CARTESIAN_POINT ( 'NONE',  ( 10.00000000000000000, 77.32052557432849937, -5.256550761632002633 ) ) ;
#6312=EDGE_CURVE ( 'NONE', #4680, #39290, #17634, .T. ) ;
#6326=DIRECTION ( 'NONE',  ( 0.000000000000000000, 0.000000000000000000, 1.000000000000000000 ) ) ;
#6327=DIRECTION ( 'NONE',  ( 1.000000000000000000, -0.000000000000000000, -0.000000000000000000 ) ) ;
#6337=DIRECTION ( 'NONE',  ( 0.000000000000000000, -0.5224985647159559043, 0.8526401643540878483 ) ) ;
#6338=ORIENTED_EDGE ( 'NONE', *, *, #34386, .T. ) ;
#6339=LINE ( 'NONE', #16492, #25145 ) ;
#6348=DIRECTION ( 'NONE',  ( 1.000000000000000000, -0.000000000000000000, -0.000000000000000000 ) ) ;
#6349=DIRECTION ( 'NONE',  ( -1.000000000000000000, -0.000000000000000000, -0.000000000000000000 ) ) ;
#6357=CARTESIAN_POINT ( 'NONE',  ( 0.000000000000000000, 2.946379043146343246, 75.11764819372150725 ) ) ;
#6362=VECTOR ( 'NONE', #18224, 1000.000000000000000 ) ;
#6364=ADVANCED_FACE ( 'NONE', ( #52196 ), #57482, .T. ) ;
#6366=EDGE_CURVE ( 'NONE', #31543, #26168, #56056, .T. ) ;
#6368=CIRCLE ( 'NONE', #41194, 31.99999999999999645 ) ;
#6370=DIRECTION ( 'NONE',  ( 1.000000000000000000, -0.000000000000000000, -0.000000000000000000 ) ) ;
#6373=DIRECTION ( 'NONE',  ( 0.000000000000000000, 0.000000000000000000, 1.000000000000000000 ) ) ;
#6379=ORIENTED_EDGE ( 'NONE', *, *, #18906, .T. ) ;
#6393=DIRECTION ( 'NONE',  ( 0.000000000000000000, 0.000000000000000000, 1.000000000000000000 ) ) ;
#6397=EDGE_CURVE ( 'NONE', #1496, #27817, #3280, .T. ) ;
#6408=SURFACE_STYLE_FILL_AREA ( #12028 ) ;
#6429=DIRECTION ( 'NONE',  ( 0.000000000000000000, 0.000000000000000000, 1.000000000000000000 ) ) ;
#6430=DIRECTION ( 'NONE',  ( -1.000000000000000000, 0.000000000000000000, 0.000000000000000000 ) ) ;
#6436=CARTESIAN_POINT ( 'NONE',  ( 0.000000000000000000, 41.19522573413826194, -65.64334221924865176 ) ) ;
#6445=CYLINDRICAL_SURFACE ( 'NONE', #37023, 82.00000000000000000 ) ;
#6447=DIRECTION ( 'NONE',  ( 0.000000000000000000, 0.000000000000000000, 1.000000000000000000 ) ) ;
#6452=LINE ( 'NONE', #34265, #16448 ) ;
#6454=ORIENTED_EDGE ( 'NONE', *, *, #73834, .F. ) ;
#6456=CYLINDRICAL_SURFACE ( 'NONE', #39475, 82.00000000000000000 ) ;
#6466=EDGE_LOOP ( 'NONE', ( #41428, #10904, #56874, #53023 ) ) ;
#6467=CIRCLE ( 'NONE', #56925, 82.00000000000000000 ) ;
#6478=AXIS2_PLACEMENT_3D ( 'NONE', #19915, #31204, #18445 ) ;
#6487=CARTESIAN_POINT ( 'NONE',  ( 10.00000000000000000, -40.65526001592565564, -71.21200624218839437 ) ) ;
#6490=ADVANCED_FACE ( 'NONE', ( #71694 ), #19460, .T. ) ;
#6500=LINE ( 'NONE', #18140, #3659 ) ;
#6508=DIRECTION ( 'NONE',  ( -1.000000000000000000, -0.000000000000000000, 0.000000000000000000 ) ) ;
#6513=LINE ( 'NONE', #18515, #17475 ) ;
#6527=AXIS2_PLACEMENT_3D ( 'NONE', #35594, #12663, #42362 ) ;
#6528=DIRECTION ( 'NONE',  ( 0.000000000000000000, 0.000000000000000000, 1.000000000000000000 ) ) ;
#6529=AXIS2_PLACEMENT_3D ( 'NONE', #71524, #37711, #65917 ) ;
#6539=EDGE_CURVE ( 'NONE', #19072, #60775, #60448, .T. ) ;
#6543=AXIS2_PLACEMENT_3D ( 'NONE', #57637, #18498, #35781 ) ;
#6549=DIRECTION ( 'NONE',  ( -1.000000000000000000, 0.000000000000000000, -0.000000000000000000 ) ) ;
#6553=VERTEX_POINT ( 'NONE', #72796 ) ;
#6556=EDGE_CURVE ( 'NONE', #38932, #25891, #54789, .T. ) ;
#6558=CYLINDRICAL_SURFACE ( 'NONE', #73570, 82.00000000000000000 ) ;
#6561=DIRECTION ( 'NONE',  ( 0.000000000000000000, -0.1564344650402381132, 0.9876883405951365491 ) ) ;
#6563=AXIS2_PLACEMENT_3D ( 'NONE', #18035, #52989, #30771 ) ;
#6565=ORIENTED_EDGE ( 'NONE', *, *, #52349, .T. ) ;
#6577=ORIENTED_EDGE ( 'NONE', *, *, #5734, .T. ) ;
#6609=LINE ( 'NONE', #1009, #36124 ) ;
#6613=CARTESIAN_POINT ( 'NONE',  ( 0.000000000000000000, 0.000000000000000000, 0.000000000000000000 ) ) ;
#6622=ADVANCED_FACE ( 'NONE', ( #49515 ), #61181, .T. ) ;
#6640=CARTESIAN_POINT ( 'NONE',  ( 10.00000000000000000, 46.54456581323888997, -59.03342792756214408 ) ) ;
#6644=CIRCLE ( 'NONE', #676, 31.99999999999999289 ) ;
#6645=ORIENTED_EDGE ( 'NONE', *, *, #24062, .T. ) ;
#6648=DIRECTION ( 'NONE',  ( 0.000000000000000000, -0.9510565162951565288, 0.3090169943749382919 ) ) ;
#6651=AXIS2_PLACEMENT_3D ( 'NONE', #60094, #49156, #55545 ) ;
#6653=DIRECTION ( 'NONE',  ( 0.000000000000000000, 0.000000000000000000, 1.000000000000000000 ) ) ;
#6658=ORIENTED_EDGE ( 'NONE', *, *, #74103, .T. ) ;
#6664=CYLINDRICAL_SURFACE ( 'NONE', #49752, 77.49899999999999523 ) ;
#6671=DIRECTION ( 'NONE',  ( 0.000000000000000000, 0.3826834323650841752, 0.9238795325112891810 ) ) ;
#6679=LINE ( 'NONE', #17957, #1413 ) ;
#6697=ORIENTED_EDGE ( 'NONE', *, *, #33338, .T. ) ;
#6698=DIRECTION ( 'NONE',  ( -1.000000000000000000, 0.000000000000000000, 0.000000000000000000 ) ) ;
#6701=ORIENTED_EDGE ( 'NONE', *, *, #39986, .T. ) ;
#6704=AXIS2_PLACEMENT_3D ( 'NONE', #35844, #7296, #30211 ) ;
#6707=CYLINDRICAL_SURFACE ( 'NONE', #72415, 82.00000000000000000 ) ;
#6714=DIRECTION ( 'NONE',  ( -1.000000000000000000, -0.000000000000000000, -0.000000000000000000 ) ) ;
#6717=CARTESIAN_POINT ( 'NONE',  ( -10.00000000000000000, 0.000000000000000000, 0.000000000000000000 ) ) ;
#6727=CARTESIAN_POINT ( 'NONE',  ( -10.00000000000000000, 0.000000000000000000, 0.000000000000000000 ) ) ;
#6728=FACE_OUTER_BOUND ( 'NONE', #64089, .T. ) ;
#6736=EDGE_LOOP ( 'NONE', ( #25794, #68132, #53568, #74156 ) ) ;
#6738=ORIENTED_EDGE ( 'NONE', *, *, #17747, .F. ) ;
#6749=FACE_OUTER_BOUND ( 'NONE', #3462, .T. ) ;
#6756=DIRECTION ( 'NONE',  ( -1.000000000000000000, 0.000000000000000000, 0.000000000000000000 ) ) ;
#6776=ORIENTED_EDGE ( 'NONE', *, *, #2584, .F. ) ;
#6781=CARTESIAN_POINT ( 'NONE',  ( 10.00000000000000000, -72.35160999960831418, 20.41045688087797672 ) ) ;
#6795=FACE_OUTER_BOUND ( 'NONE', #46601, .T. ) ;
#6803=CARTESIAN_POINT ( 'NONE',  ( 10.00000000000000000, 50.95692526931328104, 58.39081064771769292 ) ) ;
#6804=FACE_OUTER_BOUND ( 'NONE', #71179, .T. ) ;
#6836=ORIENTED_EDGE ( 'NONE', *, *, #43544, .T. ) ;
#6837=DIRECTION ( 'NONE',  ( -1.000000000000000000, -0.000000000000000000, 0.000000000000000000 ) ) ;
#6839=ADVANCED_FACE ( 'NONE', ( #35191 ), #33708, .T. ) ;
#6849=ORIENTED_EDGE ( 'NONE', *, *, #61978, .F. ) ;
#6855=CARTESIAN_POINT ( 'NONE',  ( 10.00000000000000000, 17.28742895386191236, -75.54627589209927407 ) ) ;
#6867=DIRECTION ( 'NONE',  ( -1.000000000000000000, -0.000000000000000000, -0.000000000000000000 ) ) ;
#6868=CARTESIAN_POINT ( 'NONE',  ( -10.00000000000000000, 0.000000000000000000, 0.000000000000000000 ) ) ;
#6873=DIRECTION ( 'NONE',  ( 1.000000000000000000, 0.000000000000000000, 0.000000000000000000 ) ) ;
#6886=CARTESIAN_POINT ( 'NONE',  ( 0.000000000000000000, 46.11716303203188261, 67.80270845531904911 ) ) ;
#6887=EDGE_CURVE ( 'NONE', #14607, #38641, #46052, .T. ) ;
#6894=CIRCLE ( 'NONE', #20086, 31.99999999999999645 ) ;
#6923=ORIENTED_EDGE ( 'NONE', *, *, #25705, .T. ) ;
#6927=AXIS2_PLACEMENT_3D ( 'NONE', #67549, #34437, #22813 ) ;
#6935=AXIS2_PLACEMENT_3D ( 'NONE', #4127, #72512, #71766 ) ;
#6938=CIRCLE ( 'NONE', #50129, 77.49899999999999523 ) ;
#6956=EDGE_CURVE ( 'NONE', #1870, #975, #52046, .T. ) ;
#6960=ORIENTED_EDGE ( 'NONE', *, *, #51937, .T. ) ;
#6962=EDGE_LOOP ( 'NONE', ( #20044, #40146, #30752, #10339 ) ) ;
#6972=EDGE_CURVE ( 'NONE', #16649, #25971, #31389, .T. ) ;
#6979=DIRECTION ( 'NONE',  ( 0.000000000000000000, 0.8526401643540935105, -0.5224985647159468005 ) ) ;
#6984=ADVANCED_FACE ( 'NONE', ( #36293 ), #64508, .T. ) ;
#6999=ORIENTED_EDGE ( 'NONE', *, *, #44465, .F. ) ;
#7000=CIRCLE ( 'NONE', #21419, 82.00000000000000000 ) ;
#7001=CYLINDRICAL_SURFACE ( 'NONE', #27515, 31.99999999999999289 ) ;
#7017=ORIENTED_EDGE ( 'NONE', *, *, #55835, .T. ) ;
#7028=ADVANCED_FACE ( 'NONE', ( #14847 ), #61083, .T. ) ;
#7032=VERTEX_POINT ( 'NONE', #32123 ) ;
#7037=EDGE_LOOP ( 'NONE', ( #6207, #35670, #34432, #6379 ) ) ;
#7040=AXIS2_PLACEMENT_3D ( 'NONE', #10969, #4977, #71982 ) ;
#7046=CARTESIAN_POINT ( 'NONE',  ( 10.00000000000000000, 55.19960302592066625, 51.03279382321107249 ) ) ;
#7054=EDGE_CURVE ( 'NONE', #26436, #35888, #55643, .T. ) ;
#7089=ORIENTED_EDGE ( 'NONE', *, *, #55487, .T. ) ;
#7094=CIRCLE ( 'NONE', #21512, 82.00000000000000000 ) ;
#7115=CARTESIAN_POINT ( 'NONE',  ( 10.00000000000000000, 41.76937507738875155, -62.50329211542393892 ) ) ;
#7121=VECTOR ( 'NONE', #5658, 1000.000000000000000 ) ;
#7122=VERTEX_POINT ( 'NONE', #30876 ) ;
#7130=CARTESIAN_POINT ( 'NONE',  ( 0.000000000000000000, 0.000000000000000000, 0.000000000000000000 ) ) ;
#7133=ORIENTED_EDGE ( 'NONE', *, *, #68282, .T. ) ;
#7141=LINE ( 'NONE', #70266, #58244 ) ;
#7145=CARTESIAN_POINT ( 'NONE',  ( 10.00000000000000000, -8.966570791701267140, 81.50828551894223040 ) ) ;
#7150=CARTESIAN_POINT ( 'NONE',  ( 0.000000000000000000, 56.15606465355042332, -59.75363087400017292 ) ) ;
#7151=DIRECTION ( 'NONE',  ( -1.000000000000000000, -0.000000000000000000, -0.000000000000000000 ) ) ;
#7152=VERTEX_POINT ( 'NONE', #1629 ) ;
#7160=CARTESIAN_POINT ( 'NONE',  ( 10.00000000000000000, -54.21277698773715059, 55.38113227695762930 ) ) ;
#7162=AXIS2_PLACEMENT_3D ( 'NONE', #7610, #47463, #52733 ) ;
#7165=EDGE_CURVE ( 'NONE', #52760, #33517, #70068, .T. ) ;
#7167=DIRECTION ( 'NONE',  ( -1.000000000000000000, -0.000000000000000000, -0.000000000000000000 ) ) ;
#7171=DIRECTION ( 'NONE',  ( -1.000000000000000000, 0.000000000000000000, 0.000000000000000000 ) ) ;
#7177=CARTESIAN_POINT ( 'NONE',  ( 10.00000000000000000, 30.41916302227113178, 71.27951684758036777 ) ) ;
#7178=CIRCLE ( 'NONE', #68421, 82.00000000000000000 ) ;
#7188=DIRECTION ( 'NONE',  ( -1.000000000000000000, 0.000000000000000000, 0.000000000000000000 ) ) ;
#7194=CARTESIAN_POINT ( 'NONE',  ( 0.000000000000000000, -29.01471420065507090, -76.69515212746047439 ) ) ;
#7205=DIRECTION ( 'NONE',  ( 0.000000000000000000, 0.000000000000000000, 1.000000000000000000 ) ) ;
#7210=ORIENTED_EDGE ( 'NONE', *, *, #19751, .F. ) ;
#7213=VERTEX_POINT ( 'NONE', #19602 ) ;
#7248=FACE_OUTER_BOUND ( 'NONE', #34337, .T. ) ;
#7250=DIRECTION ( 'NONE',  ( -1.000000000000000000, 0.000000000000000000, 0.000000000000000000 ) ) ;
#7251=CARTESIAN_POINT ( 'NONE',  ( 10.00000000000000000, 35.91791733033475253, 68.67312586195009771 ) ) ;
#7259=EDGE_CURVE ( 'NONE', #28369, #26699, #58065, .T. ) ;
#7264=CARTESIAN_POINT ( 'NONE',  ( 0.000000000000000000, -65.64334221924939072, 41.19522573413710376 ) ) ;
#7271=VECTOR ( 'NONE', #62294, 1000.000000000000000 ) ;
#7292=CARTESIAN_POINT ( 'NONE',  ( 0.000000000000000000, -70.53064760720297954, -26.01480285779911839 ) ) ;
#7295=EDGE_CURVE ( 'NONE', #64863, #59272, #35263, .T. ) ;
#7296=DIRECTION ( 'NONE',  ( -1.000000000000000000, 0.000000000000000000, -0.000000000000000000 ) ) ;
#7299=CARTESIAN_POINT ( 'NONE',  ( 10.00000000000000000, -17.28742895386031719, -75.54627589209962935 ) ) ;
#7303=ORIENTED_EDGE ( 'NONE', *, *, #6397, .T. ) ;
#7305=VERTEX_POINT ( 'NONE', #17603 ) ;
#7315=VECTOR ( 'NONE', #52856, 1000.000000000000000 ) ;
#7345=CYLINDRICAL_SURFACE ( 'NONE', #67324, 77.49899999999999523 ) ;
#7362=DIRECTION ( 'NONE',  ( 0.000000000000000000, 0.000000000000000000, -1.000000000000000000 ) ) ;
#7366=CARTESIAN_POINT ( 'NONE',  ( 10.00000000000000000, 26.02418014898407961, -70.52718814184231633 ) ) ;
#7398=LINE ( 'NONE', #20521, #53114 ) ;
#7408=DIRECTION ( 'NONE',  ( -1.000000000000000000, 0.000000000000000000, -0.000000000000000000 ) ) ;
#7415=ORIENTED_EDGE ( 'NONE', *, *, #4032, .F. ) ;
#7419=VERTEX_POINT ( 'NONE', #29984 ) ;
#7429=VERTEX_POINT ( 'NONE', #48026 ) ;
#7434=CARTESIAN_POINT ( 'NONE',  ( 10.00000000000000000, 65.59268652807263322, -36.72794159290169347 ) ) ;
#7437=CARTESIAN_POINT ( 'NONE',  ( 0.000000000000000000, -74.65374052328654386, 8.840884882374837161 ) ) ;
#7452=DIRECTION ( 'NONE',  ( -1.000000000000000000, -0.000000000000000000, -0.000000000000000000 ) ) ;
#7456=EDGE_CURVE ( 'NONE', #1351, #26686, #58945, .T. ) ;
#7460=EDGE_CURVE ( 'NONE', #61671, #26809, #62981, .T. ) ;
#7467=DIRECTION ( 'NONE',  ( -1.000000000000000000, 0.000000000000000000, 0.000000000000000000 ) ) ;
#7477=ORIENTED_EDGE ( 'NONE', *, *, #67667, .T. ) ;
#7498=ORIENTED_EDGE ( 'NONE', *, *, #53702, .F. ) ;
#7510=ORIENTED_EDGE ( 'NONE', *, *, #72462, .F. ) ;
#7521=CARTESIAN_POINT ( 'NONE',  ( 0.000000000000000000, -73.95703589263990807, 23.16143007188399139 ) ) ;
#7533=CARTESIAN_POINT ( 'NONE',  ( 0.000000000000000000, 35.91791733033570466, -68.67312586194960033 ) ) ;
#7541=DIRECTION ( 'NONE',  ( 0.000000000000000000, 0.000000000000000000, 1.000000000000000000 ) ) ;
#7552=CARTESIAN_POINT ( 'NONE',  ( 10.00000000000000000, 0.000000000000000000, 0.000000000000000000 ) ) ;
#7570=ORIENTED_EDGE ( 'NONE', *, *, #722, .T. ) ;
#7573=DIRECTION ( 'NONE',  ( -1.000000000000000000, -0.000000000000000000, -0.000000000000000000 ) ) ;
#7578=ORIENTED_EDGE ( 'NONE', *, *, #10674, .T. ) ;
#7587=CIRCLE ( 'NONE', #55620, 31.99999999999999289 ) ;
#7589=AXIS2_PLACEMENT_3D ( 'NONE', #13636, #8380, #25666 ) ;
#7593=ORIENTED_EDGE ( 'NONE', *, *, #11299, .T. ) ;
#7597=AXIS2_PLACEMENT_3D ( 'NONE', #1484, #47306, #54056 ) ;
#7600=DIRECTION ( 'NONE',  ( 0.000000000000000000, 0.000000000000000000, -1.000000000000000000 ) ) ;
#7610=CARTESIAN_POINT ( 'NONE',  ( 0.000000000000000000, 0.000000000000000000, 0.000000000000000000 ) ) ;
#7611=DIRECTION ( 'NONE',  ( 0.000000000000000000, 0.5224985647159500202, -0.8526401643540915121 ) ) ;
#7625=AXIS2_PLACEMENT_3D ( 'NONE', #17529, #56663, #57024 ) ;
#7638=ADVANCED_FACE ( 'NONE', ( #48388 ), #49128, .T. ) ;
#7639=CARTESIAN_POINT ( 'NONE',  ( 5.000000000000002665, 74.18225833017888249, 34.94270380257665209 ) ) ;
#7640=AXIS2_PLACEMENT_3D ( 'NONE', #16175, #68439, #6035 ) ;
#7646=ORIENTED_EDGE ( 'NONE', *, *, #35330, .F. ) ;
#7655=VERTEX_POINT ( 'NONE', #43521 ) ;
#7657=FACE_OUTER_BOUND ( 'NONE', #18701, .T. ) ;
#7660=FACE_OUTER_BOUND ( 'NONE', #66386, .T. ) ;
#7662=DIRECTION ( 'NONE',  ( 0.000000000000000000, 0.000000000000000000, 1.000000000000000000 ) ) ;
#7673=CARTESIAN_POINT ( 'NONE',  ( 10.00000000000000000, -5.256550761632340141, -77.32052557432847095 ) ) ;
#7674=CARTESIAN_POINT ( 'NONE',  ( 10.00000000000000000, 55.38113227695782115, 54.21277698773695164 ) ) ;
#7678=EDGE_LOOP ( 'NONE', ( #62460, #33822, #31770, #62441 ) ) ;
#7681=VECTOR ( 'NONE', #42912, 1000.000000000000000 ) ;
#7684=CARTESIAN_POINT ( 'NONE',  ( 0.000000000000000000, 0.000000000000000000, 0.000000000000000000 ) ) ;
#7686=DIRECTION ( 'NONE',  ( -1.000000000000000000, 0.000000000000000000, 0.000000000000000000 ) ) ;
#7700=CARTESIAN_POINT ( 'NONE',  ( 10.00000000000000000, -73.95703589263990807, 23.16143007188399139 ) ) ;
#7704=DIRECTION ( 'NONE',  ( 0.000000000000000000, -0.5224985647159379187, -0.8526401643540989506 ) ) ;
#7705=CIRCLE ( 'NONE', #54501, 31.99999999999998934 ) ;
#7708=VERTEX_POINT ( 'NONE', #39346 ) ;
#7715=CARTESIAN_POINT ( 'NONE',  ( 10.00000000000000000, -59.03961581697432592, 46.53671651293927880 ) ) ;
#7743=ORIENTED_EDGE ( 'NONE', *, *, #6556, .F. ) ;
#7745=DIRECTION ( 'NONE',  ( -1.000000000000000000, 0.000000000000000000, 0.000000000000000000 ) ) ;
#7749=ORIENTED_EDGE ( 'NONE', *, *, #72728, .T. ) ;
#7757=CARTESIAN_POINT ( 'NONE',  ( 0.000000000000000000, 0.000000000000000000, 0.000000000000000000 ) ) ;
#7762=DIRECTION ( 'NONE',  ( 0.000000000000000000, 0.4539904997395476927, -0.8910065241883674547 ) ) ;
#7764=DIRECTION ( 'NONE',  ( -1.000000000000000000, -0.000000000000000000, 0.000000000000000000 ) ) ;
#7766=CIRCLE ( 'NONE', #1797, 82.00000000000000000 ) ;
#7770=ORIENTED_EDGE ( 'NONE', *, *, #49901, .F. ) ;
#7776=ORIENTED_EDGE ( 'NONE', *, *, #9834, .F. ) ;
#7779=ORIENTED_EDGE ( 'NONE', *, *, #16014, .T. ) ;
#7787=CARTESIAN_POINT ( 'NONE',  ( 0.000000000000000000, 0.000000000000000000, -2.500000000000000000 ) ) ;
#7791=ORIENTED_EDGE ( 'NONE', *, *, #61728, .T. ) ;
#7807=CYLINDRICAL_SURFACE ( 'NONE', #35496, 82.00000000000000000 ) ;
#7823=ORIENTED_EDGE ( 'NONE', *, *, #3907, .T. ) ;
#7843=VECTOR ( 'NONE', #30301, 1000.000000000000000 ) ;
#7854=AXIS2_PLACEMENT_3D ( 'NONE', #6613, #11866, #641 ) ;
#7878=DIRECTION ( 'NONE',  ( 0.000000000000000000, 0.1564344650402244019, 0.9876883405951387696 ) ) ;
#7888=CYLINDRICAL_SURFACE ( 'NONE', #8658, 31.99999999999999289 ) ;
#7895=CARTESIAN_POINT ( 'NONE',  ( 0.000000000000000000, 55.19960302592066625, 51.03279382321107249 ) ) ;
#7903=AXIS2_PLACEMENT_3D ( 'NONE', #905, #60606, #43328 ) ;
#7904=DIRECTION ( 'NONE',  ( 0.000000000000000000, 0.000000000000000000, 1.000000000000000000 ) ) ;
#7905=EDGE_CURVE ( 'NONE', #58612, #16918, #24275, .T. ) ;
#7916=CARTESIAN_POINT ( 'NONE',  ( 0.000000000000000000, 44.88180994100468268, -63.18004540532978552 ) ) ;
#7919=ORIENTED_EDGE ( 'NONE', *, *, #22703, .F. ) ;
#7928=EDGE_LOOP ( 'NONE', ( #4269, #36616, #16259, #51125 ) ) ;
#7943=CARTESIAN_POINT ( 'NONE',  ( 10.00000000000000000, 0.000000000000000000, 0.000000000000000000 ) ) ;
#7945=CARTESIAN_POINT ( 'NONE',  ( 0.000000000000000000, 68.55367621811141987, 44.99326035066078333 ) ) ;
#7950=ORIENTED_EDGE ( 'NONE', *, *, #27324, .F. ) ;
#7953=ORIENTED_EDGE ( 'NONE', *, *, #58135, .T. ) ;
#7956=CARTESIAN_POINT ( 'NONE',  ( 10.00000000000000000, -68.55367621811173251, 44.99326035066030016 ) ) ;
#7966=EDGE_CURVE ( 'NONE', #63936, #44444, #42153, .T. ) ;
#7970=ORIENTED_EDGE ( 'NONE', *, *, #38696, .F. ) ;
#7973=AXIS2_PLACEMENT_3D ( 'NONE', #17331, #21467, #4584 ) ;
#7977=DIRECTION ( 'NONE',  ( -1.000000000000000000, -0.000000000000000000, -0.000000000000000000 ) ) ;
#7982=EDGE_CURVE ( 'NONE', #58170, #37734, #6609, .T. ) ;
#7986=VERTEX_POINT ( 'NONE', #12969 ) ;
#7991=DIRECTION ( 'NONE',  ( -1.000000000000000000, 0.000000000000000000, 0.000000000000000000 ) ) ;
#8000=EDGE_CURVE ( 'NONE', #2885, #34381, #31294, .T. ) ;
#8004=FACE_OUTER_BOUND ( 'NONE', #22549, .T. ) ;
#8005=CARTESIAN_POINT ( 'NONE',  ( 0.000000000000000000, 39.47590169984846398, 71.87247863392428826 ) ) ;
#8009=EDGE_CURVE ( 'NONE', #43566, #69008, #14492, .T. ) ;
#8013=CYLINDRICAL_SURFACE ( 'NONE', #62202, 32.00000000000000000 ) ;
#8016=CARTESIAN_POINT ( 'NONE',  ( 0.000000000000000000, 12.93880638057426502, -76.41127070299258150 ) ) ;
#8019=AXIS2_PLACEMENT_3D ( 'NONE', #45717, #5856, #28765 ) ;
#8025=CARTESIAN_POINT ( 'NONE',  ( 10.00000000000000000, 41.19522573413731692, 65.64334221924924861 ) ) ;
#8032=AXIS2_PLACEMENT_3D ( 'NONE', #25424, #48714, #71258 ) ;
#8035=ORIENTED_EDGE ( 'NONE', *, *, #15515, .T. ) ;
#8041=DIRECTION ( 'NONE',  ( 0.000000000000000000, 0.000000000000000000, 1.000000000000000000 ) ) ;
#8042=DIRECTION ( 'NONE',  ( -1.000000000000000000, 0.000000000000000000, 0.000000000000000000 ) ) ;
#8061=ORIENTED_EDGE ( 'NONE', *, *, #27146, .T. ) ;
#8091=CARTESIAN_POINT ( 'NONE',  ( 10.00000000000000000, 0.000000000000000000, 0.000000000000000000 ) ) ;
#8093=CARTESIAN_POINT ( 'NONE',  ( 0.000000000000000000, 60.67117009219216328, -55.16347631942977614 ) ) ;
#8100=LINE ( 'NONE', #12625, #29004 ) ;
#8101=ORIENTED_EDGE ( 'NONE', *, *, #19284, .T. ) ;
#8108=AXIS2_PLACEMENT_3D ( 'NONE', #49502, #66079, #20929 ) ;
#8110=VECTOR ( 'NONE', #62290, 1000.000000000000000 ) ;
#8111=CARTESIAN_POINT ( 'NONE',  ( 10.00000000000000000, 0.000000000000000000, 0.000000000000000000 ) ) ;
#8113=AXIS2_PLACEMENT_3D ( 'NONE', #58853, #45083, #30264 ) ;
#8119=LINE ( 'NONE', #25786, #66420 ) ;
#8133=EDGE_CURVE ( 'NONE', #10016, #42721, #4921, .T. ) ;
#8139=EDGE_CURVE ( 'NONE', #42336, #55165, #10912, .T. ) ;
#8153=ORIENTED_EDGE ( 'NONE', *, *, #73381, .F. ) ;
#8160=ADVANCED_FACE ( 'NONE', ( #66354 ), #65240, .T. ) ;
#8170=DIRECTION ( 'NONE',  ( -1.000000000000000000, -0.000000000000000000, 0.000000000000000000 ) ) ;
#8186=CARTESIAN_POINT ( 'NONE',  ( 10.00000000000000000, 11.30684508768339569, 76.66974797899841576 ) ) ;
#8187=VECTOR ( 'NONE', #67317, 1000.000000000000000 ) ;
#8196=EDGE_CURVE ( 'NONE', #27575, #37462, #19322, .T. ) ;
#8204=DIRECTION ( 'NONE',  ( -1.000000000000000000, -0.000000000000000000, 0.000000000000000000 ) ) ;
#8207=ORIENTED_EDGE ( 'NONE', *, *, #60885, .T. ) ;
#8219=CARTESIAN_POINT ( 'NONE',  ( 10.00000000000000000, -77.32052557432845674, 5.256550761632577284 ) ) ;
#8235=CIRCLE ( 'NONE', #70634, 31.99999999999999645 ) ;
#8237=ORIENTED_EDGE ( 'NONE', *, *, #10674, .F. ) ;
#8241=ORIENTED_EDGE ( 'NONE', *, *, #72901, .T. ) ;
#8254=CARTESIAN_POINT ( 'NONE',  ( 10.00000000000000000, 24.73286445877808148, -73.44644590900034586 ) ) ;
#8259=CARTESIAN_POINT ( 'NONE',  ( 10.00000000000000000, -73.72996012237449293, 14.67089635893687571 ) ) ;
#8261=CARTESIAN_POINT ( 'NONE',  ( 10.00000000000000000, -74.74816331893404708, -33.71516098798818462 ) ) ;
#8267=DIRECTION ( 'NONE',  ( -1.000000000000000000, 0.000000000000000000, 0.000000000000000000 ) ) ;
#8270=CARTESIAN_POINT ( 'NONE',  ( 10.00000000000000000, -31.47745569255092235, -68.26794271651296242 ) ) ;
#8275=CARTESIAN_POINT ( 'NONE',  ( 10.00000000000000000, 46.53671651294032330, -59.03961581697353012 ) ) ;
#8277=CIRCLE ( 'NONE', #34675, 82.00000000000000000 ) ;
#8280=DIRECTION ( 'NONE',  ( -1.000000000000000000, 0.000000000000000000, 0.000000000000000000 ) ) ;
#8290=CIRCLE ( 'NONE', #14298, 77.49899999999999523 ) ;
#8295=CIRCLE ( 'NONE', #28693, 77.49899999999999523 ) ;
#8297=ADVANCED_FACE ( 'NONE', ( #33600 ), #57284, .T. ) ;
#8302=CARTESIAN_POINT ( 'NONE',  ( 0.000000000000000000, 62.20884554314020676, 46.21855187248652896 ) ) ;
#8303=ORIENTED_EDGE ( 'NONE', *, *, #13057, .T. ) ;
#8309=EDGE_CURVE ( 'NONE', #51433, #55666, #51642, .T. ) ;
#8336=VERTEX_POINT ( 'NONE', #27204 ) ;
#8340=CARTESIAN_POINT ( 'NONE',  ( 0.000000000000000000, 71.87247863392471459, -39.47590169984770370 ) ) ;
#8349=VERTEX_POINT ( 'NONE', #13265 ) ;
#8353=FACE_OUTER_BOUND ( 'NONE', #22657, .T. ) ;
#8359=DIRECTION ( 'NONE',  ( -1.000000000000000000, 0.000000000000000000, -0.000000000000000000 ) ) ;
#8360=DIRECTION ( 'NONE',  ( -1.000000000000000000, -0.000000000000000000, 0.000000000000000000 ) ) ;
#8372=DIRECTION ( 'NONE',  ( 0.000000000000000000, -0.07845909572785234043, 0.9969173337331274087 ) ) ;
#8380=DIRECTION ( 'NONE',  ( -1.000000000000000000, 0.000000000000000000, -0.000000000000000000 ) ) ;
#8385=FACE_OUTER_BOUND ( 'NONE', #41620, .T. ) ;
#8394=CARTESIAN_POINT ( 'NONE',  ( 10.00000000000000000, -68.26794271651286294, 31.47745569255117104 ) ) ;
#8398=CYLINDRICAL_SURFACE ( 'NONE', #10889, 77.49899999999999523 ) ;
#8400=ORIENTED_EDGE ( 'NONE', *, *, #43161, .F. ) ;
#8401=CARTESIAN_POINT ( 'NONE',  ( 10.00000000000000000, 0.000000000000000000, 0.000000000000000000 ) ) ;
#8405=VERTEX_POINT ( 'NONE', #17431 ) ;
#8427=VERTEX_POINT ( 'NONE', #1300 ) ;
#8434=CYLINDRICAL_SURFACE ( 'NONE', #763, 82.00000000000000000 ) ;
#8435=DIRECTION ( 'NONE',  ( 0.000000000000000000, -0.9876883405951359940, -0.1564344650402420822 ) ) ;
#8437=DIRECTION ( 'NONE',  ( -1.000000000000000000, -0.000000000000000000, -0.000000000000000000 ) ) ;
#8442=EDGE_CURVE ( 'NONE', #1463, #63017, #29072, .T. ) ;
#8448=CARTESIAN_POINT ( 'NONE',  ( 10.00000000000000000, 46.11716303203188261, 67.80270845531904911 ) ) ;
#8451=CYLINDRICAL_SURFACE ( 'NONE', #66698, 82.00000000000000000 ) ;
#8473=DIRECTION ( 'NONE',  ( -1.000000000000000000, -0.000000000000000000, -0.000000000000000000 ) ) ;
#8475=( NAMED_UNIT ( * ) PLANE_ANGLE_UNIT ( ) SI_UNIT ( $, .RADIAN. ) );
#8478=DIRECTION ( 'NONE',  ( 0.000000000000000000, 0.9238795325112877377, -0.3826834323650873948 ) ) ;
#8486=CARTESIAN_POINT ( 'NONE',  ( 0.000000000000000000, 0.000000000000000000, 0.000000000000000000 ) ) ;
#8499=ORIENTED_EDGE ( 'NONE', *, *, #62259, .F. ) ;
#8506=LINE ( 'NONE', #30311, #35082 ) ;
#8511=VERTEX_POINT ( 'NONE', #55242 ) ;
#8522=CIRCLE ( 'NONE', #1382, 77.49899999999999523 ) ;
#8540=DIRECTION ( 'NONE',  ( 0.000000000000000000, 0.000000000000000000, 1.000000000000000000 ) ) ;
#8542=ORIENTED_EDGE ( 'NONE', *, *, #30915, .F. ) ;
#8545=PRODUCT_DEFINITION_SHAPE ( 'NONE', 'NONE',  #5869 ) ;
#8549=ORIENTED_EDGE ( 'NONE', *, *, #28083, .F. ) ;
#8555=CIRCLE ( 'NONE', #50557, 31.99999999999999645 ) ;
#8565=CARTESIAN_POINT ( 'NONE',  ( 10.00000000000000000, -39.78640506895653317, 66.50666863321987421 ) ) ;
#8567=DIRECTION ( 'NONE',  ( -1.000000000000000000, 0.000000000000000000, 0.000000000000000000 ) ) ;
#8568=VERTEX_POINT ( 'NONE', #61632 ) ;
#8569=EDGE_CURVE ( 'NONE', #36612, #58170, #51807, .T. ) ;
#8573=CIRCLE ( 'NONE', #30126, 77.49899999999999523 ) ;
#8578=ORIENTED_EDGE ( 'NONE', *, *, #2992, .F. ) ;
#8581=DIRECTION ( 'NONE',  ( 0.000000000000000000, -6.938893903907228378E-15, 1.000000000000000000 ) ) ;
#8582=CARTESIAN_POINT ( 'NONE',  ( 10.00000000000000000, 71.21200624218795383, 40.65526001592638039 ) ) ;
#8597=VERTEX_POINT ( 'NONE', #27027 ) ;
#8600=ADVANCED_FACE ( 'NONE', ( #49959 ), #4135, .T. ) ;
#8604=DIRECTION ( 'NONE',  ( -1.000000000000000000, 0.000000000000000000, -0.000000000000000000 ) ) ;
#8620=DIRECTION ( 'NONE',  ( 0.000000000000000000, 0.000000000000000000, 1.000000000000000000 ) ) ;
#8623=CIRCLE ( 'NONE', #21812, 77.49899999999999523 ) ;
#8626=ORIENTED_EDGE ( 'NONE', *, *, #6312, .T. ) ;
#8639=CARTESIAN_POINT ( 'NONE',  ( 10.00000000000000000, 73.95703589264006439, -23.16143007188350822 ) ) ;
#8640=DIRECTION ( 'NONE',  ( -1.000000000000000000, 0.000000000000000000, 0.000000000000000000 ) ) ;
#8642=CARTESIAN_POINT ( 'NONE',  ( 10.00000000000000000, -41.19522573413780009, 65.64334221924896440 ) ) ;
#8645=CARTESIAN_POINT ( 'NONE',  ( 5.000000000000000000, 27.74655509720669500, 77.16300072079670258 ) ) ;
#8651=CARTESIAN_POINT ( 'NONE',  ( 10.00000000000000000, 77.49459641780886443, 0.8261519478433866359 ) ) ;
#8656=ADVANCED_FACE ( 'NONE', ( #51831 ), #17618, .T. ) ;
#8658=AXIS2_PLACEMENT_3D ( 'NONE', #31547, #1924, #24443 ) ;
#8672=CARTESIAN_POINT ( 'NONE',  ( 0.000000000000000000, -54.21277698773636899, -55.38113227695839669 ) ) ;
#8673=AXIS2_PLACEMENT_3D ( 'NONE', #47988, #59267, #8870 ) ;
#8674=CIRCLE ( 'NONE', #38678, 77.49899999999999523 ) ;
#8677=DIRECTION ( 'NONE',  ( 0.000000000000000000, 0.000000000000000000, 1.000000000000000000 ) ) ;
#8683=ORIENTED_EDGE ( 'NONE', *, *, #59437, .T. ) ;
#8692=ORIENTED_EDGE ( 'NONE', *, *, #8442, .T. ) ;
#8694=FACE_OUTER_BOUND ( 'NONE', #18315, .T. ) ;
#8697=ORIENTED_EDGE ( 'NONE', *, *, #59032, .F. ) ;
#8706=ORIENTED_EDGE ( 'NONE', *, *, #54582, .T. ) ;
#8708=ORIENTED_EDGE ( 'NONE', *, *, #31914, .T. ) ;
#8716=EDGE_CURVE ( 'NONE', #29107, #42748, #16980, .T. ) ;
#8724=FACE_OUTER_BOUND ( 'NONE', #69881, .T. ) ;
#8728=DIRECTION ( 'NONE',  ( 1.000000000000000000, -0.000000000000000000, -0.000000000000000000 ) ) ;
#8738=DIRECTION ( 'NONE',  ( -1.000000000000000000, 0.000000000000000000, -0.000000000000000000 ) ) ;
#8742=DIRECTION ( 'NONE',  ( 0.000000000000000000, 0.000000000000000000, 1.000000000000000000 ) ) ;
#8743=VERTEX_POINT ( 'NONE', #52193 ) ;
#8744=DIRECTION ( 'NONE',  ( 1.000000000000000000, 0.000000000000000000, 0.000000000000000000 ) ) ;
#8746=ADVANCED_FACE ( 'NONE', ( #17252 ), #57113, .T. ) ;
#8749=LINE ( 'NONE', #71511, #60986 ) ;
#8751=DIRECTION ( 'NONE',  ( 0.000000000000000000, 0.000000000000000000, 1.000000000000000000 ) ) ;
#8774=AXIS2_PLACEMENT_3D ( 'NONE', #68763, #40187, #62008 ) ;
#8776=CIRCLE ( 'NONE', #50791, 82.00000000000000000 ) ;
#8779=ORIENTED_EDGE ( 'NONE', *, *, #73845, .F. ) ;
#8789=ORIENTED_EDGE ( 'NONE', *, *, #28605, .F. ) ;
#8792=VERTEX_POINT ( 'NONE', #47662 ) ;
#8794=FACE_OUTER_BOUND ( 'NONE', #52708, .T. ) ;
#8795=DIRECTION ( 'NONE',  ( -1.000000000000000000, -0.000000000000000000, -0.000000000000000000 ) ) ;
#8799=DIRECTION ( 'NONE',  ( 0.000000000000000000, 0.000000000000000000, 1.000000000000000000 ) ) ;
#8802=VERTEX_POINT ( 'NONE', #65704 ) ;
#8813=FACE_OUTER_BOUND ( 'NONE', #4850, .T. ) ;
#8818=EDGE_CURVE ( 'NONE', #32719, #63900, #67361, .T. ) ;
#8829=VECTOR ( 'NONE', #72167, 1000.000000000000000 ) ;
#8838=CARTESIAN_POINT ( 'NONE',  ( 10.00000000000000000, 70.52718814184294160, -26.02418014898236720 ) ) ;
#8849=DIRECTION ( 'NONE',  ( 0.000000000000000000, 0.000000000000000000, 1.000000000000000000 ) ) ;
#8851=CARTESIAN_POINT ( 'NONE',  ( 10.00000000000000000, 74.65491531819118620, -8.830959090342659579 ) ) ;
#8853=DIRECTION ( 'NONE',  ( -1.000000000000000000, -0.000000000000000000, -0.000000000000000000 ) ) ;
#8856=ORIENTED_EDGE ( 'NONE', *, *, #6956, .F. ) ;
#8858=VECTOR ( 'NONE', #41208, 1000.000000000000000 ) ;
#8870=DIRECTION ( 'NONE',  ( 0.000000000000000000, 0.000000000000000000, 1.000000000000000000 ) ) ;
#8874=ORIENTED_EDGE ( 'NONE', *, *, #17433, .F. ) ;
#8896=AXIS2_PLACEMENT_3D ( 'NONE', #33948, #72665, #21168 ) ;
#8897=EDGE_CURVE ( 'NONE', #73838, #1522, #8555, .T. ) ;
#8905=ORIENTED_EDGE ( 'NONE', *, *, #43896, .T. ) ;
#8913=EDGE_CURVE ( 'NONE', #56500, #64668, #21794, .T. ) ;
#8918=CARTESIAN_POINT ( 'NONE',  ( 0.000000000000000000, -70.53064760720336324, 26.01480285779810231 ) ) ;
#8920=DIRECTION ( 'NONE',  ( -1.000000000000000000, 0.000000000000000000, 0.000000000000000000 ) ) ;
#8951=VERTEX_POINT ( 'NONE', #3310 ) ;
#8954=DIRECTION ( 'NONE',  ( -1.000000000000000000, 0.000000000000000000, -0.000000000000000000 ) ) ;
#8956=ORIENTED_EDGE ( 'NONE', *, *, #38614, .F. ) ;
#8960=CARTESIAN_POINT ( 'NONE',  ( 10.00000000000000000, 0.000000000000000000, 0.000000000000000000 ) ) ;
#8966=DIRECTION ( 'NONE',  ( -1.000000000000000000, 0.000000000000000000, 0.000000000000000000 ) ) ;
#8968=CARTESIAN_POINT ( 'NONE',  ( 5.000000000000002665, 80.55351364060589958, 15.33399622253511829 ) ) ;
#8998=ORIENTED_EDGE ( 'NONE', *, *, #73691, .T. ) ;
#9004=LINE ( 'NONE', #26285, #70368 ) ;
#9005=DIRECTION ( 'NONE',  ( 1.000000000000000000, 0.000000000000000000, 0.000000000000000000 ) ) ;
#9007=DIRECTION ( 'NONE',  ( -1.000000000000000000, 0.000000000000000000, 0.000000000000000000 ) ) ;
#9008=DIRECTION ( 'NONE',  ( 0.000000000000000000, 0.000000000000000000, 1.000000000000000000 ) ) ;
#9011=DIRECTION ( 'NONE',  ( 0.000000000000000000, -0.4539904997395541875, 0.8910065241883642351 ) ) ;
#9026=AXIS2_PLACEMENT_3D ( 'NONE', #63429, #11903, #675 ) ;
#9035=VERTEX_POINT ( 'NONE', #37508 ) ;
#9037=FACE_OUTER_BOUND ( 'NONE', #15125, .T. ) ;
#9055=DIRECTION ( 'NONE',  ( -1.000000000000000000, -0.000000000000000000, 0.000000000000000000 ) ) ;
#9056=EDGE_LOOP ( 'NONE', ( #6093, #21507, #47476, #36442 ) ) ;
#9057=DIRECTION ( 'NONE',  ( -1.000000000000000000, 0.000000000000000000, 0.000000000000000000 ) ) ;
#9082=EDGE_CURVE ( 'NONE', #44963, #47803, #16882, .T. ) ;
#9088=CARTESIAN_POINT ( 'NONE',  ( 0.000000000000000000, -50.95692526931286181, -58.39081064771806240 ) ) ;
#9091=DIRECTION ( 'NONE',  ( -1.000000000000000000, -0.000000000000000000, 0.000000000000000000 ) ) ;
#9093=CIRCLE ( 'NONE', #51112, 82.00000000000000000 ) ;
#9098=CARTESIAN_POINT ( 'NONE',  ( 5.000000000000002665, -3.894527615418464705, 81.90746397400387480 ) ) ;
#9101=CARTESIAN_POINT ( 'NONE',  ( 10.00000000000000000, 0.000000000000000000, 0.000000000000000000 ) ) ;
#9104=AXIS2_PLACEMENT_3D ( 'NONE', #23797, #46737, #69661 ) ;
#9105=ORIENTED_EDGE ( 'NONE', *, *, #45797, .F. ) ;
#9107=CARTESIAN_POINT ( 'NONE',  ( 10.00000000000000000, 62.20884554314086046, -46.21855187248561236 ) ) ;
#9109=CARTESIAN_POINT ( 'NONE',  ( 10.00000000000000000, -8.840884882374576037, -74.65374052328658649 ) ) ;
#9119=ORIENTED_EDGE ( 'NONE', *, *, #17264, .T. ) ;
#9145=CIRCLE ( 'NONE', #30757, 31.99999999999998934 ) ;
#9150=ORIENTED_EDGE ( 'NONE', *, *, #58047, .T. ) ;
#9151=EDGE_CURVE ( 'NONE', #58172, #63936, #647, .T. ) ;
#9153=EDGE_LOOP ( 'NONE', ( #8956, #49579, #9411, #1338 ) ) ;
#9158=DIRECTION ( 'NONE',  ( 0.000000000000000000, 0.1564344650402244019, 0.9876883405951387696 ) ) ;
#9178=DIRECTION ( 'NONE',  ( -1.000000000000000000, -0.000000000000000000, -0.000000000000000000 ) ) ;
#9189=DIRECTION ( 'NONE',  ( -1.000000000000000000, -0.000000000000000000, -0.000000000000000000 ) ) ;
#9191=DIRECTION ( 'NONE',  ( 0.000000000000000000, 0.000000000000000000, 1.000000000000000000 ) ) ;
#9194=AXIS2_PLACEMENT_3D ( 'NONE', #11309, #41372, #17695 ) ;
#9198=LINE ( 'NONE', #56176, #67881 ) ;
#9204=CARTESIAN_POINT ( 'NONE',  ( 50.00005079999999680, 12.24744871391589207, -2.500000000000000000 ) ) ;
#9221=EDGE_CURVE ( 'NONE', #14488, #54604, #16043, .T. ) ;
#9236=ADVANCED_FACE ( 'NONE', ( #61921 ), #57760, .T. ) ;
#9239=ORIENTED_EDGE ( 'NONE', *, *, #54508, .T. ) ;
#9240=FACE_OUTER_BOUND ( 'NONE', #23239, .T. ) ;
#9249=ORIENTED_EDGE ( 'NONE', *, *, #65311, .F. ) ;
#9260=EDGE_CURVE ( 'NONE', #46225, #73479, #27697, .T. ) ;
#9271=ORIENTED_EDGE ( 'NONE', *, *, #69519, .F. ) ;
#9272=CYLINDRICAL_SURFACE ( 'NONE', #37925, 31.99999999999999289 ) ;
#9283=FACE_OUTER_BOUND ( 'NONE', #1801, .T. ) ;
#9287=CARTESIAN_POINT ( 'NONE',  ( 10.00000000000000000, 23.16143007188532366, -73.95703589263949596 ) ) ;
#9289=DIRECTION ( 'NONE',  ( -1.000000000000000000, 0.000000000000000000, -0.000000000000000000 ) ) ;
#9309=ADVANCED_FACE ( 'NONE', ( #36662 ), #30640, .T. ) ;
#9310=CIRCLE ( 'NONE', #70528, 31.99999999999998579 ) ;
#9316=CARTESIAN_POINT ( 'NONE',  ( 10.00000000000000000, 0.000000000000000000, 0.000000000000000000 ) ) ;
#9324=DIRECTION ( 'NONE',  ( 0.000000000000000000, 0.000000000000000000, 1.000000000000000000 ) ) ;
#9326=CYLINDRICAL_SURFACE ( 'NONE', #551, 77.49899999999999523 ) ;
#9327=ORIENTED_EDGE ( 'NONE', *, *, #9782, .F. ) ;
#9335=ORIENTED_EDGE ( 'NONE', *, *, #12557, .T. ) ;
#9341=ORIENTED_EDGE ( 'NONE', *, *, #33801, .F. ) ;
#9343=CIRCLE ( 'NONE', #48996, 77.49899999999999523 ) ;
#9349=ORIENTED_EDGE ( 'NONE', *, *, #63822, .F. ) ;
#9350=ORIENTED_EDGE ( 'NONE', *, *, #1593, .F. ) ;
#9356=ADVANCED_FACE ( 'NONE', ( #2507 ), #52468, .T. ) ;
#9359=ORIENTED_EDGE ( 'NONE', *, *, #22404, .F. ) ;
#9362=VERTEX_POINT ( 'NONE', #23912 ) ;
#9364=CARTESIAN_POINT ( 'NONE',  ( 10.00000000000000000, 0.000000000000000000, 0.000000000000000000 ) ) ;
#9366=DIRECTION ( 'NONE',  ( -1.000000000000000000, 0.000000000000000000, 0.000000000000000000 ) ) ;
#9367=EDGE_CURVE ( 'NONE', #1777, #43566, #2487, .T. ) ;
#9375=AXIS2_PLACEMENT_3D ( 'NONE', #1336, #6200, #6561 ) ;
#9379=DIRECTION ( 'NONE',  ( -1.000000000000000000, -0.000000000000000000, 0.000000000000000000 ) ) ;
#9381=AXIS2_PLACEMENT_3D ( 'NONE', #62880, #38805, #21498 ) ;
#9390=DIRECTION ( 'NONE',  ( -1.000000000000000000, 0.000000000000000000, -0.000000000000000000 ) ) ;
#9393=AXIS2_PLACEMENT_3D ( 'NONE', #21872, #60359, #8478 ) ;
#9398=AXIS2_PLACEMENT_3D ( 'NONE', #23549, #39742, #69403 ) ;
#9401=EDGE_LOOP ( 'NONE', ( #54073, #46609, #21900, #33225 ) ) ;
#9402=EDGE_CURVE ( 'NONE', #8802, #7419, #50454, .T. ) ;
#9411=ORIENTED_EDGE ( 'NONE', *, *, #2588, .T. ) ;
#9418=ORIENTED_EDGE ( 'NONE', *, *, #34616, .T. ) ;
#9427=FACE_OUTER_BOUND ( 'NONE', #3563, .T. ) ;
#9438=VERTEX_POINT ( 'NONE', #54700 ) ;
#9441=CYLINDRICAL_SURFACE ( 'NONE', #62522, 31.99999999999999289 ) ;
#9447=ORIENTED_EDGE ( 'NONE', *, *, #57754, .T. ) ;
#9448=DIRECTION ( 'NONE',  ( -1.000000000000000000, -0.000000000000000000, 0.000000000000000000 ) ) ;
#9449=DIRECTION ( 'NONE',  ( -1.000000000000000000, 0.000000000000000000, 0.000000000000000000 ) ) ;
#9452=FACE_OUTER_BOUND ( 'NONE', #25349, .T. ) ;
#9455=AXIS2_PLACEMENT_3D ( 'NONE', #65804, #8280, #31208 ) ;
#9459=ORIENTED_EDGE ( 'NONE', *, *, #10122, .T. ) ;
#9472=AXIS2_PLACEMENT_3D ( 'NONE', #58281, #42478, #24437 ) ;
#9479=CIRCLE ( 'NONE', #51501, 31.99999999999999289 ) ;
#9495=EDGE_CURVE ( 'NONE', #54579, #8511, #15211, .T. ) ;
#9502=CARTESIAN_POINT ( 'NONE',  ( -10.00000000000000000, 0.000000000000000000, 0.000000000000000000 ) ) ;
#9504=ORIENTED_EDGE ( 'NONE', *, *, #18935, .T. ) ;
#9506=CIRCLE ( 'NONE', #35956, 32.00000000000000000 ) ;
#9519=ADVANCED_FACE ( 'NONE', ( #3596 ), #26859, .T. ) ;
#9536=CYLINDRICAL_SURFACE ( 'NONE', #12570, 31.99999999999999289 ) ;
#9538=DIRECTION ( 'NONE',  ( -1.000000000000000000, -0.000000000000000000, 0.000000000000000000 ) ) ;
#9557=DIRECTION ( 'NONE',  ( 1.000000000000000000, 0.000000000000000000, 0.000000000000000000 ) ) ;
#9564=DIRECTION ( 'NONE',  ( 0.000000000000000000, 0.9510565162951546414, -0.3090169943749446202 ) ) ;
#9575=DIRECTION ( 'NONE',  ( 0.000000000000000000, 0.000000000000000000, 1.000000000000000000 ) ) ;
#9576=CIRCLE ( 'NONE', #33548, 31.99999999999999289 ) ;
#9579=EDGE_CURVE ( 'NONE', #26686, #36758, #8235, .T. ) ;
#9580=LINE ( 'NONE', #55441, #61410 ) ;
#9582=EDGE_CURVE ( 'NONE', #23124, #16471, #7000, .T. ) ;
#9587=CARTESIAN_POINT ( 'NONE',  ( 5.000000000000002665, -40.65526001592565564, -71.21200624218839437 ) ) ;
#9590=DIRECTION ( 'NONE',  ( -1.000000000000000000, 0.000000000000000000, 0.000000000000000000 ) ) ;
#9593=AXIS2_PLACEMENT_3D ( 'NONE', #57858, #52202, #69496 ) ;
#9596=VECTOR ( 'NONE', #58594, 1000.000000000000000 ) ;
#9603=ORIENTED_EDGE ( 'NONE', *, *, #56716, .T. ) ;
#9608=DIRECTION ( 'NONE',  ( 0.000000000000000000, 1.000000000000000000, 0.000000000000000000 ) ) ;
#9611=DIRECTION ( 'NONE',  ( 0.000000000000000000, 0.000000000000000000, 1.000000000000000000 ) ) ;
#9617=ORIENTED_EDGE ( 'NONE', *, *, #59491, .F. ) ;
#9625=DIRECTION ( 'NONE',  ( -1.000000000000000000, -0.000000000000000000, -0.000000000000000000 ) ) ;
#9631=CARTESIAN_POINT ( 'NONE',  ( 10.00000000000000000, -73.72996012237429397, -14.67089635893794508 ) ) ;
#9632=VERTEX_POINT ( 'NONE', #202 ) ;
#9637=CARTESIAN_POINT ( 'NONE',  ( 10.00000000000000000, 8.840884882375075193, 74.65374052328651544 ) ) ;
#9641=DIRECTION ( 'NONE',  ( 0.000000000000000000, 0.7604059656000277112, 0.6494480483301875440 ) ) ;
#9649=AXIS2_PLACEMENT_3D ( 'NONE', #54626, #25326, #26045 ) ;
#9662=CARTESIAN_POINT ( 'NONE',  ( 0.000000000000000000, 24.73286445877703699, 73.44644590900068692 ) ) ;
#9667=DIRECTION ( 'NONE',  ( -1.000000000000000000, -0.000000000000000000, 0.000000000000000000 ) ) ;
#9668=EDGE_CURVE ( 'NONE', #14681, #57613, #3429, .T. ) ;
#9671=ADVANCED_FACE ( 'NONE', ( #28349 ), #73469, .T. ) ;
#9678=CARTESIAN_POINT ( 'NONE',  ( 10.00000000000000000, -46.54456581323847786, 59.03342792756247093 ) ) ;
#9679=CYLINDRICAL_SURFACE ( 'NONE', #6651, 82.00000000000000000 ) ;
#9680=ORIENTED_EDGE ( 'NONE', *, *, #25291, .F. ) ;
#9690=CIRCLE ( 'NONE', #45741, 31.99999999999999289 ) ;
#9699=CARTESIAN_POINT ( 'NONE',  ( 5.000000000000002665, 8.966570791701863996, -81.50828551894218776 ) ) ;
#9703=DIRECTION ( 'NONE',  ( 0.000000000000000000, 0.6494480483301849905, -0.7604059656000299317 ) ) ;
#9706=CYLINDRICAL_SURFACE ( 'NONE', #33320, 31.99999999999999289 ) ;
#9708=CARTESIAN_POINT ( 'NONE',  ( 10.00000000000000000, 65.64334221924966073, -41.19522573413664190 ) ) ;
#9714=CARTESIAN_POINT ( 'NONE',  ( 0.000000000000000000, -74.65491531819111515, -8.830959090343204920 ) ) ;
#9716=DIRECTION ( 'NONE',  ( -1.000000000000000000, 0.000000000000000000, 0.000000000000000000 ) ) ;
#9731=DIRECTION ( 'NONE',  ( 0.000000000000000000, 0.000000000000000000, 1.000000000000000000 ) ) ;
#9732=ORIENTED_EDGE ( 'NONE', *, *, #44659, .T. ) ;
#9733=CARTESIAN_POINT ( 'NONE',  ( 0.000000000000000000, 69.42325613327439271, 34.44570377933623462 ) ) ;
#9739=ORIENTED_EDGE ( 'NONE', *, *, #28718, .F. ) ;
#9740=LINE ( 'NONE', #55604, #1502 ) ;
#9768=LINE ( 'NONE', #49607, #31107 ) ;
#9769=ADVANCED_FACE ( 'NONE', ( #13649 ), #70049, .T. ) ;
#9776=EDGE_CURVE ( 'NONE', #45747, #12010, #35819, .T. ) ;
#9779=VERTEX_POINT ( 'NONE', #18553 ) ;
#9780=EDGE_LOOP ( 'NONE', ( #22673, #18693, #12667, #33202 ) ) ;
#9782=EDGE_CURVE ( 'NONE', #11119, #59559, #13006, .T. ) ;
#9799=EDGE_LOOP ( 'NONE', ( #15518, #59543, #33915, #58794 ) ) ;
#9800=DIRECTION ( 'NONE',  ( -1.000000000000000000, 0.000000000000000000, 0.000000000000000000 ) ) ;
#9821=DIRECTION ( 'NONE',  ( 0.000000000000000000, -0.7071067811865389130, -0.7071067811865561215 ) ) ;
#9823=CARTESIAN_POINT ( 'NONE',  ( 0.000000000000000000, 0.000000000000000000, 0.000000000000000000 ) ) ;
#9827=MECHANICAL_DESIGN_GEOMETRIC_PRESENTATION_REPRESENTATION('',(#47033),#49434);
#9834=EDGE_CURVE ( 'NONE', #46909, #21857, #42244, .T. ) ;
#9847=CARTESIAN_POINT ( 'NONE',  ( 0.000000000000000000, -75.11725578898470701, 2.956366410620372864 ) ) ;
#9850=CARTESIAN_POINT ( 'NONE',  ( 5.000000000000002665, -81.34940948281328588, -10.30890764327469711 ) ) ;
#9862=LINE ( 'NONE', #50451, #5353 ) ;
#9871=EDGE_LOOP ( 'NONE', ( #4648, #4869, #37631, #56550 ) ) ;
#9876=ORIENTED_EDGE ( 'NONE', *, *, #20156, .T. ) ;
#9879=AXIS2_PLACEMENT_3D ( 'NONE', #53313, #64595, #70957 ) ;
#9891=VERTEX_POINT ( 'NONE', #65542 ) ;
#9902=CYLINDRICAL_SURFACE ( 'NONE', #58292, 31.99999999999999289 ) ;
#9904=CARTESIAN_POINT ( 'NONE',  ( 10.00000000000000000, 0.000000000000000000, 0.000000000000000000 ) ) ;
#9910=VERTEX_POINT ( 'NONE', #37712 ) ;
#9919=DIRECTION ( 'NONE',  ( 0.000000000000000000, 0.000000000000000000, 1.000000000000000000 ) ) ;
#9934=EDGE_LOOP ( 'NONE', ( #38381, #20928, #26410, #18533 ) ) ;
#9949=EDGE_LOOP ( 'NONE', ( #38138, #9239, #71183, #58428 ) ) ;
#9953=EDGE_CURVE ( 'NONE', #36612, #60921, #55087, .T. ) ;
#9958=EDGE_LOOP ( 'NONE', ( #20346, #69259, #3930, #9335 ) ) ;
#9961=CARTESIAN_POINT ( 'NONE',  ( 0.000000000000000000, -71.21200624218825226, 40.65526001592589722 ) ) ;
#9972=CARTESIAN_POINT ( 'NONE',  ( 10.00000000000000000, 0.000000000000000000, 0.000000000000000000 ) ) ;
#9979=VERTEX_POINT ( 'NONE', #2789 ) ;
#9993=DIRECTION ( 'NONE',  ( -1.000000000000000000, -0.000000000000000000, -0.000000000000000000 ) ) ;
#9997=AXIS2_PLACEMENT_3D ( 'NONE', #40490, #53253, #12648 ) ;
#9998=ORIENTED_EDGE ( 'NONE', *, *, #33145, .T. ) ;
#10003=EDGE_CURVE ( 'NONE', #16822, #69125, #38296, .T. ) ;
#10009=CIRCLE ( 'NONE', #52026, 77.49900000000002365 ) ;
#10016=VERTEX_POINT ( 'NONE', #25541 ) ;
#10020=ORIENTED_EDGE ( 'NONE', *, *, #4422, .F. ) ;
#10028=CARTESIAN_POINT ( 'NONE',  ( 10.00000000000000000, -77.16300072079680206, 27.74655509720639657 ) ) ;
#10030=DIRECTION ( 'NONE',  ( 0.000000000000000000, -0.8526401643540970632, 0.5224985647159411384 ) ) ;
#10035=ADVANCED_FACE ( 'NONE', ( #48478 ), #24804, .T. ) ;
#10043=DIRECTION ( 'NONE',  ( -1.000000000000000000, 0.000000000000000000, -0.000000000000000000 ) ) ;
#10046=FACE_OUTER_BOUND ( 'NONE', #30433, .T. ) ;
#10047=ORIENTED_EDGE ( 'NONE', *, *, #69075, .F. ) ;
#10051=CARTESIAN_POINT ( 'NONE',  ( 0.000000000000000000, 27.74655509720779634, -77.16300072079631889 ) ) ;
#10052=CARTESIAN_POINT ( 'NONE',  ( 0.000000000000000000, 0.000000000000000000, 0.000000000000000000 ) ) ;
#10053=AXIS2_PLACEMENT_3D ( 'NONE', #71689, #37873, #14183 ) ;
#10067=VERTEX_POINT ( 'NONE', #7521 ) ;
#10068=CARTESIAN_POINT ( 'NONE',  ( 10.00000000000000000, 31.47745569255140552, 68.26794271651274926 ) ) ;
#10073=EDGE_CURVE ( 'NONE', #41590, #48015, #52740, .T. ) ;
#10084=ORIENTED_EDGE ( 'NONE', *, *, #56033, .F. ) ;
#10092=FACE_OUTER_BOUND ( 'NONE', #67310, .T. ) ;
#10095=LINE ( 'NONE', #33017, #59704 ) ;
#10102=DIRECTION ( 'NONE',  ( -1.000000000000000000, 0.000000000000000000, -0.000000000000000000 ) ) ;
#10109=ADVANCED_FACE ( 'NONE', ( #47734 ), #12774, .T. ) ;
#10110=DIRECTION ( 'NONE',  ( 0.000000000000000000, -0.9876883405951359940, -0.1564344650402420267 ) ) ;
#10119=CYLINDRICAL_SURFACE ( 'NONE', #36070, 31.99999999999998579 ) ;
#10122=EDGE_CURVE ( 'NONE', #44625, #36499, #30797, .T. ) ;
#10126=DIRECTION ( 'NONE',  ( 0.000000000000000000, -0.8526401643540860720, -0.5224985647159590130 ) ) ;
#10127=EDGE_CURVE ( 'NONE', #8792, #8349, #62304, .T. ) ;
#10138=CYLINDRICAL_SURFACE ( 'NONE', #28729, 77.49899999999999523 ) ;
#10156=CARTESIAN_POINT ( 'NONE',  ( 10.00000000000000000, 0.000000000000000000, 0.000000000000000000 ) ) ;
#10172=ORIENTED_EDGE ( 'NONE', *, *, #9668, .F. ) ;
#10197=CARTESIAN_POINT ( 'NONE',  ( 10.00000000000000000, 0.000000000000000000, 0.000000000000000000 ) ) ;
#10198=CARTESIAN_POINT ( 'NONE',  ( 10.00000000000000000, 2.956366410620650420, 75.11725578898469280 ) ) ;
#10201=CIRCLE ( 'NONE', #52219, 31.99999999999998579 ) ;
#10208=CARTESIAN_POINT ( 'NONE',  ( 0.000000000000000000, 68.67312586195046720, -35.91791733033402068 ) ) ;
#10215=DIRECTION ( 'NONE',  ( -1.000000000000000000, -0.000000000000000000, 0.000000000000000000 ) ) ;
#10217=CARTESIAN_POINT ( 'NONE',  ( 10.00000000000000000, 0.000000000000000000, 0.000000000000000000 ) ) ;
#10219=CARTESIAN_POINT ( 'NONE',  ( 10.00000000000000000, -46.53671651293907274, -59.03961581697448935 ) ) ;
#10236=AXIS2_PLACEMENT_3D ( 'NONE', #49522, #72448, #48783 ) ;
#10238=CARTESIAN_POINT ( 'NONE',  ( 0.000000000000000000, -55.16347631942998220, -60.67117009219196433 ) ) ;
#10245=AXIS2_PLACEMENT_3D ( 'NONE', #42644, #8437, #43407 ) ;
#10249=VERTEX_POINT ( 'NONE', #68464 ) ;
#10253=DIRECTION ( 'NONE',  ( 0.000000000000000000, 0.000000000000000000, -1.000000000000000000 ) ) ;
#10254=ORIENTED_EDGE ( 'NONE', *, *, #10623, .F. ) ;
#10255=VERTEX_POINT ( 'NONE', #51149 ) ;
#10265=ORIENTED_EDGE ( 'NONE', *, *, #42684, .F. ) ;
#10267=VERTEX_POINT ( 'NONE', #5684 ) ;
#10276=CARTESIAN_POINT ( 'NONE',  ( 0.000000000000000000, -62.50884508063453637, 41.76106447765467777 ) ) ;
#10299=STYLED_ITEM ( 'NONE', ( #49708 ), #37525 ) ;
#10302=DIRECTION ( 'NONE',  ( 0.000000000000000000, -0.3090169943749548898, 0.9510565162951511997 ) ) ;
#10307=CARTESIAN_POINT ( 'NONE',  ( 10.00000000000000000, -76.41127070299262414, -12.93880638057396304 ) ) ;
#10314=LINE ( 'NONE', #27605, #46495 ) ;
#10326=CIRCLE ( 'NONE', #3115, 77.49900000000000944 ) ;
#10339=ORIENTED_EDGE ( 'NONE', *, *, #58569, .T. ) ;
#10343=EDGE_CURVE ( 'NONE', #62606, #57645, #47373, .T. ) ;
#10345=VERTEX_POINT ( 'NONE', #7150 ) ;
#10352=ORIENTED_EDGE ( 'NONE', *, *, #14283, .F. ) ;
#10363=ORIENTED_EDGE ( 'NONE', *, *, #39164, .F. ) ;
#10367=ORIENTED_EDGE ( 'NONE', *, *, #66821, .T. ) ;
#10402=DIRECTION ( 'NONE',  ( -1.000000000000000000, 0.000000000000000000, 0.000000000000000000 ) ) ;
#10408=DIRECTION ( 'NONE',  ( 1.000000000000000000, 0.000000000000000000, 0.000000000000000000 ) ) ;
#10410=CARTESIAN_POINT ( 'NONE',  ( 0.000000000000000000, 0.000000000000000000, 0.000000000000000000 ) ) ;
#10440=ORIENTED_EDGE ( 'NONE', *, *, #42513, .F. ) ;
#10441=DIRECTION ( 'NONE',  ( -1.000000000000000000, 0.000000000000000000, -0.000000000000000000 ) ) ;
#10452=FACE_OUTER_BOUND ( 'NONE', #22399, .T. ) ;
#10455=FACE_OUTER_BOUND ( 'NONE', #19687, .T. ) ;
#10461=CARTESIAN_POINT ( 'NONE',  ( 0.000000000000000000, -58.39081064771787766, 50.95692526931307498 ) ) ;
#10462=DIRECTION ( 'NONE',  ( 0.000000000000000000, 0.000000000000000000, 1.000000000000000000 ) ) ;
#10464=CARTESIAN_POINT ( 'NONE',  ( 0.000000000000000000, 15.33399622253600292, -80.55351364060572905 ) ) ;
#10467=EDGE_CURVE ( 'NONE', #59483, #808, #61171, .T. ) ;
#10469=VERTEX_POINT ( 'NONE', #9733 ) ;
#10479=CARTESIAN_POINT ( 'NONE',  ( 5.000000000000002665, -81.90746397400386059, -3.894527615418773347 ) ) ;
#10483=CARTESIAN_POINT ( 'NONE',  ( 0.000000000000000000, -35.91791733033426226, -68.67312586195033930 ) ) ;
#10485=CARTESIAN_POINT ( 'NONE',  ( 0.000000000000000000, 8.966570791701863996, -81.50828551894218776 ) ) ;
#10487=VECTOR ( 'NONE', #23909, 1000.000000000000000 ) ;
#10492=CARTESIAN_POINT ( 'NONE',  ( 0.000000000000000000, 44.99326035066149387, -68.55367621811095091 ) ) ;
#10497=CARTESIAN_POINT ( 'NONE',  ( 0.000000000000000000, 26.01480285779837232, 70.53064760720326376 ) ) ;
#10499=CARTESIAN_POINT ( 'NONE',  ( 10.00000000000000000, 0.000000000000000000, 0.000000000000000000 ) ) ;
#10505=FACE_OUTER_BOUND ( 'NONE', #2383, .T. ) ;
#10506=CARTESIAN_POINT ( 'NONE',  ( 0.000000000000000000, 0.000000000000000000, 0.000000000000000000 ) ) ;
#10515=ORIENTED_EDGE ( 'NONE', *, *, #38709, .T. ) ;
#10525=ORIENTED_EDGE ( 'NONE', *, *, #38648, .F. ) ;
#10527=CIRCLE ( 'NONE', #23734, 31.99999999999999645 ) ;
#10537=CARTESIAN_POINT ( 'NONE',  ( 0.000000000000000000, 49.70050353004889132, 59.46389618801982380 ) ) ;
#10541=ORIENTED_EDGE ( 'NONE', *, *, #58817, .T. ) ;
#10544=FACE_OUTER_BOUND ( 'NONE', #48101, .T. ) ;
#10550=FACE_OUTER_BOUND ( 'NONE', #6466, .T. ) ;
#10558=EDGE_LOOP ( 'NONE', ( #58522, #5648, #21809, #44942 ) ) ;
#10562=DIRECTION ( 'NONE',  ( 0.000000000000000000, -0.1564344650402170744, -0.9876883405951399908 ) ) ;
#10565=CARTESIAN_POINT ( 'NONE',  ( 5.000000000000000000, 81.96053171279902472, 2.543863470248670211 ) ) ;
#10572=CARTESIAN_POINT ( 'NONE',  ( 10.00000000000000000, 69.42325613327489009, -34.44570377933524696 ) ) ;
#10573=DIRECTION ( 'NONE',  ( -1.000000000000000000, 0.000000000000000000, 0.000000000000000000 ) ) ;
#10580=EDGE_CURVE ( 'NONE', #56916, #62512, #37172, .T. ) ;
#10591=ORIENTED_EDGE ( 'NONE', *, *, #60851, .T. ) ;
#10600=UNCERTAINTY_MEASURE_WITH_UNIT (LENGTH_MEASURE( 1.000000000000000082E-05 ), #795, 'distance_accuracy_value', 'NONE');
#10602=CIRCLE ( 'NONE', #59832, 32.00000000000000000 ) ;
#10603=DIRECTION ( 'NONE',  ( -1.000000000000000000, -0.000000000000000000, 0.000000000000000000 ) ) ;
#10604=VERTEX_POINT ( 'NONE', #27382 ) ;
#10605=AXIS2_PLACEMENT_3D ( 'NONE', #42875, #67560, #31572 ) ;
#10613=ORIENTED_EDGE ( 'NONE', *, *, #48656, .T. ) ;
#10616=CARTESIAN_POINT ( 'NONE',  ( 10.00000000000000000, -77.16300072079640415, -27.74655509720751567 ) ) ;
#10619=ORIENTED_EDGE ( 'NONE', *, *, #45855, .F. ) ;
#10622=CARTESIAN_POINT ( 'NONE',  ( -10.00000000000000000, 0.000000000000000000, 0.000000000000000000 ) ) ;
#10623=EDGE_CURVE ( 'NONE', #21187, #5866, #29968, .T. ) ;
#10625=EDGE_CURVE ( 'NONE', #15472, #34053, #40775, .T. ) ;
#10637=ORIENTED_EDGE ( 'NONE', *, *, #11530, .F. ) ;
#10646=DIRECTION ( 'NONE',  ( 0.000000000000000000, 0.1564344650402244852, 0.9876883405951387696 ) ) ;
#10655=DIRECTION ( 'NONE',  ( -1.000000000000000000, -0.000000000000000000, -0.000000000000000000 ) ) ;
#10666=AXIS2_PLACEMENT_3D ( 'NONE', #10156, #33080, #56021 ) ;
#10674=EDGE_CURVE ( 'NONE', #1522, #6553, #32279, .T. ) ;
#10683=DIRECTION ( 'NONE',  ( 0.000000000000000000, 1.000000000000000000, 3.469446951953614978E-15 ) ) ;
#10701=AXIS2_PLACEMENT_3D ( 'NONE', #6727, #18366, #41673 ) ;
#10719=AXIS2_PLACEMENT_3D ( 'NONE', #31879, #54823, #3348 ) ;
#10725=DIRECTION ( 'NONE',  ( 0.000000000000000000, 0.000000000000000000, 1.000000000000000000 ) ) ;
#10726=DIRECTION ( 'NONE',  ( -1.000000000000000000, 0.000000000000000000, 0.000000000000000000 ) ) ;
#10732=VERTEX_POINT ( 'NONE', #17602 ) ;
#10738=CYLINDRICAL_SURFACE ( 'NONE', #58232, 82.00000000000000000 ) ;
#10741=ORIENTED_EDGE ( 'NONE', *, *, #37441, .T. ) ;
#10743=ORIENTED_EDGE ( 'NONE', *, *, #68856, .T. ) ;
#10748=ORIENTED_EDGE ( 'NONE', *, *, #38950, .F. ) ;
#10754=DIRECTION ( 'NONE',  ( -1.000000000000000000, -0.000000000000000000, 0.000000000000000000 ) ) ;
#10755=CIRCLE ( 'NONE', #26354, 77.49899999999999523 ) ;
#10765=CARTESIAN_POINT ( 'NONE',  ( -10.00000000000000000, 0.000000000000000000, 0.000000000000000000 ) ) ;
#10770=ORIENTED_EDGE ( 'NONE', *, *, #52710, .F. ) ;
#10771=EDGE_CURVE ( 'NONE', #50470, #16727, #6339, .T. ) ;
#10772=CARTESIAN_POINT ( 'NONE',  ( 0.000000000000000000, -56.15606465354917276, -59.75363087400133111 ) ) ;
#10778=CARTESIAN_POINT ( 'NONE',  ( 10.00000000000000000, -31.47745569255189224, 68.26794271651249346 ) ) ;
#10785=AXIS2_PLACEMENT_3D ( 'NONE', #27330, #16068, #39374 ) ;
#10788=LINE ( 'NONE', #27701, #53965 ) ;
#10790=CARTESIAN_POINT ( 'NONE',  ( 10.00000000000000000, -2.956366410620109519, -75.11725578898472122 ) ) ;
#10793=ORIENTED_EDGE ( 'NONE', *, *, #33362, .T. ) ;
#10794=DIRECTION ( 'NONE',  ( -1.000000000000000000, -0.000000000000000000, -0.000000000000000000 ) ) ;
#10817=LINE ( 'NONE', #33354, #68140 ) ;
#10819=AXIS2_PLACEMENT_3D ( 'NONE', #11495, #73162, #16404 ) ;
#10829=VECTOR ( 'NONE', #40317, 1000.000000000000000 ) ;
#10839=CARTESIAN_POINT ( 'NONE',  ( 5.000000000000002665, -44.99326035066006568, -68.55367621811190304 ) ) ;
#10842=VERTEX_POINT ( 'NONE', #19438 ) ;
#10847=ORIENTED_EDGE ( 'NONE', *, *, #57358, .F. ) ;
#10850=ORIENTED_EDGE ( 'NONE', *, *, #62916, .F. ) ;
#10851=ORIENTED_EDGE ( 'NONE', *, *, #35256, .F. ) ;
#10862=DIRECTION ( 'NONE',  ( -1.000000000000000000, -0.000000000000000000, -0.000000000000000000 ) ) ;
#10868=EDGE_CURVE ( 'NONE', #2983, #63033, #24355, .T. ) ;
#10869=CARTESIAN_POINT ( 'NONE',  ( 10.00000000000000000, 0.000000000000000000, 0.000000000000000000 ) ) ;
#10875=CARTESIAN_POINT ( 'NONE',  ( 10.00000000000000000, 0.000000000000000000, 0.000000000000000000 ) ) ;
#10882=DIRECTION ( 'NONE',  ( -1.000000000000000000, 0.000000000000000000, 0.000000000000000000 ) ) ;
#10884=DIRECTION ( 'NONE',  ( 0.000000000000000000, 0.8526401643540897357, 0.5224985647159527957 ) ) ;
#10889=AXIS2_PLACEMENT_3D ( 'NONE', #31315, #37716, #42246 ) ;
#10897=FACE_OUTER_BOUND ( 'NONE', #37920, .T. ) ;
#10904=ORIENTED_EDGE ( 'NONE', *, *, #64352, .F. ) ;
#10907=ORIENTED_EDGE ( 'NONE', *, *, #25227, .T. ) ;
#10912=CIRCLE ( 'NONE', #64966, 77.49900000000000944 ) ;
#10916=VERTEX_POINT ( 'NONE', #69834 ) ;
#10940=EDGE_LOOP ( 'NONE', ( #44216, #2007, #60032, #65884 ) ) ;
#10944=DIRECTION ( 'NONE',  ( -1.000000000000000000, 0.000000000000000000, 0.000000000000000000 ) ) ;
#10956=CARTESIAN_POINT ( 'NONE',  ( 0.000000000000000000, 75.11764819372149304, -2.946379043146603482 ) ) ;
#10960=DIRECTION ( 'NONE',  ( 0.000000000000000000, 0.000000000000000000, -1.000000000000000000 ) ) ;
#10962=VERTEX_POINT ( 'NONE', #14544 ) ;
#10964=VECTOR ( 'NONE', #71979, 1000.000000000000000 ) ;
#10968=LINE ( 'NONE', #27505, #29752 ) ;
#10969=CARTESIAN_POINT ( 'NONE',  ( 10.00000000000000000, 59.03961581697399907, 46.53671651293969802 ) ) ;
#10974=CYLINDRICAL_SURFACE ( 'NONE', #26048, 32.00000000000000000 ) ;
#10983=VECTOR ( 'NONE', #16681, 1000.000000000000000 ) ;
#10985=CIRCLE ( 'NONE', #42237, 31.99999999999999289 ) ;
#11004=ORIENTED_EDGE ( 'NONE', *, *, #40605, .T. ) ;
#11015=ORIENTED_EDGE ( 'NONE', *, *, #56100, .T. ) ;
#11018=CARTESIAN_POINT ( 'NONE',  ( 10.00000000000000000, 76.66974797899852945, -11.30684508768257679 ) ) ;
#11024=DIRECTION ( 'NONE',  ( 0.000000000000000000, 0.000000000000000000, -1.000000000000000000 ) ) ;
#11027=ADVANCED_FACE ( 'NONE', ( #67164 ), #4034, .T. ) ;
#11030=ORIENTED_EDGE ( 'NONE', *, *, #1604, .T. ) ;
#11041=CARTESIAN_POINT ( 'NONE',  ( 0.000000000000000000, -16.65972982744877484, -80.28980883073775487 ) ) ;
#11045=DIRECTION ( 'NONE',  ( -1.000000000000000000, 0.000000000000000000, 0.000000000000000000 ) ) ;
#11065=CARTESIAN_POINT ( 'NONE',  ( 10.00000000000000000, -36.72794159290288718, 65.59268652807197952 ) ) ;
#11066=CARTESIAN_POINT ( 'NONE',  ( 10.00000000000000000, 0.000000000000000000, 0.000000000000000000 ) ) ;
#11073=ORIENTED_EDGE ( 'NONE', *, *, #66153, .F. ) ;
#11074=CARTESIAN_POINT ( 'NONE',  ( 10.00000000000000000, 0.000000000000000000, 0.000000000000000000 ) ) ;
#11075=AXIS2_PLACEMENT_3D ( 'NONE', #44330, #73625, #54860 ) ;
#11076=DIRECTION ( 'NONE',  ( -1.000000000000000000, 0.000000000000000000, -0.000000000000000000 ) ) ;
#11082=CIRCLE ( 'NONE', #5143, 77.49900000000000944 ) ;
#11085=CYLINDRICAL_SURFACE ( 'NONE', #32726, 31.99999999999999289 ) ;
#11095=ADVANCED_FACE ( 'NONE', ( #65690 ), #2931, .T. ) ;
#11108=CYLINDRICAL_SURFACE ( 'NONE', #49797, 31.99999999999999289 ) ;
#11111=DIRECTION ( 'NONE',  ( 0.000000000000000000, 0.000000000000000000, -1.000000000000000000 ) ) ;
#11119=VERTEX_POINT ( 'NONE', #43873 ) ;
#11128=ORIENTED_EDGE ( 'NONE', *, *, #35867, .T. ) ;
#11130=LINE ( 'NONE', #57005, #26532 ) ;
#11136=CIRCLE ( 'NONE', #37535, 77.49900000000000944 ) ;
#11138=ADVANCED_FACE ( 'NONE', ( #274 ), #34063, .T. ) ;
#11152=DIRECTION ( 'NONE',  ( 0.000000000000000000, 0.000000000000000000, 1.000000000000000000 ) ) ;
#11155=CARTESIAN_POINT ( 'NONE',  ( 5.000000000000000000, -56.15606465355001120, 59.75363087400055662 ) ) ;
#11156=CARTESIAN_POINT ( 'NONE',  ( 0.000000000000000000, 36.73666225445988687, -65.58780272294035285 ) ) ;
#11164=CYLINDRICAL_SURFACE ( 'NONE', #62893, 82.00000000000000000 ) ;
#11168=DIRECTION ( 'NONE',  ( 0.000000000000000000, 0.000000000000000000, 1.000000000000000000 ) ) ;
#11190=ORIENTED_EDGE ( 'NONE', *, *, #42465, .T. ) ;
#11194=CARTESIAN_POINT ( 'NONE',  ( 10.00000000000000000, 0.000000000000000000, 0.000000000000000000 ) ) ;
#11202=DIRECTION ( 'NONE',  ( 0.000000000000000000, 0.3826834323650905589, -0.9238795325112864054 ) ) ;
#11213=ORIENTED_EDGE ( 'NONE', *, *, #56716, .F. ) ;
#11217=VERTEX_POINT ( 'NONE', #44619 ) ;
#11225=FACE_OUTER_BOUND ( 'NONE', #5378, .T. ) ;
#11246=DIRECTION ( 'NONE',  ( 0.000000000000000000, 0.3090169943749480619, -0.9510565162951533091 ) ) ;
#11264=CARTESIAN_POINT ( 'NONE',  ( 10.00000000000000000, 44.99326035066149387, -68.55367621811095091 ) ) ;
#11268=ORIENTED_EDGE ( 'NONE', *, *, #61396, .T. ) ;
#11272=ORIENTED_EDGE ( 'NONE', *, *, #49544, .F. ) ;
#11273=ORIENTED_EDGE ( 'NONE', *, *, #63346, .F. ) ;
#11275=EDGE_CURVE ( 'NONE', #31341, #8511, #54078, .T. ) ;
#11285=ADVANCED_FACE ( 'NONE', ( #71496 ), #34810, .T. ) ;
#11299=EDGE_CURVE ( 'NONE', #71089, #73769, #42217, .T. ) ;
#11302=EDGE_LOOP ( 'NONE', ( #11814, #57626, #42635, #43381 ) ) ;
#11309=CARTESIAN_POINT ( 'NONE',  ( -10.00000000000000000, 0.000000000000000000, 0.000000000000000000 ) ) ;
#11322=LINE ( 'NONE', #51549, #14600 ) ;
#11327=AXIS2_PLACEMENT_3D ( 'NONE', #20983, #60487, #49187 ) ;
#11343=LINE ( 'NONE', #125, #31214 ) ;
#11347=EDGE_CURVE ( 'NONE', #38625, #71349, #6070, .T. ) ;
#11365=DIRECTION ( 'NONE',  ( 0.000000000000000000, 0.000000000000000000, 1.000000000000000000 ) ) ;
#11367=ORIENTED_EDGE ( 'NONE', *, *, #28083, .T. ) ;
#11368=EDGE_LOOP ( 'NONE', ( #17884, #53164, #13834, #73111 ) ) ;
#11373=ORIENTED_EDGE ( 'NONE', *, *, #14407, .F. ) ;
#11405=VERTEX_POINT ( 'NONE', #57748 ) ;
#11411=CARTESIAN_POINT ( 'NONE',  ( 0.000000000000000000, -27.74655509720725988, 77.16300072079653205 ) ) ;
#11413=CARTESIAN_POINT ( 'NONE',  ( 10.00000000000000000, 20.40083707022987625, -72.35432306680462489 ) ) ;
#11430=CARTESIAN_POINT ( 'NONE',  ( 0.000000000000000000, 0.000000000000000000, 0.000000000000000000 ) ) ;
#11431=DIRECTION ( 'NONE',  ( -1.000000000000000000, 0.000000000000000000, 0.000000000000000000 ) ) ;
#11433=AXIS2_PLACEMENT_3D ( 'NONE', #31714, #2823, #49008 ) ;
#11441=AXIS2_PLACEMENT_3D ( 'NONE', #43874, #66796, #15285 ) ;
#11443=CIRCLE ( 'NONE', #45057, 82.00000000000000000 ) ;
#11452=DIRECTION ( 'NONE',  ( -1.000000000000000000, 0.000000000000000000, -0.000000000000000000 ) ) ;
#11461=ORIENTED_EDGE ( 'NONE', *, *, #48718, .F. ) ;
#11478=ADVANCED_FACE ( 'NONE', ( #20746 ), #27110, .T. ) ;
#11495=CARTESIAN_POINT ( 'NONE',  ( -10.00000000000000000, 0.000000000000000000, 0.000000000000000000 ) ) ;
#11506=CARTESIAN_POINT ( 'NONE',  ( 10.00000000000000000, 0.000000000000000000, 0.000000000000000000 ) ) ;
#11513=CARTESIAN_POINT ( 'NONE',  ( 10.00000000000000000, 55.38113227695858143, -54.21277698773617715 ) ) ;
#11520=EDGE_CURVE ( 'NONE', #40918, #30770, #73276, .T. ) ;
#11524=CARTESIAN_POINT ( 'NONE',  ( 0.000000000000000000, 0.000000000000000000, 0.000000000000000000 ) ) ;
#11530=EDGE_CURVE ( 'NONE', #8427, #21255, #20485, .T. ) ;
#11545=ORIENTED_EDGE ( 'NONE', *, *, #32759, .F. ) ;
#11546=VERTEX_POINT ( 'NONE', #61353 ) ;
#11547=ORIENTED_EDGE ( 'NONE', *, *, #60377, .T. ) ;
#11550=DIRECTION ( 'NONE',  ( -1.000000000000000000, -0.000000000000000000, -0.000000000000000000 ) ) ;
#11557=VERTEX_POINT ( 'NONE', #72241 ) ;
#11559=DIRECTION ( 'NONE',  ( -1.000000000000000000, 0.000000000000000000, 0.000000000000000000 ) ) ;
#11566=CARTESIAN_POINT ( 'NONE',  ( 0.000000000000000000, 76.41127070299273782, 12.93880638057342836 ) ) ;
#11568=DIRECTION ( 'NONE',  ( 0.000000000000000000, -0.9723699203976789995, 0.2334453638558956767 ) ) ;
#11569=CARTESIAN_POINT ( 'NONE',  ( 0.000000000000000000, -34.94270380257693631, 74.18225833017875459 ) ) ;
#11571=LINE ( 'NONE', #29589, #37497 ) ;
#11583=LINE ( 'NONE', #17243, #74062 ) ;
#11585=ORIENTED_EDGE ( 'NONE', *, *, #73993, .T. ) ;
#11589=LINE ( 'NONE', #34168, #12361 ) ;
#11596=CIRCLE ( 'NONE', #33163, 12.50000000000000000 ) ;
#11604=AXIS2_PLACEMENT_3D ( 'NONE', #10778, #10402, #57382 ) ;
#11611=DIRECTION ( 'NONE',  ( 0.000000000000000000, 0.000000000000000000, 1.000000000000000000 ) ) ;
#11612=EDGE_CURVE ( 'NONE', #43494, #1463, #36031, .T. ) ;
#11615=CIRCLE ( 'NONE', #38081, 32.00000000000000000 ) ;
#11648=VERTEX_POINT ( 'NONE', #6436 ) ;
#11652=ORIENTED_EDGE ( 'NONE', *, *, #57732, .F. ) ;
#11653=VECTOR ( 'NONE', #57559, 1000.000000000000000 ) ;
#11668=DIRECTION ( 'NONE',  ( -1.000000000000000000, 0.000000000000000000, 0.000000000000000000 ) ) ;
#11677=DIRECTION ( 'NONE',  ( -1.000000000000000000, 0.000000000000000000, -0.000000000000000000 ) ) ;
#11697=DIRECTION ( 'NONE',  ( -1.000000000000000000, -0.000000000000000000, 0.000000000000000000 ) ) ;
#11698=DIRECTION ( 'NONE',  ( 1.000000000000000000, 0.000000000000000000, 0.000000000000000000 ) ) ;
#11711=EDGE_LOOP ( 'NONE', ( #67859, #51492, #37051, #59385 ) ) ;
#11714=CYLINDRICAL_SURFACE ( 'NONE', #59898, 32.00000000000000000 ) ;
#11718=CARTESIAN_POINT ( 'NONE',  ( 10.00000000000000000, 0.000000000000000000, 0.000000000000000000 ) ) ;
#11720=ORIENTED_EDGE ( 'NONE', *, *, #73856, .F. ) ;
#11722=VERTEX_POINT ( 'NONE', #47387 ) ;
#11725=VECTOR ( 'NONE', #14742, 1000.000000000000000 ) ;
#11726=ORIENTED_EDGE ( 'NONE', *, *, #72901, .F. ) ;
#11731=ORIENTED_EDGE ( 'NONE', *, *, #34449, .T. ) ;
#11744=VERTEX_POINT ( 'NONE', #7533 ) ;
#11750=DIRECTION ( 'NONE',  ( 1.000000000000000000, 0.000000000000000000, 0.000000000000000000 ) ) ;
#11754=CIRCLE ( 'NONE', #25016, 77.49899999999999523 ) ;
#11755=CARTESIAN_POINT ( 'NONE',  ( 0.000000000000000000, 8.830959090343430518, -74.65491531819107252 ) ) ;
#11761=AXIS2_PLACEMENT_3D ( 'NONE', #23367, #6089, #40280 ) ;
#11765=CYLINDRICAL_SURFACE ( 'NONE', #33776, 82.00000000000000000 ) ;
#11773=EDGE_CURVE ( 'NONE', #15290, #39348, #13891, .T. ) ;
#11780=CARTESIAN_POINT ( 'NONE',  ( 0.000000000000000000, 40.65526001592713357, -71.21200624218752750 ) ) ;
#11784=ADVANCED_FACE ( 'NONE', ( #42856 ), #71404, .T. ) ;
#11803=CIRCLE ( 'NONE', #3472, 77.49899999999999523 ) ;
#11810=AXIS2_PLACEMENT_3D ( 'NONE', #63786, #50628, #12261 ) ;
#11811=VERTEX_POINT ( 'NONE', #42124 ) ;
#11814=ORIENTED_EDGE ( 'NONE', *, *, #12912, .F. ) ;
#11833=VERTEX_POINT ( 'NONE', #44337 ) ;
#11864=AXIS2_PLACEMENT_3D ( 'NONE', #38713, #4516, #27414 ) ;
#11866=DIRECTION ( 'NONE',  ( -1.000000000000000000, -0.000000000000000000, -0.000000000000000000 ) ) ;
#11885=ORIENTED_EDGE ( 'NONE', *, *, #36425, .T. ) ;
#11889=AXIS2_PLACEMENT_3D ( 'NONE', #24061, #48088, #70255 ) ;
#11890=AXIS2_PLACEMENT_3D ( 'NONE', #8960, #72830, #21332 ) ;
#11892=DIRECTION ( 'NONE',  ( 0.000000000000000000, 0.000000000000000000, 1.000000000000000000 ) ) ;
#11903=DIRECTION ( 'NONE',  ( -1.000000000000000000, 0.000000000000000000, 0.000000000000000000 ) ) ;
#11905=ORIENTED_EDGE ( 'NONE', *, *, #41117, .F. ) ;
#11906=VECTOR ( 'NONE', #48921, 1000.000000000000000 ) ;
#11917=VECTOR ( 'NONE', #2009, 1000.000000000000000 ) ;
#11928=VERTEX_POINT ( 'NONE', #14642 ) ;
#11930=EDGE_CURVE ( 'NONE', #57622, #6059, #25313, .T. ) ;
#11931=VERTEX_POINT ( 'NONE', #10485 ) ;
#11933=ORIENTED_EDGE ( 'NONE', *, *, #60017, .F. ) ;
#11960=DIRECTION ( 'NONE',  ( -1.000000000000000000, 0.000000000000000000, 0.000000000000000000 ) ) ;
#11971=CARTESIAN_POINT ( 'NONE',  ( 10.00000000000000000, 20.40083707022882820, 72.35432306680490910 ) ) ;
#11974=DIRECTION ( 'NONE',  ( 0.000000000000000000, 0.000000000000000000, 1.000000000000000000 ) ) ;
#11976=CYLINDRICAL_SURFACE ( 'NONE', #47090, 82.00000000000000000 ) ;
#11977=CIRCLE ( 'NONE', #63621, 77.49899999999999523 ) ;
#12000=ORIENTED_EDGE ( 'NONE', *, *, #6199, .F. ) ;
#12010=VERTEX_POINT ( 'NONE', #69484 ) ;
#12011=CARTESIAN_POINT ( 'NONE',  ( 5.000000000000000000, -64.81221759200306565, -50.23322058963418613 ) ) ;
#12022=ORIENTED_EDGE ( 'NONE', *, *, #8196, .F. ) ;
#12023=LINE ( 'NONE', #57166, #43316 ) ;
#12028=FILL_AREA_STYLE ('',( #57907 ) ) ;
#12032=VERTEX_POINT ( 'NONE', #5613 ) ;
#12035=AXIS2_PLACEMENT_3D ( 'NONE', #37224, #7167, #19540 ) ;
#12046=ORIENTED_EDGE ( 'NONE', *, *, #46857, .T. ) ;
#12053=EDGE_CURVE ( 'NONE', #15157, #8951, #45776, .T. ) ;
#12055=CARTESIAN_POINT ( 'NONE',  ( 10.00000000000000000, 58.39081064771751528, 50.95692526931350841 ) ) ;
#12058=CARTESIAN_POINT ( 'NONE',  ( 0.000000000000000000, 59.03961581697399907, 46.53671651293969802 ) ) ;
#12065=CARTESIAN_POINT ( 'NONE',  ( 0.000000000000000000, 44.99326035066051332, 68.55367621811160461 ) ) ;
#12070=ADVANCED_FACE ( 'NONE', ( #36008 ), #41645, .T. ) ;
#12084=LINE ( 'NONE', #69958, #58140 ) ;
#12088=ORIENTED_EDGE ( 'NONE', *, *, #9953, .F. ) ;
#12096=ORIENTED_EDGE ( 'NONE', *, *, #59610, .F. ) ;
#12097=DIRECTION ( 'NONE',  ( -1.000000000000000000, -0.000000000000000000, -0.000000000000000000 ) ) ;
#12110=DIRECTION ( 'NONE',  ( -1.000000000000000000, -0.000000000000000000, 0.000000000000000000 ) ) ;
#12115=ORIENTED_EDGE ( 'NONE', *, *, #26545, .F. ) ;
#12118=DIRECTION ( 'NONE',  ( 0.000000000000000000, 0.000000000000000000, 1.000000000000000000 ) ) ;
#12122=DIRECTION ( 'NONE',  ( -1.000000000000000000, -0.000000000000000000, -0.000000000000000000 ) ) ;
#12131=DIRECTION ( 'NONE',  ( 1.000000000000000000, 0.000000000000000000, 0.000000000000000000 ) ) ;
#12174=DIRECTION ( 'NONE',  ( 0.000000000000000000, 0.000000000000000000, 1.000000000000000000 ) ) ;
#12181=FACE_OUTER_BOUND ( 'NONE', #4097, .T. ) ;
#12185=AXIS2_PLACEMENT_3D ( 'NONE', #24369, #13073, #25103 ) ;
#12188=ORIENTED_EDGE ( 'NONE', *, *, #29684, .T. ) ;
#12190=CARTESIAN_POINT ( 'NONE',  ( 10.00000000000000000, 0.000000000000000000, 0.000000000000000000 ) ) ;
#12196=EDGE_LOOP ( 'NONE', ( #12644, #52800, #48430, #32386 ) ) ;
#12202=AXIS2_PLACEMENT_3D ( 'NONE', #18071, #74093, #57929 ) ;
#12206=DIRECTION ( 'NONE',  ( 0.000000000000000000, -0.8090169943749402348, -0.5877852522924830181 ) ) ;
#12208=LINE ( 'NONE', #34779, #6362 ) ;
#12210=AXIS2_PLACEMENT_3D ( 'NONE', #52020, #56578, #68961 ) ;
#12214=EDGE_CURVE ( 'NONE', #11744, #1159, #59751, .T. ) ;
#12222=ADVANCED_FACE ( 'NONE', ( #37505 ), #14927, .T. ) ;
#12231=DIRECTION ( 'NONE',  ( 0.000000000000000000, 0.000000000000000000, 1.000000000000000000 ) ) ;
#12232=CARTESIAN_POINT ( 'NONE',  ( -10.00000000000000000, 0.000000000000000000, 0.000000000000000000 ) ) ;
#12233=ORIENTED_EDGE ( 'NONE', *, *, #39839, .F. ) ;
#12234=ORIENTED_EDGE ( 'NONE', *, *, #18906, .F. ) ;
#12236=ADVANCED_FACE ( 'NONE', ( #9283 ), #25835, .T. ) ;
#12240=DIRECTION ( 'NONE',  ( -1.000000000000000000, 0.000000000000000000, 0.000000000000000000 ) ) ;
#12242=CIRCLE ( 'NONE', #47080, 82.00000000000000000 ) ;
#12244=AXIS2_PLACEMENT_3D ( 'NONE', #32660, #72865, #55229 ) ;
#12252=DIRECTION ( 'NONE',  ( 0.000000000000000000, 0.000000000000000000, 1.000000000000000000 ) ) ;
#12254=CARTESIAN_POINT ( 'NONE',  ( 5.000000000000000000, 81.96053171279902472, -2.543863470248670211 ) ) ;
#12261=DIRECTION ( 'NONE',  ( 0.000000000000000000, 0.000000000000000000, 1.000000000000000000 ) ) ;
#12267=AXIS2_PLACEMENT_3D ( 'NONE', #39323, #50586, #5495 ) ;
#12275=EDGE_LOOP ( 'NONE', ( #755, #19788, #41213, #62907 ) ) ;
#12283=CARTESIAN_POINT ( 'NONE',  ( 0.000000000000000000, -22.90783923731686045, 78.73519480814945837 ) ) ;
#12288=ORIENTED_EDGE ( 'NONE', *, *, #41402, .F. ) ;
#12308=ADVANCED_FACE ( 'NONE', ( #44631 ), #73918, .T. ) ;
#12321=ORIENTED_EDGE ( 'NONE', *, *, #35555, .F. ) ;
#12327=DIRECTION ( 'NONE',  ( -1.000000000000000000, 0.000000000000000000, 0.000000000000000000 ) ) ;
#12331=DIRECTION ( 'NONE',  ( 1.000000000000000000, 0.000000000000000000, -0.000000000000000000 ) ) ;
#12333=EDGE_LOOP ( 'NONE', ( #28636, #35490, #11547, #71538 ) ) ;
#12334=ORIENTED_EDGE ( 'NONE', *, *, #73461, .F. ) ;
#12339=DIRECTION ( 'NONE',  ( 0.000000000000000000, -0.6494480483301739993, -0.7604059656000392575 ) ) ;
#12344=DIRECTION ( 'NONE',  ( 0.000000000000000000, 0.9969173337331276308, 0.07845909572784873220 ) ) ;
#12356=CARTESIAN_POINT ( 'NONE',  ( 0.000000000000000000, -12.93880638057258814, -76.41127070299285151 ) ) ;
#12361=VECTOR ( 'NONE', #57112, 1000.000000000000000 ) ;
#12363=ORIENTED_EDGE ( 'NONE', *, *, #57797, .T. ) ;
#12414=EDGE_LOOP ( 'NONE', ( #55218, #7510, #59284, #28388 ) ) ;
#12415=EDGE_CURVE ( 'NONE', #39808, #19228, #39353, .T. ) ;
#12433=CARTESIAN_POINT ( 'NONE',  ( 10.00000000000000000, 75.16055320797030959, 18.89407956138283851 ) ) ;
#12434=AXIS2_PLACEMENT_3D ( 'NONE', #18497, #51974, #69273 ) ;
#12442=ORIENTED_EDGE ( 'NONE', *, *, #43340, .T. ) ;
#12478=EDGE_CURVE ( 'NONE', #65118, #21621, #11754, .T. ) ;
#12483=AXIS2_PLACEMENT_3D ( 'NONE', #53927, #26816, #26452 ) ;
#12492=FACE_OUTER_BOUND ( 'NONE', #73046, .T. ) ;
#12493=CARTESIAN_POINT ( 'NONE',  ( 0.000000000000000000, -14.66109333815410487, -73.73191006444587003 ) ) ;
#12501=ORIENTED_EDGE ( 'NONE', *, *, #28930, .T. ) ;
#12502=DIRECTION ( 'NONE',  ( 0.000000000000000000, 0.000000000000000000, -1.000000000000000000 ) ) ;
#12527=CIRCLE ( 'NONE', #71327, 82.00000000000000000 ) ;
#12529=CARTESIAN_POINT ( 'NONE',  ( 0.000000000000000000, 0.000000000000000000, 0.000000000000000000 ) ) ;
#12530=DIRECTION ( 'NONE',  ( 0.000000000000000000, 0.9510565162951523099, 0.3090169943749515591 ) ) ;
#12554=CARTESIAN_POINT ( 'NONE',  ( -10.00000000000000000, 0.000000000000000000, 0.000000000000000000 ) ) ;
#12557=EDGE_CURVE ( 'NONE', #69079, #38213, #24643, .T. ) ;
#12562=ORIENTED_EDGE ( 'NONE', *, *, #21288, .F. ) ;
#12570=AXIS2_PLACEMENT_3D ( 'NONE', #72663, #44869, #56523 ) ;
#12572=ORIENTED_EDGE ( 'NONE', *, *, #71960, .T. ) ;
#12574=EDGE_LOOP ( 'NONE', ( #28641, #39861, #16083, #61858 ) ) ;
#12575=CARTESIAN_POINT ( 'NONE',  ( 10.00000000000000000, 55.20638768913760686, 51.02545421589343988 ) ) ;
#12585=DIRECTION ( 'NONE',  ( 0.000000000000000000, -0.2334453638559125521, 0.9723699203976750027 ) ) ;
#12591=ORIENTED_EDGE ( 'NONE', *, *, #72027, .F. ) ;
#12605=FACE_OUTER_BOUND ( 'NONE', #27076, .T. ) ;
#12625=CARTESIAN_POINT ( 'NONE',  ( 10.00000000000000000, -71.27951684758046724, 30.41916302227088309 ) ) ;
#12644=ORIENTED_EDGE ( 'NONE', *, *, #18438, .T. ) ;
#12647=CARTESIAN_POINT ( 'NONE',  ( 10.00000000000000000, 71.21200624218852226, -40.65526001592539984 ) ) ;
#12648=DIRECTION ( 'NONE',  ( 0.000000000000000000, 0.2334453638558990629, 0.9723699203976782224 ) ) ;
#12650=CARTESIAN_POINT ( 'NONE',  ( 10.00000000000000000, -58.39081064771713869, -50.95692526931392052 ) ) ;
#12655=ORIENTED_EDGE ( 'NONE', *, *, #56282, .F. ) ;
#12663=DIRECTION ( 'NONE',  ( -1.000000000000000000, 0.000000000000000000, 0.000000000000000000 ) ) ;
#12667=ORIENTED_EDGE ( 'NONE', *, *, #59580, .F. ) ;
#12682=CIRCLE ( 'NONE', #36725, 77.49900000000000944 ) ;
#12686=AXIS2_PLACEMENT_3D ( 'NONE', #66805, #33310, #38979 ) ;
#12687=CARTESIAN_POINT ( 'NONE',  ( 0.000000000000000000, 81.96053171279902472, 2.543863470248670211 ) ) ;
#12698=LINE ( 'NONE', #13068, #28247 ) ;
#12704=DIRECTION ( 'NONE',  ( -1.000000000000000000, 0.000000000000000000, 0.000000000000000000 ) ) ;
#12706=CARTESIAN_POINT ( 'NONE',  ( 10.00000000000000000, 0.000000000000000000, 0.000000000000000000 ) ) ;
#12711=EDGE_CURVE ( 'NONE', #23922, #70598, #26192, .T. ) ;
#12714=CARTESIAN_POINT ( 'NONE',  ( 0.000000000000000000, 81.50828551894227303, 8.966570791700979370 ) ) ;
#12724=DIRECTION ( 'NONE',  ( -1.000000000000000000, 0.000000000000000000, 0.000000000000000000 ) ) ;
#12727=ORIENTED_EDGE ( 'NONE', *, *, #29965, .F. ) ;
#12740=EDGE_LOOP ( 'NONE', ( #66310, #37633, #28129, #52807 ) ) ;
#12749=ORIENTED_EDGE ( 'NONE', *, *, #971, .T. ) ;
#12756=ORIENTED_EDGE ( 'NONE', *, *, #18478, .T. ) ;
#12758=DIRECTION ( 'NONE',  ( 1.000000000000000000, -0.000000000000000000, 0.000000000000000000 ) ) ;
#12766=ORIENTED_EDGE ( 'NONE', *, *, #20017, .T. ) ;
#12767=VERTEX_POINT ( 'NONE', #16327 ) ;
#12774=CYLINDRICAL_SURFACE ( 'NONE', #15483, 31.99999999999999289 ) ;
#12780=DIRECTION ( 'NONE',  ( 0.000000000000000000, -0.8910065241883626808, -0.4539904997395568520 ) ) ;
#12781=CYLINDRICAL_SURFACE ( 'NONE', #3217, 77.49899999999999523 ) ;
#12783=CARTESIAN_POINT ( 'NONE',  ( 10.00000000000000000, -6.903761155838323837, 77.19088730480521576 ) ) ;
#12784=ADVANCED_FACE ( 'NONE', ( #45286 ), #61831, .T. ) ;
#12788=DIRECTION ( 'NONE',  ( 0.000000000000000000, -0.9969173337331287410, 0.07845909572783489605 ) ) ;
#12792=ADVANCED_FACE ( 'NONE', ( #4325 ), #27214, .T. ) ;
#12802=DIRECTION ( 'NONE',  ( -1.000000000000000000, 0.000000000000000000, -0.000000000000000000 ) ) ;
#12819=EDGE_CURVE ( 'NONE', #5506, #71442, #12989, .T. ) ;
#12820=CARTESIAN_POINT ( 'NONE',  ( 10.00000000000000000, -18.89407956138310496, 75.16055320797023853 ) ) ;
#12824=EDGE_CURVE ( 'NONE', #70724, #28823, #35849, .T. ) ;
#12826=ORIENTED_EDGE ( 'NONE', *, *, #29001, .F. ) ;
#12830=LINE ( 'NONE', #63630, #55089 ) ;
#12831=ORIENTED_EDGE ( 'NONE', *, *, #39826, .F. ) ;
#12833=ORIENTED_EDGE ( 'NONE', *, *, #15169, .F. ) ;
#12838=DIRECTION ( 'NONE',  ( -1.000000000000000000, -0.000000000000000000, -0.000000000000000000 ) ) ;
#12839=EDGE_LOOP ( 'NONE', ( #57346, #36186, #61389, #8153 ) ) ;
#12840=CARTESIAN_POINT ( 'NONE',  ( 10.00000000000000000, 12.93880638057314059, 76.41127070299278046 ) ) ;
#12842=CIRCLE ( 'NONE', #68083, 32.00000000000000000 ) ;
#12845=ORIENTED_EDGE ( 'NONE', *, *, #6887, .T. ) ;
#12850=PRODUCT_CONTEXT ( 'NONE', #52686, 'mechanical' ) ;
#12852=CARTESIAN_POINT ( 'NONE',  ( 10.00000000000000000, 0.000000000000000000, 0.000000000000000000 ) ) ;
#12869=DIRECTION ( 'NONE',  ( -1.000000000000000000, 0.000000000000000000, 0.000000000000000000 ) ) ;
#12888=AXIS2_PLACEMENT_3D ( 'NONE', #22580, #32721, #15070 ) ;
#12894=CARTESIAN_POINT ( 'NONE',  ( 10.00000000000000000, 28.89263327155746097, 71.91182617369197771 ) ) ;
#12904=ORIENTED_EDGE ( 'NONE', *, *, #60093, .T. ) ;
#12907=CIRCLE ( 'NONE', #71713, 77.49900000000000944 ) ;
#12912=EDGE_CURVE ( 'NONE', #7708, #7152, #42233, .T. ) ;
#12917=EDGE_LOOP ( 'NONE', ( #7646, #54638, #3950, #43540, #11545, #9327, #31467, #25828, #63835, #54569, #40420, #68137, #61697, #67777, #45173, #68648, #37097, #37637, #15158, #60929, #41463, #74217, #55669, #8578, #26634, #7498, #20391, #57813, #48679, #18002, #5015, #33561, #63548, #3446, #15695, #12831, #1544, #64833, #52411, #40644, #18338, #10254, #30697, #3432, #29188, #2272, #10352, #38680, #54665, #4100, #62063, #19690, #40363, #29387, #5738, #73408, #30944, #899, #34036, #17100, #73242, #950, #52598, #18557, #56804, #62079, #34848, #41221, #14583, #48925, #27195, #4848, #29591, #23886, #37176, #48355, #24256, #4116, #67250, #14866, #61012, #53698, #4909, #31602, #46485, #14978, #33686, #54747, #60740, #26679, #18928, #39890, #37285, #34876, #20256, #35588, #11272, #7970, #27910, #55043, #23606, #34372, #15179, #47721, #51525, #4175, #69622, #65683, #28569, #72831, #12562, #26514, #73228, #4566, #66653, #23424, #8779, #14598, #14456, #35240, #6738, #48998, #37164, #14041, #27300, #12932, #68116, #6454, #72784, #1468, #27809, #48802, #48752, #28572, #239, #36600, #20687, #49274, #44327, #23522, #42440, #73297, #25817, #52045, #51877, #64224, #23439, #5100, #57923, #63268, #35417, #29016, #63850, #18694, #58332, #20157, #27615, #28007, #7919, #70283, #1699, #21248, #2652, #50661, #57279, #14505, #33157, #35531, #47010, #68429, #49991, #24848, #31647, #5286, #71098, #65826, #40671, #50177, #20326, #13309, #47926, #33270, #68624, #69254, #46906, #5122, #30317, #28089, #48645, #11905, #12288, #37648, #59886, #23997, #1911, #70708, #42927, #3321, #64404, #23101, #69451, #11652, #30233, #13823, #11726, #39789, #21060, #16637, #56628, #33849, #12115, #9680, #26056, #34964, #31986, #4225, #33307, #49271, #38754, #69903, #43224, #44768, #66521, #20973, #26035, #36003, #67318, #39204, #8499, #10265, #29485, #46753, #18387, #57709, #46099, #48610, #29471, #67079, #65886, #30778, #37499, #53080, #9341, #427, #38844, #13582, #33326, #62275, #59091, #12000, #2530, #24411, #40144, #59746, #19980, #59732, #29875, #32786, #68224, #33437, #46693, #15975, #10850, #29922, #29833, #55215, #72934, #5021, #22391, #52823, #58142, #13208, #34861, #10440, #61231, #53904, #16572, #4295, #13380, #62934, #29148, #36330, #36050, #74074, #50271, #45723, #52355, #51898, #68695, #19680, #3153, #13048, #69532, #8542, #43225, #39407, #29172, #41999, #36806, #26827, #35119, #8789, #34468, #32706, #67699, #27473, #15175, #61143, #10525, #46792, #18580, #17936, #58655, #4161, #55105, #53484, #65094, #23687, #69200, #489, #32649, #21664, #5788, #41244, #15130 ) ) ;
#12923=ORIENTED_EDGE ( 'NONE', *, *, #71899, .F. ) ;
#12932=ORIENTED_EDGE ( 'NONE', *, *, #57472, .F. ) ;
#12937=CIRCLE ( 'NONE', #58567, 31.99999999999999289 ) ;
#12939=CARTESIAN_POINT ( 'NONE',  ( 10.00000000000000000, -30.41916302227164337, 71.27951684758015460 ) ) ;
#12940=AXIS2_PLACEMENT_3D ( 'NONE', #36568, #72612, #21119 ) ;
#12943=CYLINDRICAL_SURFACE ( 'NONE', #4439, 82.00000000000000000 ) ;
#12947=EDGE_CURVE ( 'NONE', #60509, #56683, #4647, .T. ) ;
#12962=AXIS2_PLACEMENT_3D ( 'NONE', #52500, #36326, #34855 ) ;
#12969=CARTESIAN_POINT ( 'NONE',  ( 10.00000000000000000, -60.67117009219097667, -55.16347631943105512 ) ) ;
#12971=AXIS2_PLACEMENT_3D ( 'NONE', #27889, #11698, #21880 ) ;
#12973=ADVANCED_FACE ( 'NONE', ( #18539 ), #41476, .T. ) ;
#12979=DIRECTION ( 'NONE',  ( 0.000000000000000000, 0.000000000000000000, 1.000000000000000000 ) ) ;
#12987=EDGE_CURVE ( 'NONE', #29474, #72004, #73026, .T. ) ;
#12989=CIRCLE ( 'NONE', #43071, 77.49900000000002365 ) ;
#13006=CIRCLE ( 'NONE', #44262, 32.00000000000000000 ) ;
#13007=DIRECTION ( 'NONE',  ( -1.000000000000000000, 0.000000000000000000, 0.000000000000000000 ) ) ;
#13024=ORIENTED_EDGE ( 'NONE', *, *, #34814, .T. ) ;
#13032=VERTEX_POINT ( 'NONE', #43710 ) ;
#13048=ORIENTED_EDGE ( 'NONE', *, *, #24682, .F. ) ;
#13057=EDGE_CURVE ( 'NONE', #39711, #46797, #29834, .T. ) ;
#13058=EDGE_CURVE ( 'NONE', #50178, #61657, #37329, .T. ) ;
#13063=CARTESIAN_POINT ( 'NONE',  ( 10.00000000000000000, 77.32052557432841411, 5.256550761633138613 ) ) ;
#13068=CARTESIAN_POINT ( 'NONE',  ( 5.000000000000000000, -68.55367621811112144, -44.99326035066125939 ) ) ;
#13072=FACE_OUTER_BOUND ( 'NONE', #55270, .T. ) ;
#13073=DIRECTION ( 'NONE',  ( -1.000000000000000000, 0.000000000000000000, -0.000000000000000000 ) ) ;
#13076=CARTESIAN_POINT ( 'NONE',  ( 0.000000000000000000, 72.35160999960844208, -20.41045688087747223 ) ) ;
#13083=DIRECTION ( 'NONE',  ( 0.000000000000000000, 1.000000000000000000, 3.469446951953614978E-15 ) ) ;
#13088=VECTOR ( 'NONE', #37663, 1000.000000000000000 ) ;
#13091=AXIS2_PLACEMENT_3D ( 'NONE', #29778, #6867, #52732 ) ;
#13092=DIRECTION ( 'NONE',  ( -1.000000000000000000, -0.000000000000000000, -0.000000000000000000 ) ) ;
#13094=DIRECTION ( 'NONE',  ( -1.000000000000000000, -0.000000000000000000, 0.000000000000000000 ) ) ;
#13103=ORIENTED_EDGE ( 'NONE', *, *, #16225, .T. ) ;
#13125=CARTESIAN_POINT ( 'NONE',  ( 10.00000000000000000, -8.840884882375609877, 74.65374052328647281 ) ) ;
#13134=EDGE_LOOP ( 'NONE', ( #34069, #71804, #12088, #41925 ) ) ;
#13139=ADVANCED_FACE ( 'NONE', ( #54968 ), #65528, .T. ) ;
#13140=VERTEX_POINT ( 'NONE', #59892 ) ;
#13149=CARTESIAN_POINT ( 'NONE',  ( 0.000000000000000000, 77.49459641780886443, -0.8261519478433788644 ) ) ;
#13154=CARTESIAN_POINT ( 'NONE',  ( 10.00000000000000000, -77.49459641780886443, 0.8261519478428377417 ) ) ;
#13159=CIRCLE ( 'NONE', #69572, 31.99999999999998579 ) ;
#13161=CYLINDRICAL_SURFACE ( 'NONE', #33134, 77.49899999999999523 ) ;
#13173=LINE ( 'NONE', #12433, #49768 ) ;
#13175=DIRECTION ( 'NONE',  ( 0.000000000000000000, 0.3090169943749412895, 0.9510565162951556406 ) ) ;
#13183=CYLINDRICAL_SURFACE ( 'NONE', #70043, 77.49899999999999523 ) ;
#13187=DIRECTION ( 'NONE',  ( 0.000000000000000000, 0.000000000000000000, 1.000000000000000000 ) ) ;
#13188=ORIENTED_EDGE ( 'NONE', *, *, #50042, .F. ) ;
#13199=VECTOR ( 'NONE', #74168, 1000.000000000000000 ) ;
#13203=CIRCLE ( 'NONE', #20413, 31.99999999999999289 ) ;
#13208=ORIENTED_EDGE ( 'NONE', *, *, #47865, .F. ) ;
#13213=ORIENTED_EDGE ( 'NONE', *, *, #63262, .F. ) ;
#13219=ORIENTED_EDGE ( 'NONE', *, *, #73737, .F. ) ;
#13236=CARTESIAN_POINT ( 'NONE',  ( 10.00000000000000000, 72.35432306680485226, -20.40083707022909110 ) ) ;
#13250=DIRECTION ( 'NONE',  ( 0.000000000000000000, -0.9238795325112822976, -0.3826834323651008285 ) ) ;
#13265=CARTESIAN_POINT ( 'NONE',  ( 10.00000000000000000, 75.16055320797030959, 18.89407956138283851 ) ) ;
#13266=DIRECTION ( 'NONE',  ( 0.000000000000000000, 0.000000000000000000, 1.000000000000000000 ) ) ;
#13269=AXIS2_PLACEMENT_3D ( 'NONE', #5618, #34915, #376 ) ;
#13272=DIRECTION ( 'NONE',  ( 0.000000000000000000, 0.9876883405951383255, -0.1564344650402277048 ) ) ;
#13277=CYLINDRICAL_SURFACE ( 'NONE', #61667, 82.00000000000000000 ) ;
#13283=DIRECTION ( 'NONE',  ( -1.000000000000000000, 0.000000000000000000, 0.000000000000000000 ) ) ;
#13292=CYLINDRICAL_SURFACE ( 'NONE', #37161, 77.49899999999999523 ) ;
#13295=DIRECTION ( 'NONE',  ( 0.000000000000000000, 0.000000000000000000, 1.000000000000000000 ) ) ;
#13296=ORIENTED_EDGE ( 'NONE', *, *, #71336, .T. ) ;
#13309=ORIENTED_EDGE ( 'NONE', *, *, #46330, .F. ) ;
#13334=DIRECTION ( 'NONE',  ( -1.000000000000000000, 0.000000000000000000, 0.000000000000000000 ) ) ;
#13343=AXIS2_PLACEMENT_3D ( 'NONE', #36731, #49125, #25822 ) ;
#13344=EDGE_LOOP ( 'NONE', ( #50314, #20792, #28938, #67780 ) ) ;
#13347=EDGE_CURVE ( 'NONE', #42089, #968, #70723, .T. ) ;
#13358=CARTESIAN_POINT ( 'NONE',  ( 0.000000000000000000, 79.10210256391368944, 21.60688246758614284 ) ) ;
#13360=DIRECTION ( 'NONE',  ( -1.000000000000000000, 0.000000000000000000, 0.000000000000000000 ) ) ;
#13369=CIRCLE ( 'NONE', #55388, 82.00000000000000000 ) ;
#13375=VECTOR ( 'NONE', #42225, 1000.000000000000000 ) ;
#13380=ORIENTED_EDGE ( 'NONE', *, *, #33145, .F. ) ;
#13384=VECTOR ( 'NONE', #4010, 1000.000000000000000 ) ;
#13407=DIRECTION ( 'NONE',  ( -1.000000000000000000, 0.000000000000000000, 0.000000000000000000 ) ) ;
#13419=EDGE_CURVE ( 'NONE', #34204, #39425, #7094, .T. ) ;
#13421=DIRECTION ( 'NONE',  ( -1.000000000000000000, 0.000000000000000000, 0.000000000000000000 ) ) ;
#13424=VECTOR ( 'NONE', #12331, 1000.000000000000000 ) ;
#13425=FACE_OUTER_BOUND ( 'NONE', #51047, .T. ) ;
#13428=EDGE_CURVE ( 'NONE', #28262, #16918, #33487, .T. ) ;
#13436=CARTESIAN_POINT ( 'NONE',  ( 10.00000000000000000, 46.21855187248719687, -62.20884554313968806 ) ) ;
#13449=DIRECTION ( 'NONE',  ( 0.000000000000000000, 0.3090169943749480619, -0.9510565162951533091 ) ) ;
#13466=CARTESIAN_POINT ( 'NONE',  ( 10.00000000000000000, -6.903761155837252694, -77.19088730480530103 ) ) ;
#13471=DIRECTION ( 'NONE',  ( -1.000000000000000000, 0.000000000000000000, 0.000000000000000000 ) ) ;
#13474=CIRCLE ( 'NONE', #33879, 82.00000000000000000 ) ;
#13479=CIRCLE ( 'NONE', #38716, 31.99999999999999645 ) ;
#13489=CARTESIAN_POINT ( 'NONE',  ( 0.000000000000000000, -73.44644590900043113, -24.73286445877782924 ) ) ;
#13494=VECTOR ( 'NONE', #53397, 1000.000000000000000 ) ;
#13497=DIRECTION ( 'NONE',  ( -1.000000000000000000, -0.000000000000000000, -0.000000000000000000 ) ) ;
#13507=ADVANCED_FACE ( 'NONE', ( #58063 ), #52409, .T. ) ;
#13508=ORIENTED_EDGE ( 'NONE', *, *, #68261, .T. ) ;
#13514=VERTEX_POINT ( 'NONE', #29842 ) ;
#13535=DIRECTION ( 'NONE',  ( -1.000000000000000000, 0.000000000000000000, 0.000000000000000000 ) ) ;
#13558=DIRECTION ( 'NONE',  ( 0.000000000000000000, -0.2334453638558922628, -0.9723699203976798877 ) ) ;
#13559=ORIENTED_EDGE ( 'NONE', *, *, #51162, .F. ) ;
#13567=CARTESIAN_POINT ( 'NONE',  ( 0.000000000000000000, -59.75363087400035056, -56.15606465355021015 ) ) ;
#13576=CARTESIAN_POINT ( 'NONE',  ( 10.00000000000000000, 0.000000000000000000, 0.000000000000000000 ) ) ;
#13582=ORIENTED_EDGE ( 'NONE', *, *, #34062, .F. ) ;
#13583=CARTESIAN_POINT ( 'NONE',  ( 10.00000000000000000, -71.87247863392384772, -39.47590169984921005 ) ) ;
#13584=VECTOR ( 'NONE', #21622, 1000.000000000000000 ) ;
#13589=CIRCLE ( 'NONE', #38958, 82.00000000000000000 ) ;
#13594=AXIS2_PLACEMENT_3D ( 'NONE', #9847, #8744, #55711 ) ;
#13603=DIRECTION ( 'NONE',  ( 0.000000000000000000, 0.3826834323650842862, 0.9238795325112890700 ) ) ;
#13610=ORIENTED_EDGE ( 'NONE', *, *, #32341, .T. ) ;
#13612=CARTESIAN_POINT ( 'NONE',  ( 0.000000000000000000, 20.40083707022882820, 72.35432306680490910 ) ) ;
#13615=DIRECTION ( 'NONE',  ( -1.000000000000000000, 0.000000000000000000, 0.000000000000000000 ) ) ;
#13618=DIRECTION ( 'NONE',  ( 0.000000000000000000, 0.07845909572784512398, -0.9969173337331279638 ) ) ;
#13621=ORIENTED_EDGE ( 'NONE', *, *, #47689, .T. ) ;
#13628=DIRECTION ( 'NONE',  ( 0.000000000000000000, 0.000000000000000000, -1.000000000000000000 ) ) ;
#13636=CARTESIAN_POINT ( 'NONE',  ( 10.00000000000000000, 41.76937507738788469, 62.50329211542452157 ) ) ;
#13649=FACE_OUTER_BOUND ( 'NONE', #26360, .T. ) ;
#13660=EDGE_CURVE ( 'NONE', #10255, #17228, #57561, .T. ) ;
#13665=ORIENTED_EDGE ( 'NONE', *, *, #26968, .F. ) ;
#13666=ORIENTED_EDGE ( 'NONE', *, *, #22417, .F. ) ;
#13676=CARTESIAN_POINT ( 'NONE',  ( 10.00000000000000000, 0.000000000000000000, 0.000000000000000000 ) ) ;
#13694=ORIENTED_EDGE ( 'NONE', *, *, #10868, .F. ) ;
#13701=CARTESIAN_POINT ( 'NONE',  ( 10.00000000000000000, -68.27212725128254078, -31.46837873495049465 ) ) ;
#13707=EDGE_LOOP ( 'NONE', ( #46436, #37742, #68291, #35110 ) ) ;
#13710=DIRECTION ( 'NONE',  ( 0.000000000000000000, 0.3826834323650841752, 0.9238795325112891810 ) ) ;
#13713=DIRECTION ( 'NONE',  ( 0.000000000000000000, 0.2334453638558990907, 0.9723699203976781114 ) ) ;
#13720=CARTESIAN_POINT ( 'NONE',  ( 10.00000000000000000, 62.50329211542494789, -41.76937507738723099 ) ) ;
#13729=DIRECTION ( 'NONE',  ( 0.000000000000000000, 0.000000000000000000, -1.000000000000000000 ) ) ;
#13742=FACE_OUTER_BOUND ( 'NONE', #19885, .T. ) ;
#13743=ORIENTED_EDGE ( 'NONE', *, *, #24362, .T. ) ;
#13745=ADVANCED_FACE ( 'NONE', ( #20794 ), #15147, .T. ) ;
#13755=DIRECTION ( 'NONE',  ( -1.000000000000000000, 0.000000000000000000, 0.000000000000000000 ) ) ;
#13759=DIRECTION ( 'NONE',  ( -1.000000000000000000, 0.000000000000000000, -0.000000000000000000 ) ) ;
#13761=EDGE_CURVE ( 'NONE', #39587, #44855, #69570, .T. ) ;
#13762=DIRECTION ( 'NONE',  ( 0.000000000000000000, 0.000000000000000000, 1.000000000000000000 ) ) ;
#13770=CARTESIAN_POINT ( 'NONE',  ( 5.000000000000002665, 81.50828551894227303, 8.966570791700979370 ) ) ;
#13777=CYLINDRICAL_SURFACE ( 'NONE', #47054, 31.99999999999999289 ) ;
#13784=CARTESIAN_POINT ( 'NONE',  ( 0.000000000000000000, 74.18225833017937987, -34.94270380257560049 ) ) ;
#13790=ORIENTED_EDGE ( 'NONE', *, *, #29617, .F. ) ;
#13791=FACE_OUTER_BOUND ( 'NONE', #37463, .T. ) ;
#13796=AXIS2_PLACEMENT_3D ( 'NONE', #45113, #68037, #66911 ) ;
#13823=ORIENTED_EDGE ( 'NONE', *, *, #4625, .F. ) ;
#13833=LINE ( 'NONE', #66113, #22430 ) ;
#13834=ORIENTED_EDGE ( 'NONE', *, *, #66190, .T. ) ;
#13843=CYLINDRICAL_SURFACE ( 'NONE', #25105, 31.99999999999999289 ) ;
#13856=DIRECTION ( 'NONE',  ( -1.000000000000000000, 0.000000000000000000, -0.000000000000000000 ) ) ;
#13858=VECTOR ( 'NONE', #8728, 1000.000000000000000 ) ;
#13859=ORIENTED_EDGE ( 'NONE', *, *, #25612, .F. ) ;
#13871=AXIS2_PLACEMENT_3D ( 'NONE', #64814, #23839, #14024 ) ;
#13874=CARTESIAN_POINT ( 'NONE',  ( 0.000000000000000000, 0.000000000000000000, 0.000000000000000000 ) ) ;
#13879=DIRECTION ( 'NONE',  ( -1.000000000000000000, 0.000000000000000000, -0.000000000000000000 ) ) ;
#13891=LINE ( 'NONE', #53394, #49338 ) ;
#13892=CARTESIAN_POINT ( 'NONE',  ( 10.00000000000000000, 0.000000000000000000, 0.000000000000000000 ) ) ;
#13894=ADVANCED_FACE ( 'NONE', ( #874 ), #58715, .T. ) ;
#13898=CARTESIAN_POINT ( 'NONE',  ( 10.00000000000000000, 31.47745569255140552, 68.26794271651274926 ) ) ;
#13904=LINE ( 'NONE', #53770, #32220 ) ;
#13925=CARTESIAN_POINT ( 'NONE',  ( 0.000000000000000000, -74.74816331893404708, -33.71516098798818462 ) ) ;
#13931=ADVANCED_FACE ( 'NONE', ( #52326 ), #41424, .T. ) ;
#13941=PLANE ( 'NONE',  #59313 ) ;
#13944=DIRECTION ( 'NONE',  ( -1.000000000000000000, -0.000000000000000000, -0.000000000000000000 ) ) ;
#13948=ORIENTED_EDGE ( 'NONE', *, *, #42775, .F. ) ;
#13950=ORIENTED_EDGE ( 'NONE', *, *, #23203, .T. ) ;
#13962=CARTESIAN_POINT ( 'NONE',  ( 0.000000000000000000, 0.000000000000000000, 0.000000000000000000 ) ) ;
#13972=CARTESIAN_POINT ( 'NONE',  ( 0.000000000000000000, 0.000000000000000000, 0.000000000000000000 ) ) ;
#13973=DIRECTION ( 'NONE',  ( -1.000000000000000000, 0.000000000000000000, -0.000000000000000000 ) ) ;
#13977=EDGE_CURVE ( 'NONE', #63033, #2062, #47670, .T. ) ;
#13982=EDGE_CURVE ( 'NONE', #71305, #68580, #68530, .T. ) ;
#13984=ORIENTED_EDGE ( 'NONE', *, *, #65311, .T. ) ;
#13992=DIRECTION ( 'NONE',  ( 0.000000000000000000, -0.8526401643540859610, -0.5224985647159591240 ) ) ;
#13993=DIRECTION ( 'NONE',  ( -1.000000000000000000, -0.000000000000000000, -0.000000000000000000 ) ) ;
#13994=ORIENTED_EDGE ( 'NONE', *, *, #66737, .F. ) ;
#13999=CARTESIAN_POINT ( 'NONE',  ( 0.000000000000000000, 0.000000000000000000, -2.500000000000000000 ) ) ;
#14004=EDGE_CURVE ( 'NONE', #11722, #40784, #40313, .T. ) ;
#14011=EDGE_LOOP ( 'NONE', ( #46535, #36233, #61392, #26433 ) ) ;
#14022=DIRECTION ( 'NONE',  ( -1.000000000000000000, -0.000000000000000000, -0.000000000000000000 ) ) ;
#14023=CIRCLE ( 'NONE', #24827, 31.99999999999998934 ) ;
#14024=DIRECTION ( 'NONE',  ( 0.000000000000000000, 0.9876883405951383255, -0.1564344650402276216 ) ) ;
#14030=AXIS2_PLACEMENT_3D ( 'NONE', #44280, #27726, #28459 ) ;
#14035=CIRCLE ( 'NONE', #51293, 31.99999999999999645 ) ;
#14036=ORIENTED_EDGE ( 'NONE', *, *, #45283, .F. ) ;
#14040=DIRECTION ( 'NONE',  ( -1.000000000000000000, -0.000000000000000000, 0.000000000000000000 ) ) ;
#14041=ORIENTED_EDGE ( 'NONE', *, *, #50820, .F. ) ;
#14042=EDGE_LOOP ( 'NONE', ( #41220, #835, #63163, #39048 ) ) ;
#14047=DIRECTION ( 'NONE',  ( 1.000000000000000000, -0.000000000000000000, -0.000000000000000000 ) ) ;
#14057=ORIENTED_EDGE ( 'NONE', *, *, #61480, .T. ) ;
#14066=DIRECTION ( 'NONE',  ( 1.000000000000000000, -0.000000000000000000, -0.000000000000000000 ) ) ;
#14069=CARTESIAN_POINT ( 'NONE',  ( 10.00000000000000000, -2.956366410621191765, 75.11725578898467859 ) ) ;
#14072=EDGE_CURVE ( 'NONE', #49109, #36877, #62062, .T. ) ;
#14073=ORIENTED_EDGE ( 'NONE', *, *, #57984, .T. ) ;
#14076=DIRECTION ( 'NONE',  ( 0.000000000000000000, 0.000000000000000000, 1.000000000000000000 ) ) ;
#14077=DIRECTION ( 'NONE',  ( 0.000000000000000000, 0.4539904997395413644, 0.8910065241883706744 ) ) ;
#14080=CARTESIAN_POINT ( 'NONE',  ( 10.00000000000000000, -14.67089635893764665, 73.72996012237435082 ) ) ;
#14087=CARTESIAN_POINT ( 'NONE',  ( 5.000000000000000000, 67.80270845531956070, -46.11716303203112943 ) ) ;
#14091=CARTESIAN_POINT ( 'NONE',  ( 10.00000000000000000, 28.89263327155746097, 71.91182617369197771 ) ) ;
#14096=CARTESIAN_POINT ( 'NONE',  ( 0.000000000000000000, 68.26794271651262136, 31.47745569255165066 ) ) ;
#14097=EDGE_CURVE ( 'NONE', #25646, #38932, #35641, .T. ) ;
#14106=ADVANCED_FACE ( 'NONE', ( #8694 ), #70715, .T. ) ;
#14113=DIRECTION ( 'NONE',  ( -1.000000000000000000, -0.000000000000000000, 0.000000000000000000 ) ) ;
#14122=DIRECTION ( 'NONE',  ( 0.000000000000000000, 0.000000000000000000, 1.000000000000000000 ) ) ;
#14130=DIRECTION ( 'NONE',  ( 0.000000000000000000, 0.000000000000000000, 1.000000000000000000 ) ) ;
#14150=AXIS2_PLACEMENT_3D ( 'NONE', #19653, #26034, #37339 ) ;
#14158=FACE_OUTER_BOUND ( 'NONE', #54084, .T. ) ;
#14161=DIRECTION ( 'NONE',  ( -1.000000000000000000, -0.000000000000000000, 0.000000000000000000 ) ) ;
#14163=EDGE_CURVE ( 'NONE', #50561, #55514, #20022, .T. ) ;
#14166=DIRECTION ( 'NONE',  ( -1.000000000000000000, -0.000000000000000000, -0.000000000000000000 ) ) ;
#14173=ORIENTED_EDGE ( 'NONE', *, *, #32763, .F. ) ;
#14175=AXIS2_PLACEMENT_3D ( 'NONE', #46476, #10408, #67932 ) ;
#14180=DIRECTION ( 'NONE',  ( -1.000000000000000000, 0.000000000000000000, -0.000000000000000000 ) ) ;
#14182=AXIS2_PLACEMENT_3D ( 'NONE', #10410, #2690, #36476 ) ;
#14183=DIRECTION ( 'NONE',  ( 0.000000000000000000, 0.000000000000000000, -1.000000000000000000 ) ) ;
#14189=DIRECTION ( 'NONE',  ( 0.000000000000000000, 0.8090169943749445647, 0.5877852522924770229 ) ) ;
#14199=CIRCLE ( 'NONE', #35827, 31.99999999999999289 ) ;
#14205=CARTESIAN_POINT ( 'NONE',  ( 0.000000000000000000, -46.54456581323762521, -59.03342792756313884 ) ) ;
#14209=ADVANCED_FACE ( 'NONE', ( #4926 ), #66934, .T. ) ;
#14213=VECTOR ( 'NONE', #55106, 1000.000000000000000 ) ;
#14219=DIRECTION ( 'NONE',  ( -1.000000000000000000, -0.000000000000000000, 0.000000000000000000 ) ) ;
#14220=VERTEX_POINT ( 'NONE', #56417 ) ;
#14222=CIRCLE ( 'NONE', #62289, 77.49899999999999523 ) ;
#14227=ORIENTED_EDGE ( 'NONE', *, *, #34645, .F. ) ;
#14228=CARTESIAN_POINT ( 'NONE',  ( 0.000000000000000000, 55.19960302592141232, -51.03279382321027668 ) ) ;
#14233=DIRECTION ( 'NONE',  ( 0.000000000000000000, 0.2334453638559060296, -0.9723699203976764460 ) ) ;
#14236=ORIENTED_EDGE ( 'NONE', *, *, #24640, .T. ) ;
#14239=ORIENTED_EDGE ( 'NONE', *, *, #52956, .F. ) ;
#14252=DIRECTION ( 'NONE',  ( 0.000000000000000000, -0.8526401643540860720, -0.5224985647159590130 ) ) ;
#14258=AXIS2_PLACEMENT_3D ( 'NONE', #26513, #72001, #15231 ) ;
#14272=CARTESIAN_POINT ( 'NONE',  ( 10.00000000000000000, 16.65972982744934683, 80.28980883073762698 ) ) ;
#14281=DIRECTION ( 'NONE',  ( -1.000000000000000000, 0.000000000000000000, -0.000000000000000000 ) ) ;
#14283=EDGE_CURVE ( 'NONE', #57624, #55001, #56098, .T. ) ;
#14293=AXIS2_PLACEMENT_3D ( 'NONE', #54077, #37155, #3332 ) ;
#14298=AXIS2_PLACEMENT_3D ( 'NONE', #2393, #9091, #54953 ) ;
#14308=ORIENTED_EDGE ( 'NONE', *, *, #71806, .T. ) ;
#14325=CARTESIAN_POINT ( 'NONE',  ( 10.00000000000000000, -17.28742895386031719, -75.54627589209962935 ) ) ;
#14329=EDGE_LOOP ( 'NONE', ( #73773, #49284, #62359, #72650 ) ) ;
#14330=DIRECTION ( 'NONE',  ( 0.000000000000000000, 0.000000000000000000, 1.000000000000000000 ) ) ;
#14331=AXIS2_PLACEMENT_3D ( 'NONE', #63661, #6508, #35073 ) ;
#14343=EDGE_LOOP ( 'NONE', ( #19129, #44415, #8061, #41356 ) ) ;
#14344=DIRECTION ( 'NONE',  ( 0.000000000000000000, 0.000000000000000000, 1.000000000000000000 ) ) ;
#14346=ORIENTED_EDGE ( 'NONE', *, *, #65697, .T. ) ;
#14358=EDGE_CURVE ( 'NONE', #35896, #70403, #42901, .T. ) ;
#14359=DIRECTION ( 'NONE',  ( -1.000000000000000000, 0.000000000000000000, -0.000000000000000000 ) ) ;
#14368=VECTOR ( 'NONE', #42303, 1000.000000000000000 ) ;
#14369=ORIENTED_EDGE ( 'NONE', *, *, #7054, .F. ) ;
#14370=DIRECTION ( 'NONE',  ( -1.000000000000000000, -0.000000000000000000, 0.000000000000000000 ) ) ;
#14376=CARTESIAN_POINT ( 'NONE',  ( 10.00000000000000000, -46.11716303203136391, -67.80270845531937596 ) ) ;
#14379=CARTESIAN_POINT ( 'NONE',  ( 10.00000000000000000, 8.830959090343430518, -74.65491531819107252 ) ) ;
#14382=CYLINDRICAL_SURFACE ( 'NONE', #42972, 31.99999999999999289 ) ;
#14387=CIRCLE ( 'NONE', #56422, 77.49899999999999523 ) ;
#14392=ORIENTED_EDGE ( 'NONE', *, *, #53702, .T. ) ;
#14397=VECTOR ( 'NONE', #66864, 1000.000000000000000 ) ;
#14403=ORIENTED_EDGE ( 'NONE', *, *, #28881, .T. ) ;
#14404=DIRECTION ( 'NONE',  ( -1.000000000000000000, -0.000000000000000000, -0.000000000000000000 ) ) ;
#14407=EDGE_CURVE ( 'NONE', #35421, #47282, #45528, .T. ) ;
#14409=CIRCLE ( 'NONE', #38412, 82.00000000000000000 ) ;
#14424=ORIENTED_EDGE ( 'NONE', *, *, #54405, .T. ) ;
#14425=ORIENTED_EDGE ( 'NONE', *, *, #39291, .F. ) ;
#14431=CARTESIAN_POINT ( 'NONE',  ( 10.00000000000000000, 0.000000000000000000, 0.000000000000000000 ) ) ;
#14447=DIRECTION ( 'NONE',  ( 1.000000000000000000, 0.000000000000000000, 0.000000000000000000 ) ) ;
#14455=ORIENTED_EDGE ( 'NONE', *, *, #42612, .T. ) ;
#14456=ORIENTED_EDGE ( 'NONE', *, *, #38128, .F. ) ;
#14463=DIRECTION ( 'NONE',  ( -1.000000000000000000, -0.000000000000000000, -0.000000000000000000 ) ) ;
#14467=CIRCLE ( 'NONE', #25259, 31.99999999999998579 ) ;
#14475=CARTESIAN_POINT ( 'NONE',  ( 0.000000000000000000, 0.000000000000000000, 0.000000000000000000 ) ) ;
#14488=VERTEX_POINT ( 'NONE', #63188 ) ;
#14492=CIRCLE ( 'NONE', #55340, 82.00000000000000000 ) ;
#14505=ORIENTED_EDGE ( 'NONE', *, *, #46211, .F. ) ;
#14509=CARTESIAN_POINT ( 'NONE',  ( 0.000000000000000000, 8.830959090342393125, 74.65491531819122883 ) ) ;
#14528=VERTEX_POINT ( 'NONE', #31168 ) ;
#14544=CARTESIAN_POINT ( 'NONE',  ( 10.00000000000000000, -79.10210256391383155, 21.60688246758557796 ) ) ;
#14559=CARTESIAN_POINT ( 'NONE',  ( 0.000000000000000000, 75.16055320797030959, 18.89407956138283851 ) ) ;
#14570=CIRCLE ( 'NONE', #24197, 77.49899999999999523 ) ;
#14579=CARTESIAN_POINT ( 'NONE',  ( 50.00005079999999680, 0.000000000000000000, 0.000000000000000000 ) ) ;
#14583=ORIENTED_EDGE ( 'NONE', *, *, #38776, .F. ) ;
#14587=DIRECTION ( 'NONE',  ( 0.000000000000000000, -0.3826834323650772363, -0.9238795325112919565 ) ) ;
#14598=ORIENTED_EDGE ( 'NONE', *, *, #40302, .F. ) ;
#14600=VECTOR ( 'NONE', #34622, 1000.000000000000000 ) ;
#14607=VERTEX_POINT ( 'NONE', #38299 ) ;
#14611=DIRECTION ( 'NONE',  ( 0.000000000000000000, 0.000000000000000000, 1.000000000000000000 ) ) ;
#14613=ORIENTED_EDGE ( 'NONE', *, *, #42902, .T. ) ;
#14618=CARTESIAN_POINT ( 'NONE',  ( 10.00000000000000000, 0.000000000000000000, 0.000000000000000000 ) ) ;
#14625=ORIENTED_EDGE ( 'NONE', *, *, #15694, .F. ) ;
#14627=AXIS2_PLACEMENT_3D ( 'NONE', #60731, #72711, #73093 ) ;
#14633=ORIENTED_EDGE ( 'NONE', *, *, #56745, .F. ) ;
#14637=LINE ( 'NONE', #13154, #71048 ) ;
#14641=DIRECTION ( 'NONE',  ( 0.000000000000000000, -0.3826834323650970537, 0.9238795325112838519 ) ) ;
#14642=CARTESIAN_POINT ( 'NONE',  ( 0.000000000000000000, 69.42325613327489009, -34.44570377933524696 ) ) ;
#14681=VERTEX_POINT ( 'NONE', #21355 ) ;
#14685=VERTEX_POINT ( 'NONE', #33384 ) ;
#14692=DIRECTION ( 'NONE',  ( 0.000000000000000000, 0.4539904997395477482, -0.8910065241883674547 ) ) ;
#14699=EDGE_CURVE ( 'NONE', #15522, #27844, #10095, .T. ) ;
#14707=VERTEX_POINT ( 'NONE', #72130 ) ;
#14718=VERTEX_POINT ( 'NONE', #32270 ) ;
#14722=CYLINDRICAL_SURFACE ( 'NONE', #52332, 31.99999999999999289 ) ;
#14723=DIRECTION ( 'NONE',  ( 0.000000000000000000, 0.5877852522924743583, -0.8090169943749466741 ) ) ;
#14732=CARTESIAN_POINT ( 'NONE',  ( 0.000000000000000000, 65.59268652807210742, 36.72794159290264560 ) ) ;
#14742=DIRECTION ( 'NONE',  ( -1.000000000000000000, -0.000000000000000000, 0.000000000000000000 ) ) ;
#14749=EDGE_CURVE ( 'NONE', #69181, #39875, #11571, .T. ) ;
#14770=DIRECTION ( 'NONE',  ( 0.000000000000000000, 0.000000000000000000, 1.000000000000000000 ) ) ;
#14771=AXIS2_PLACEMENT_3D ( 'NONE', #63602, #42879, #36115 ) ;
#14772=EDGE_CURVE ( 'NONE', #71840, #53791, #57826, .T. ) ;
#14777=CIRCLE ( 'NONE', #1630, 82.00000000000000000 ) ;
#14784=VERTEX_POINT ( 'NONE', #52534 ) ;
#14789=DIRECTION ( 'NONE',  ( -1.000000000000000000, -0.000000000000000000, 0.000000000000000000 ) ) ;
#14808=VECTOR ( 'NONE', #9289, 1000.000000000000000 ) ;
#14813=CARTESIAN_POINT ( 'NONE',  ( 10.00000000000000000, -77.19088730480518734, -6.903761155838607166 ) ) ;
#14820=DIRECTION ( 'NONE',  ( -1.000000000000000000, -0.000000000000000000, -0.000000000000000000 ) ) ;
#14821=ORIENTED_EDGE ( 'NONE', *, *, #36645, .F. ) ;
#14825=CARTESIAN_POINT ( 'NONE',  ( -10.00000000000000000, 0.000000000000000000, 0.000000000000000000 ) ) ;
#14828=CARTESIAN_POINT ( 'NONE',  ( 10.00000000000000000, 0.000000000000000000, 0.000000000000000000 ) ) ;
#14841=CARTESIAN_POINT ( 'NONE',  ( 0.000000000000000000, -71.87247863392386193, -39.47590169984923136 ) ) ;
#14843=DIRECTION ( 'NONE',  ( -1.000000000000000000, 0.000000000000000000, 0.000000000000000000 ) ) ;
#14847=FACE_OUTER_BOUND ( 'NONE', #19964, .T. ) ;
#14848=DIRECTION ( 'NONE',  ( -1.000000000000000000, 0.000000000000000000, -0.000000000000000000 ) ) ;
#14852=CARTESIAN_POINT ( 'NONE',  ( 0.000000000000000000, 60.67117009219135326, 55.16347631943062169 ) ) ;
#14862=EDGE_CURVE ( 'NONE', #61671, #28369, #23115, .T. ) ;
#14865=ADVANCED_FACE ( 'NONE', ( #46915 ), #34506, .T. ) ;
#14866=ORIENTED_EDGE ( 'NONE', *, *, #25863, .F. ) ;
#14873=CYLINDRICAL_SURFACE ( 'NONE', #68096, 82.00000000000000000 ) ;
#14875=FACE_OUTER_BOUND ( 'NONE', #9958, .T. ) ;
#14876=VECTOR ( 'NONE', #17661, 1000.000000000000000 ) ;
#14877=DIRECTION ( 'NONE',  ( -1.000000000000000000, 0.000000000000000000, -0.000000000000000000 ) ) ;
#14880=CARTESIAN_POINT ( 'NONE',  ( 10.00000000000000000, -74.65374052328644439, -8.840884882375878107 ) ) ;
#14882=VERTEX_POINT ( 'NONE', #1460 ) ;
#14888=DIRECTION ( 'NONE',  ( 0.000000000000000000, 0.000000000000000000, -1.000000000000000000 ) ) ;
#14909=EDGE_LOOP ( 'NONE', ( #35675, #56988, #15528, #61658 ) ) ;
#14910=FACE_OUTER_BOUND ( 'NONE', #65668, .T. ) ;
#14919=VERTEX_POINT ( 'NONE', #19432 ) ;
#14927=CYLINDRICAL_SURFACE ( 'NONE', #60979, 32.00000000000000000 ) ;
#14931=CARTESIAN_POINT ( 'NONE',  ( 0.000000000000000000, -14.67089635893658794, -73.72996012237454977 ) ) ;
#14933=ADVANCED_FACE ( 'NONE', ( #71295 ), #30707, .T. ) ;
#14937=VECTOR ( 'NONE', #41611, 1000.000000000000000 ) ;
#14944=CIRCLE ( 'NONE', #40183, 82.00000000000000000 ) ;
#14957=EDGE_CURVE ( 'NONE', #1522, #65198, #25501, .T. ) ;
#14978=ORIENTED_EDGE ( 'NONE', *, *, #61916, .F. ) ;
#14981=ORIENTED_EDGE ( 'NONE', *, *, #73213, .F. ) ;
#14990=EDGE_LOOP ( 'NONE', ( #13188, #56772, #32524, #47993 ) ) ;
#14991=VERTEX_POINT ( 'NONE', #70930 ) ;
#14994=ORIENTED_EDGE ( 'NONE', *, *, #67580, .T. ) ;
#15000=ORIENTED_EDGE ( 'NONE', *, *, #29671, .F. ) ;
#15001=CARTESIAN_POINT ( 'NONE',  ( 10.00000000000000000, 54.21277698773752718, -55.38113227695725271 ) ) ;
#15007=ADVANCED_FACE ( 'NONE', ( #36724 ), #53285, .T. ) ;
#15015=DIRECTION ( 'NONE',  ( 0.000000000000000000, 0.000000000000000000, 1.000000000000000000 ) ) ;
#15016=ADVANCED_FACE ( 'NONE', ( #14910 ), #44613, .T. ) ;
#15017=CARTESIAN_POINT ( 'NONE',  ( 10.00000000000000000, -75.11725578898470701, 2.956366410620372864 ) ) ;
#15024=LINE ( 'NONE', #45104, #4709 ) ;
#15027=EDGE_CURVE ( 'NONE', #14919, #35421, #41141, .T. ) ;
#15045=VERTEX_POINT ( 'NONE', #44979 ) ;
#15048=ORIENTED_EDGE ( 'NONE', *, *, #52602, .F. ) ;
#15053=ORIENTED_EDGE ( 'NONE', *, *, #55491, .T. ) ;
#15060=CYLINDRICAL_SURFACE ( 'NONE', #31709, 82.00000000000000000 ) ;
#15062=ORIENTED_EDGE ( 'NONE', *, *, #72806, .F. ) ;
#15063=LINE ( 'NONE', #38001, #8187 ) ;
#15065=DIRECTION ( 'NONE',  ( -1.000000000000000000, -0.000000000000000000, -0.000000000000000000 ) ) ;
#15068=ORIENTED_EDGE ( 'NONE', *, *, #70796, .F. ) ;
#15070=DIRECTION ( 'NONE',  ( 0.000000000000000000, 0.6494480483301793283, 0.7604059656000345946 ) ) ;
#15076=EDGE_CURVE ( 'NONE', #42748, #3975, #50726, .T. ) ;
#15083=ORIENTED_EDGE ( 'NONE', *, *, #59437, .F. ) ;
#15088=DIRECTION ( 'NONE',  ( -1.000000000000000000, -0.000000000000000000, 0.000000000000000000 ) ) ;
#15099=CARTESIAN_POINT ( 'NONE',  ( 0.000000000000000000, -51.03279382321125723, 55.19960302592048862 ) ) ;
#15100=CIRCLE ( 'NONE', #12686, 82.00000000000000000 ) ;
#15101=DIRECTION ( 'NONE',  ( -1.000000000000000000, 0.000000000000000000, 0.000000000000000000 ) ) ;
#15104=DIRECTION ( 'NONE',  ( 0.000000000000000000, 0.000000000000000000, 1.000000000000000000 ) ) ;
#15105=PLANE ( 'NONE',  #1410 ) ;
#15107=VECTOR ( 'NONE', #8359, 1000.000000000000000 ) ;
#15125=EDGE_LOOP ( 'NONE', ( #51783, #29233, #40967, #2461 ) ) ;
#15127=DIRECTION ( 'NONE',  ( 0.000000000000000000, 1.000000000000000000, 3.491481338843133355E-15 ) ) ;
#15128=CARTESIAN_POINT ( 'NONE',  ( 0.000000000000000000, -6.903761155837252694, -77.19088730480530103 ) ) ;
#15130=ORIENTED_EDGE ( 'NONE', *, *, #16841, .F. ) ;
#15137=ORIENTED_EDGE ( 'NONE', *, *, #13347, .F. ) ;
#15146=ORIENTED_EDGE ( 'NONE', *, *, #9834, .T. ) ;
#15147=CYLINDRICAL_SURFACE ( 'NONE', #33538, 82.00000000000000000 ) ;
#15157=VERTEX_POINT ( 'NONE', #17873 ) ;
#15158=ORIENTED_EDGE ( 'NONE', *, *, #68261, .F. ) ;
#15165=AXIS2_PLACEMENT_3D ( 'NONE', #37901, #37166, #25498 ) ;
#15169=EDGE_CURVE ( 'NONE', #4854, #13140, #19484, .T. ) ;
#15175=ORIENTED_EDGE ( 'NONE', *, *, #33929, .F. ) ;
#15179=ORIENTED_EDGE ( 'NONE', *, *, #28411, .F. ) ;
#15185=DIRECTION ( 'NONE',  ( -1.000000000000000000, 0.000000000000000000, 0.000000000000000000 ) ) ;
#15187=EDGE_CURVE ( 'NONE', #9891, #30579, #50778, .T. ) ;
#15188=LINE ( 'NONE', #27950, #242 ) ;
#15201=CIRCLE ( 'NONE', #57228, 31.99999999999999289 ) ;
#15205=DIRECTION ( 'NONE',  ( -1.000000000000000000, 0.000000000000000000, -0.000000000000000000 ) ) ;
#15211=LINE ( 'NONE', #3960, #28629 ) ;
#15214=DIRECTION ( 'NONE',  ( 0.000000000000000000, 0.000000000000000000, 1.000000000000000000 ) ) ;
#15218=AXIS2_PLACEMENT_3D ( 'NONE', #48129, #20282, #42131 ) ;
#15221=LINE ( 'NONE', #9587, #54193 ) ;
#15230=AXIS2_PLACEMENT_3D ( 'NONE', #53538, #25703, #49369 ) ;
#15231=DIRECTION ( 'NONE',  ( 0.000000000000000000, 0.9876883405951371042, 0.1564344650402346437 ) ) ;
#15245=VECTOR ( 'NONE', #73626, 1000.000000000000000 ) ;
#15252=ORIENTED_EDGE ( 'NONE', *, *, #31215, .T. ) ;
#15253=ORIENTED_EDGE ( 'NONE', *, *, #5529, .T. ) ;
#15266=ORIENTED_EDGE ( 'NONE', *, *, #54012, .F. ) ;
#15267=LINE ( 'NONE', #60047, #13384 ) ;
#15268=ORIENTED_EDGE ( 'NONE', *, *, #58979, .F. ) ;
#15280=VERTEX_POINT ( 'NONE', #10238 ) ;
#15285=DIRECTION ( 'NONE',  ( 0.000000000000000000, 0.000000000000000000, 1.000000000000000000 ) ) ;
#15290=VERTEX_POINT ( 'NONE', #73387 ) ;
#15298=DIRECTION ( 'NONE',  ( -1.000000000000000000, 0.000000000000000000, 0.000000000000000000 ) ) ;
#15299=CARTESIAN_POINT ( 'NONE',  ( 10.00000000000000000, -60.67117009219176538, 55.16347631943019536 ) ) ;
#15300=DIRECTION ( 'NONE',  ( 0.000000000000000000, 0.000000000000000000, -1.000000000000000000 ) ) ;
#15304=LINE ( 'NONE', #42777, #21601 ) ;
#15309=DIRECTION ( 'NONE',  ( 0.000000000000000000, 0.000000000000000000, 1.000000000000000000 ) ) ;
#15315=CYLINDRICAL_SURFACE ( 'NONE', #19195, 31.99999999999999289 ) ;
#15317=DIRECTION ( 'NONE',  ( -1.000000000000000000, -0.000000000000000000, -0.000000000000000000 ) ) ;
#15320=VERTEX_POINT ( 'NONE', #27530 ) ;
#15334=EDGE_CURVE ( 'NONE', #71738, #72957, #36348, .T. ) ;
#15339=EDGE_CURVE ( 'NONE', #64804, #34327, #6368, .T. ) ;
#15342=FACE_OUTER_BOUND ( 'NONE', #33290, .T. ) ;
#15358=VERTEX_POINT ( 'NONE', #50830 ) ;
#15359=CIRCLE ( 'NONE', #72923, 82.00000000000000000 ) ;
#15377=AXIS2_PLACEMENT_3D ( 'NONE', #14880, #47990, #3259 ) ;
#15380=AXIS2_PLACEMENT_3D ( 'NONE', #1817, #47276, #64203 ) ;
#15382=CARTESIAN_POINT ( 'NONE',  ( -10.00000000000000000, 0.000000000000000000, 0.000000000000000000 ) ) ;
#15385=AXIS2_PLACEMENT_3D ( 'NONE', #47861, #19288, #31303 ) ;
#15386=DIRECTION ( 'NONE',  ( -1.000000000000000000, 0.000000000000000000, 0.000000000000000000 ) ) ;
#15398=CIRCLE ( 'NONE', #22616, 32.00000000000000000 ) ;
#15399=DIRECTION ( 'NONE',  ( -1.000000000000000000, -0.000000000000000000, 0.000000000000000000 ) ) ;
#15404=CYLINDRICAL_SURFACE ( 'NONE', #23426, 77.49899999999999523 ) ;
#15408=ORIENTED_EDGE ( 'NONE', *, *, #1560, .T. ) ;
#15409=CARTESIAN_POINT ( 'NONE',  ( 0.000000000000000000, -30.41916302227060598, -71.27951684758059514 ) ) ;
#15410=DIRECTION ( 'NONE',  ( 0.000000000000000000, 0.000000000000000000, 1.000000000000000000 ) ) ;
#15419=CARTESIAN_POINT ( 'NONE',  ( 10.00000000000000000, -75.11764819372145041, -2.946379043147127064 ) ) ;
#15424=EDGE_CURVE ( 'NONE', #66997, #57978, #5149, .T. ) ;
#15425=ORIENTED_EDGE ( 'NONE', *, *, #42513, .T. ) ;
#15427=CIRCLE ( 'NONE', #58693, 82.00000000000000000 ) ;
#15435=ORIENTED_EDGE ( 'NONE', *, *, #65859, .F. ) ;
#15436=CIRCLE ( 'NONE', #35831, 82.00000000000000000 ) ;
#15444=ORIENTED_EDGE ( 'NONE', *, *, #34309, .F. ) ;
#15449=EDGE_CURVE ( 'NONE', #278, #33646, #66368, .T. ) ;
#15460=DIRECTION ( 'NONE',  ( -1.000000000000000000, 0.000000000000000000, 0.000000000000000000 ) ) ;
#15461=DIRECTION ( 'NONE',  ( 0.000000000000000000, 0.000000000000000000, 1.000000000000000000 ) ) ;
#15472=VERTEX_POINT ( 'NONE', #57417 ) ;
#15478=CARTESIAN_POINT ( 'NONE',  ( 10.00000000000000000, 59.03342792756263435, 46.54456581323825048 ) ) ;
#15483=AXIS2_PLACEMENT_3D ( 'NONE', #19159, #19893, #36449 ) ;
#15496=CARTESIAN_POINT ( 'NONE',  ( 10.00000000000000000, -73.95703589263990807, 23.16143007188399139 ) ) ;
#15506=CIRCLE ( 'NONE', #57548, 31.99999999999998934 ) ;
#15508=CARTESIAN_POINT ( 'NONE',  ( 10.00000000000000000, 75.11764819372149304, 29.05362095685338986 ) ) ;
#15511=DIRECTION ( 'NONE',  ( -1.000000000000000000, 0.000000000000000000, 0.000000000000000000 ) ) ;
#15515=EDGE_CURVE ( 'NONE', #2062, #49474, #15957, .T. ) ;
#15517=AXIS2_PLACEMENT_3D ( 'NONE', #6868, #7977, #29779 ) ;
#15518=ORIENTED_EDGE ( 'NONE', *, *, #66, .F. ) ;
#15520=FACE_OUTER_BOUND ( 'NONE', #65111, .T. ) ;
#15522=VERTEX_POINT ( 'NONE', #5189 ) ;
#15523=EDGE_CURVE ( 'NONE', #64668, #17422, #1574, .T. ) ;
#15524=ORIENTED_EDGE ( 'NONE', *, *, #40184, .T. ) ;
#15528=ORIENTED_EDGE ( 'NONE', *, *, #22089, .T. ) ;
#15542=AXIS2_PLACEMENT_3D ( 'NONE', #9714, #55578, #33002 ) ;
#15546=DIRECTION ( 'NONE',  ( -1.000000000000000000, 0.000000000000000000, 0.000000000000000000 ) ) ;
#15564=CARTESIAN_POINT ( 'NONE',  ( 10.00000000000000000, -75.11764819372145041, -2.946379043147127064 ) ) ;
#15568=ORIENTED_EDGE ( 'NONE', *, *, #64171, .T. ) ;
#15569=ORIENTED_EDGE ( 'NONE', *, *, #62245, .T. ) ;
#15575=CARTESIAN_POINT ( 'NONE',  ( 10.00000000000000000, -77.49459641780886443, -0.8261519478439277586 ) ) ;
#15582=CIRCLE ( 'NONE', #57564, 31.99999999999999289 ) ;
#15589=CARTESIAN_POINT ( 'NONE',  ( -10.00000000000000000, 0.000000000000000000, 0.000000000000000000 ) ) ;
#15603=VECTOR ( 'NONE', #1378, 1000.000000000000000 ) ;
#15604=EDGE_CURVE ( 'NONE', #70908, #11546, #30334, .T. ) ;
#15605=CIRCLE ( 'NONE', #58871, 82.00000000000000000 ) ;
#15610=ADVANCED_FACE ( 'NONE', ( #64175 ), #2159, .T. ) ;
#15613=DIRECTION ( 'NONE',  ( -1.000000000000000000, 0.000000000000000000, 0.000000000000000000 ) ) ;
#15622=DIRECTION ( 'NONE',  ( 0.000000000000000000, 0.07845909572784530439, -0.9969173337331279638 ) ) ;
#15626=AXIS2_PLACEMENT_3D ( 'NONE', #37388, #49010, #8799 ) ;
#15637=DIRECTION ( 'NONE',  ( 0.000000000000000000, -0.9510565162951566398, 0.3090169943749381809 ) ) ;
#15644=EDGE_CURVE ( 'NONE', #49408, #70179, #43618, .T. ) ;
#15646=CARTESIAN_POINT ( 'NONE',  ( -10.00000000000000000, 0.000000000000000000, 0.000000000000000000 ) ) ;
#15650=ORIENTED_EDGE ( 'NONE', *, *, #40264, .F. ) ;
#15651=EDGE_CURVE ( 'NONE', #4576, #64387, #35581, .T. ) ;
#15665=ORIENTED_EDGE ( 'NONE', *, *, #20611, .T. ) ;
#15672=ORIENTED_EDGE ( 'NONE', *, *, #41363, .T. ) ;
#15673=CARTESIAN_POINT ( 'NONE',  ( 10.00000000000000000, -68.27212725128254078, -31.46837873495049465 ) ) ;
#15694=EDGE_CURVE ( 'NONE', #39027, #24045, #24675, .T. ) ;
#15695=ORIENTED_EDGE ( 'NONE', *, *, #2194, .F. ) ;
#15696=DIRECTION ( 'NONE',  ( -1.000000000000000000, -0.000000000000000000, 0.000000000000000000 ) ) ;
#15728=DIRECTION ( 'NONE',  ( -1.000000000000000000, 0.000000000000000000, -0.000000000000000000 ) ) ;
#15731=DIRECTION ( 'NONE',  ( -1.000000000000000000, 0.000000000000000000, 0.000000000000000000 ) ) ;
#15738=CIRCLE ( 'NONE', #44520, 31.99999999999999645 ) ;
#15744=ORIENTED_EDGE ( 'NONE', *, *, #37519, .F. ) ;
#15745=EDGE_LOOP ( 'NONE', ( #24780, #18493, #63713, #2280 ) ) ;
#15746=CARTESIAN_POINT ( 'NONE',  ( 10.00000000000000000, -55.38113227695820484, 54.21277698773656084 ) ) ;
#15747=ORIENTED_EDGE ( 'NONE', *, *, #23583, .F. ) ;
#15750=VERTEX_POINT ( 'NONE', #66025 ) ;
#15752=ORIENTED_EDGE ( 'NONE', *, *, #44063, .F. ) ;
#15756=DIRECTION ( 'NONE',  ( -1.000000000000000000, -0.000000000000000000, -0.000000000000000000 ) ) ;
#15764=AXIS2_PLACEMENT_3D ( 'NONE', #37432, #49061, #26865 ) ;
#15769=CARTESIAN_POINT ( 'NONE',  ( 0.000000000000000000, 55.20638768913831029, -51.02545421589267960 ) ) ;
#15771=DIRECTION ( 'NONE',  ( 1.000000000000000000, 0.000000000000000000, 0.000000000000000000 ) ) ;
#15775=DIRECTION ( 'NONE',  ( 1.000000000000000000, 0.000000000000000000, 0.000000000000000000 ) ) ;
#15776=EDGE_CURVE ( 'NONE', #2169, #2136, #60750, .T. ) ;
#15782=ADVANCED_FACE ( 'NONE', ( #14875 ), #37820, .T. ) ;
#15788=EDGE_CURVE ( 'NONE', #55514, #3975, #8119, .T. ) ;
#15789=AXIS2_PLACEMENT_3D ( 'NONE', #1644, #11750, #34696 ) ;
#15818=ORIENTED_EDGE ( 'NONE', *, *, #5734, .F. ) ;
#15819=DIRECTION ( 'NONE',  ( -1.000000000000000000, 0.000000000000000000, 0.000000000000000000 ) ) ;
#15823=ORIENTED_EDGE ( 'NONE', *, *, #59180, .T. ) ;
#15849=DIRECTION ( 'NONE',  ( 0.000000000000000000, -0.8910065241883626808, -0.4539904997395568520 ) ) ;
#15856=VECTOR ( 'NONE', #43241, 1000.000000000000000 ) ;
#15860=VECTOR ( 'NONE', #34399, 1000.000000000000000 ) ;
#15871=EDGE_CURVE ( 'NONE', #9438, #47803, #24384, .T. ) ;
#15872=ADVANCED_FACE ( 'NONE', ( #5104 ), #39677, .T. ) ;
#15883=VERTEX_POINT ( 'NONE', #38925 ) ;
#15893=EDGE_CURVE ( 'NONE', #67479, #10604, #28000, .T. ) ;
#15896=VERTEX_POINT ( 'NONE', #49817 ) ;
#15900=EDGE_LOOP ( 'NONE', ( #74324, #62979, #38683, #6195 ) ) ;
#15910=AXIS2_PLACEMENT_3D ( 'NONE', #17558, #17196, #63811 ) ;
#15916=CARTESIAN_POINT ( 'NONE',  ( 10.00000000000000000, 73.72996012237440766, 14.67089635893739619 ) ) ;
#15918=DIRECTION ( 'NONE',  ( 0.000000000000000000, 0.9723699203976756689, 0.2334453638559094157 ) ) ;
#15926=ORIENTED_EDGE ( 'NONE', *, *, #5370, .F. ) ;
#15927=CARTESIAN_POINT ( 'NONE',  ( 10.00000000000000000, -71.91182617369207719, 28.89263327155721228 ) ) ;
#15932=DIRECTION ( 'NONE',  ( -1.000000000000000000, 0.000000000000000000, 0.000000000000000000 ) ) ;
#15933=DIRECTION ( 'NONE',  ( 0.000000000000000000, 0.000000000000000000, -1.000000000000000000 ) ) ;
#15934=ORIENTED_EDGE ( 'NONE', *, *, #15893, .F. ) ;
#15941=CARTESIAN_POINT ( 'NONE',  ( 10.00000000000000000, -74.65491531819111515, 23.16904090965678975 ) ) ;
#15953=DIRECTION ( 'NONE',  ( 1.000000000000000000, 0.000000000000000000, 0.000000000000000000 ) ) ;
#15956=EDGE_CURVE ( 'NONE', #39383, #34204, #46026, .T. ) ;
#15957=CIRCLE ( 'NONE', #33932, 31.99999999999999289 ) ;
#15958=EDGE_CURVE ( 'NONE', #53342, #4680, #17194, .T. ) ;
#15961=CYLINDRICAL_SURFACE ( 'NONE', #38572, 32.00000000000000000 ) ;
#15962=VERTEX_POINT ( 'NONE', #21238 ) ;
#15963=DIRECTION ( 'NONE',  ( 0.000000000000000000, 0.000000000000000000, 1.000000000000000000 ) ) ;
#15972=CARTESIAN_POINT ( 'NONE',  ( 0.000000000000000000, 0.000000000000000000, 0.000000000000000000 ) ) ;
#15975=ORIENTED_EDGE ( 'NONE', *, *, #1047, .F. ) ;
#15983=DIRECTION ( 'NONE',  ( -1.000000000000000000, -0.000000000000000000, 0.000000000000000000 ) ) ;
#15985=CARTESIAN_POINT ( 'NONE',  ( 10.00000000000000000, 0.000000000000000000, 0.000000000000000000 ) ) ;
#15994=DIRECTION ( 'NONE',  ( 0.000000000000000000, 1.000000000000000000, 0.000000000000000000 ) ) ;
#15995=AXIS2_PLACEMENT_3D ( 'NONE', #71536, #20037, #26780 ) ;
#15999=FACE_BOUND ( 'NONE', #55585, .T. ) ;
#16003=ORIENTED_EDGE ( 'NONE', *, *, #793, .F. ) ;
#16005=VERTEX_POINT ( 'NONE', #35411 ) ;
#16013=DIRECTION ( 'NONE',  ( -1.000000000000000000, 0.000000000000000000, 0.000000000000000000 ) ) ;
#16014=EDGE_CURVE ( 'NONE', #4375, #72136, #7587, .T. ) ;
#16016=CYLINDRICAL_SURFACE ( 'NONE', #58264, 32.00000000000000000 ) ;
#16024=DIRECTION ( 'NONE',  ( 0.000000000000000000, -0.8910065241883627918, -0.4539904997395570185 ) ) ;
#16033=ORIENTED_EDGE ( 'NONE', *, *, #48740, .T. ) ;
#16043=LINE ( 'NONE', #33315, #39689 ) ;
#16053=EDGE_LOOP ( 'NONE', ( #22098, #7950, #73687, #38315 ) ) ;
#16059=CIRCLE ( 'NONE', #25662, 77.49899999999999523 ) ;
#16062=EDGE_CURVE ( 'NONE', #62527, #30795, #25607, .T. ) ;
#16063=ORIENTED_EDGE ( 'NONE', *, *, #30769, .T. ) ;
#16067=AXIS2_PLACEMENT_3D ( 'NONE', #49063, #9590, #66008 ) ;
#16068=DIRECTION ( 'NONE',  ( -1.000000000000000000, 0.000000000000000000, 0.000000000000000000 ) ) ;
#16081=DIRECTION ( 'NONE',  ( -1.000000000000000000, 0.000000000000000000, 0.000000000000000000 ) ) ;
#16083=ORIENTED_EDGE ( 'NONE', *, *, #48819, .F. ) ;
#16087=CARTESIAN_POINT ( 'NONE',  ( 10.00000000000000000, 68.55367621811141987, 44.99326035066078333 ) ) ;
#16089=DIRECTION ( 'NONE',  ( -1.000000000000000000, 0.000000000000000000, -0.000000000000000000 ) ) ;
#16111=CIRCLE ( 'NONE', #43709, 31.99999999999999645 ) ;
#16112=ORIENTED_EDGE ( 'NONE', *, *, #9953, .T. ) ;
#16117=ORIENTED_EDGE ( 'NONE', *, *, #57485, .T. ) ;
#16126=CARTESIAN_POINT ( 'NONE',  ( 10.00000000000000000, 8.830959090342393125, 74.65491531819122883 ) ) ;
#16139=CARTESIAN_POINT ( 'NONE',  ( 10.00000000000000000, 0.000000000000000000, 0.000000000000000000 ) ) ;
#16140=LINE ( 'NONE', #50341, #20299 ) ;
#16145=DIRECTION ( 'NONE',  ( 0.000000000000000000, 0.000000000000000000, -1.000000000000000000 ) ) ;
#16155=EDGE_LOOP ( 'NONE', ( #22495, #39499, #39199, #4668 ) ) ;
#16158=CARTESIAN_POINT ( 'NONE',  ( 10.00000000000000000, 41.76937507738875155, -62.50329211542393892 ) ) ;
#16160=ORIENTED_EDGE ( 'NONE', *, *, #17455, .T. ) ;
#16166=AXIS2_PLACEMENT_3D ( 'NONE', #61906, #38972, #16406 ) ;
#16170=CARTESIAN_POINT ( 'NONE',  ( 5.000000000000002665, 3.894527615419058009, -81.90746397400384637 ) ) ;
#16173=CARTESIAN_POINT ( 'NONE',  ( 10.00000000000000000, -76.69515212745996280, -29.01471420065644580 ) ) ;
#16175=CARTESIAN_POINT ( 'NONE',  ( 0.000000000000000000, 68.27212725128275395, 31.46837873495001503 ) ) ;
#16177=DIRECTION ( 'NONE',  ( -1.000000000000000000, 0.000000000000000000, 0.000000000000000000 ) ) ;
#16181=CIRCLE ( 'NONE', #52200, 31.99999999999999645 ) ;
#16184=CARTESIAN_POINT ( 'NONE',  ( 0.000000000000000000, 71.87247863392414615, 39.47590169984871267 ) ) ;
#16185=ORIENTED_EDGE ( 'NONE', *, *, #25705, .F. ) ;
#16186=AXIS2_PLACEMENT_3D ( 'NONE', #39046, #3097, #14344 ) ;
#16187=EDGE_CURVE ( 'NONE', #66404, #26445, #65836, .T. ) ;
#16195=VERTEX_POINT ( 'NONE', #38371 ) ;
#16208=LINE ( 'NONE', #72590, #28454 ) ;
#16218=CARTESIAN_POINT ( 'NONE',  ( 10.00000000000000000, -33.71516098798684880, -74.74816331893465815 ) ) ;
#16221=DIRECTION ( 'NONE',  ( 0.000000000000000000, -0.5224985647159560154, 0.8526401643540879594 ) ) ;
#16225=EDGE_CURVE ( 'NONE', #31776, #45326, #29258, .T. ) ;
#16233=DIRECTION ( 'NONE',  ( 1.000000000000000000, 0.000000000000000000, 0.000000000000000000 ) ) ;
#16243=DIRECTION ( 'NONE',  ( -1.000000000000000000, 0.000000000000000000, -0.000000000000000000 ) ) ;
#16254=DIRECTION ( 'NONE',  ( -1.000000000000000000, 0.000000000000000000, -0.000000000000000000 ) ) ;
#16259=ORIENTED_EDGE ( 'NONE', *, *, #49544, .T. ) ;
#16260=AXIS2_PLACEMENT_3D ( 'NONE', #2470, #32084, #20452 ) ;
#16263=VERTEX_POINT ( 'NONE', #72198 ) ;
#16264=VERTEX_POINT ( 'NONE', #67311 ) ;
#16278=AXIS2_PLACEMENT_3D ( 'NONE', #40798, #247, #12206 ) ;
#16284=FACE_OUTER_BOUND ( 'NONE', #10940, .T. ) ;
#16297=VECTOR ( 'NONE', #1651, 1000.000000000000000 ) ;
#16306=CARTESIAN_POINT ( 'NONE',  ( 10.00000000000000000, -6.903761155837252694, -77.19088730480530103 ) ) ;
#16311=EDGE_CURVE ( 'NONE', #29474, #55514, #2891, .T. ) ;
#16327=CARTESIAN_POINT ( 'NONE',  ( 10.00000000000000000, 76.66974797899852945, -11.30684508768257679 ) ) ;
#16336=VERTEX_POINT ( 'NONE', #416 ) ;
#16339=CARTESIAN_POINT ( 'NONE',  ( 10.00000000000000178, 0.000000000000000000, 12.50000000000000000 ) ) ;
#16340=VECTOR ( 'NONE', #46715, 1000.000000000000000 ) ;
#16353=AXIS2_PLACEMENT_3D ( 'NONE', #49615, #59814, #15410 ) ;
#16360=DIRECTION ( 'NONE',  ( 0.000000000000000000, -0.7071067811865536790, 0.7071067811865414665 ) ) ;
#16368=VERTEX_POINT ( 'NONE', #52238 ) ;
#16370=AXIS2_PLACEMENT_3D ( 'NONE', #21734, #55210, #55954 ) ;
#16378=ORIENTED_EDGE ( 'NONE', *, *, #49468, .F. ) ;
#16380=VERTEX_POINT ( 'NONE', #62051 ) ;
#16385=EDGE_CURVE ( 'NONE', #32140, #58910, #52074, .T. ) ;
#16388=CIRCLE ( 'NONE', #59638, 31.99999999999999289 ) ;
#16394=ORIENTED_EDGE ( 'NONE', *, *, #72729, .F. ) ;
#16398=ORIENTED_EDGE ( 'NONE', *, *, #6972, .F. ) ;
#16402=EDGE_CURVE ( 'NONE', #73223, #60373, #4923, .T. ) ;
#16403=EDGE_CURVE ( 'NONE', #45162, #65655, #71260, .T. ) ;
#16404=DIRECTION ( 'NONE',  ( 0.000000000000000000, 0.000000000000000000, 1.000000000000000000 ) ) ;
#16405=VECTOR ( 'NONE', #59786, 1000.000000000000000 ) ;
#16406=DIRECTION ( 'NONE',  ( 0.000000000000000000, 0.000000000000000000, 1.000000000000000000 ) ) ;
#16411=ORIENTED_EDGE ( 'NONE', *, *, #60623, .T. ) ;
#16413=EDGE_CURVE ( 'NONE', #71089, #53435, #6467, .T. ) ;
#16418=DIRECTION ( 'NONE',  ( -1.000000000000000000, -0.000000000000000000, -0.000000000000000000 ) ) ;
#16435=CARTESIAN_POINT ( 'NONE',  ( 0.000000000000000000, -46.11716303203234446, 67.80270845531873647 ) ) ;
#16446=CYLINDRICAL_SURFACE ( 'NONE', #52464, 77.49899999999999523 ) ;
#16448=VECTOR ( 'NONE', #46664, 1000.000000000000000 ) ;
#16451=DIRECTION ( 'NONE',  ( -1.000000000000000000, 0.000000000000000000, -0.000000000000000000 ) ) ;
#16460=DIRECTION ( 'NONE',  ( 0.000000000000000000, 0.000000000000000000, 1.000000000000000000 ) ) ;
#16461=VECTOR ( 'NONE', #71634, 1000.000000000000000 ) ;
#16471=VERTEX_POINT ( 'NONE', #22949 ) ;
#16484=DIRECTION ( 'NONE',  ( -1.000000000000000000, 0.000000000000000000, -0.000000000000000000 ) ) ;
#16492=CARTESIAN_POINT ( 'NONE',  ( 10.00000000000000000, 73.95703589263975175, 23.16143007188454206 ) ) ;
#16505=DIRECTION ( 'NONE',  ( -1.000000000000000000, 0.000000000000000000, 0.000000000000000000 ) ) ;
#16512=DIRECTION ( 'NONE',  ( -1.000000000000000000, 0.000000000000000000, 0.000000000000000000 ) ) ;
#16519=EDGE_CURVE ( 'NONE', #36744, #9362, #70994, .T. ) ;
#16520=CARTESIAN_POINT ( 'NONE',  ( 0.000000000000000000, 0.000000000000000000, 2.500000000000000000 ) ) ;
#16523=LINE ( 'NONE', #17269, #68349 ) ;
#16527=VERTEX_POINT ( 'NONE', #31148 ) ;
#16536=ORIENTED_EDGE ( 'NONE', *, *, #40182, .T. ) ;
#16550=DIRECTION ( 'NONE',  ( 0.000000000000000000, 0.000000000000000000, 1.000000000000000000 ) ) ;
#16572=ORIENTED_EDGE ( 'NONE', *, *, #46491, .F. ) ;
#16576=DIRECTION ( 'NONE',  ( 0.000000000000000000, 0.000000000000000000, 1.000000000000000000 ) ) ;
#16584=LINE ( 'NONE', #44426, #23074 ) ;
#16585=CYLINDRICAL_SURFACE ( 'NONE', #43991, 31.99999999999999289 ) ;
#16592=FACE_OUTER_BOUND ( 'NONE', #65027, .T. ) ;
#16594=VERTEX_POINT ( 'NONE', #18385 ) ;
#16601=CIRCLE ( 'NONE', #70618, 82.00000000000000000 ) ;
#16609=CARTESIAN_POINT ( 'NONE',  ( 0.000000000000000000, 0.000000000000000000, 0.000000000000000000 ) ) ;
#16614=DIRECTION ( 'NONE',  ( -1.000000000000000000, -0.000000000000000000, 0.000000000000000000 ) ) ;
#16637=ORIENTED_EDGE ( 'NONE', *, *, #8716, .F. ) ;
#16645=EDGE_CURVE ( 'NONE', #69079, #10016, #50941, .T. ) ;
#16649=VERTEX_POINT ( 'NONE', #4460 ) ;
#16652=VERTEX_POINT ( 'NONE', #43932 ) ;
#16654=ADVANCED_FACE ( 'NONE', ( #20619 ), #9326, .T. ) ;
#16658=FACE_OUTER_BOUND ( 'NONE', #58234, .T. ) ;
#16663=FACE_OUTER_BOUND ( 'NONE', #45829, .T. ) ;
#16677=AXIS2_PLACEMENT_3D ( 'NONE', #73440, #18158, #1292 ) ;
#16681=DIRECTION ( 'NONE',  ( -1.000000000000000000, -0.000000000000000000, 0.000000000000000000 ) ) ;
#16688=AXIS2_PLACEMENT_3D ( 'NONE', #16609, #23730, #115 ) ;
#16693=DIRECTION ( 'NONE',  ( 0.000000000000000000, 0.000000000000000000, 1.000000000000000000 ) ) ;
#16696=CIRCLE ( 'NONE', #27453, 82.00000000000000000 ) ;
#16708=AXIS2_PLACEMENT_3D ( 'NONE', #48261, #25696, #19310 ) ;
#16709=CIRCLE ( 'NONE', #11864, 31.99999999999999645 ) ;
#16710=EDGE_CURVE ( 'NONE', #53528, #968, #32996, .T. ) ;
#16717=AXIS2_PLACEMENT_3D ( 'NONE', #72412, #37486, #38209 ) ;
#16720=EDGE_CURVE ( 'NONE', #19951, #62129, #55199, .T. ) ;
#16721=AXIS2_PLACEMENT_3D ( 'NONE', #14205, #70976, #53694 ) ;
#16727=VERTEX_POINT ( 'NONE', #43201 ) ;
#16739=ORIENTED_EDGE ( 'NONE', *, *, #37516, .T. ) ;
#16792=CIRCLE ( 'NONE', #33564, 31.99999999999998934 ) ;
#16807=CARTESIAN_POINT ( 'NONE',  ( 10.00000000000000000, -73.72996012237429397, -14.67089635893794508 ) ) ;
#16809=EDGE_CURVE ( 'NONE', #21165, #63343, #60845, .T. ) ;
#16813=ADVANCED_FACE ( 'NONE', ( #28105 ), #45422, .T. ) ;
#16818=CIRCLE ( 'NONE', #58844, 32.00000000000000000 ) ;
#16822=VERTEX_POINT ( 'NONE', #73221 ) ;
#16824=EDGE_CURVE ( 'NONE', #71862, #42798, #43717, .T. ) ;
#16825=ADVANCED_FACE ( 'NONE', ( #27740 ), #57430, .T. ) ;
#16829=LINE ( 'NONE', #9699, #57891 ) ;
#16830=CARTESIAN_POINT ( 'NONE',  ( 5.000000000000000000, 59.75363087400076267, 56.15606465354979804 ) ) ;
#16839=DIRECTION ( 'NONE',  ( -1.000000000000000000, -0.000000000000000000, 0.000000000000000000 ) ) ;
#16841=EDGE_CURVE ( 'NONE', #16652, #64804, #4119, .T. ) ;
#16843=CIRCLE ( 'NONE', #39656, 77.49899999999999523 ) ;
#16850=CIRCLE ( 'NONE', #46855, 31.99999999999999289 ) ;
#16872=CARTESIAN_POINT ( 'NONE',  ( 10.00000000000000000, 0.000000000000000000, 0.000000000000000000 ) ) ;
#16881=CARTESIAN_POINT ( 'NONE',  ( 5.000000000000000000, -21.60688246758642705, 79.10210256391360417 ) ) ;
#16882=CIRCLE ( 'NONE', #26471, 82.00000000000000000 ) ;
#16891=CARTESIAN_POINT ( 'NONE',  ( 5.000000000000002665, -16.65972982744991882, 80.28980883073752750 ) ) ;
#16916=EDGE_CURVE ( 'NONE', #2716, #36430, #71320, .T. ) ;
#16918=VERTEX_POINT ( 'NONE', #30686 ) ;
#16927=VERTEX_POINT ( 'NONE', #23961 ) ;
#16936=DIRECTION ( 'NONE',  ( 1.000000000000000000, 0.000000000000000000, 0.000000000000000000 ) ) ;
#16947=EDGE_LOOP ( 'NONE', ( #9249, #60396, #19798, #58328 ) ) ;
#16964=EDGE_CURVE ( 'NONE', #45506, #62606, #2954, .T. ) ;
#16970=EDGE_CURVE ( 'NONE', #30770, #73126, #47262, .T. ) ;
#16976=DIRECTION ( 'NONE',  ( -1.000000000000000000, -0.000000000000000000, -0.000000000000000000 ) ) ;
#16977=ADVANCED_FACE ( 'NONE', ( #19041 ), #6664, .T. ) ;
#16980=CIRCLE ( 'NONE', #52981, 31.99999999999999645 ) ;
#16981=DIRECTION ( 'NONE',  ( -1.000000000000000000, -0.000000000000000000, -0.000000000000000000 ) ) ;
#16988=DIRECTION ( 'NONE',  ( 0.000000000000000000, 0.000000000000000000, 1.000000000000000000 ) ) ;
#16993=CARTESIAN_POINT ( 'NONE',  ( 10.00000000000000000, 34.44570377933695227, -69.42325613327405165 ) ) ;
#16999=ORIENTED_EDGE ( 'NONE', *, *, #48698, .F. ) ;
#17004=ORIENTED_EDGE ( 'NONE', *, *, #1936, .F. ) ;
#17016=ORIENTED_EDGE ( 'NONE', *, *, #46689, .T. ) ;
#17021=FACE_OUTER_BOUND ( 'NONE', #44893, .T. ) ;
#17027=ORIENTED_EDGE ( 'NONE', *, *, #47806, .T. ) ;
#17030=LINE ( 'NONE', #74161, #28187 ) ;
#17034=CARTESIAN_POINT ( 'NONE',  ( 0.000000000000000000, 59.75363087400076267, 56.15606465354979804 ) ) ;
#17035=CARTESIAN_POINT ( 'NONE',  ( 0.000000000000000000, -59.03961581697367933, -46.53671651294010303 ) ) ;
#17043=CIRCLE ( 'NONE', #59225, 82.00000000000000000 ) ;
#17062=ADVANCED_FACE ( 'NONE', ( #48001 ), #23582, .T. ) ;
#17064=CARTESIAN_POINT ( 'NONE',  ( 0.000000000000000000, 63.18004540533027580, 44.88180994100400056 ) ) ;
#17083=DIRECTION ( 'NONE',  ( -1.000000000000000000, 0.000000000000000000, 0.000000000000000000 ) ) ;
#17100=ORIENTED_EDGE ( 'NONE', *, *, #55491, .F. ) ;
#17117=DIRECTION ( 'NONE',  ( 0.000000000000000000, -0.9723699203976789995, 0.2334453638558956212 ) ) ;
#17125=EDGE_LOOP ( 'NONE', ( #13666, #29857, #17837, #33738 ) ) ;
#17127=VERTEX_POINT ( 'NONE', #31435 ) ;
#17144=CIRCLE ( 'NONE', #18303, 82.00000000000000000 ) ;
#17179=EDGE_LOOP ( 'NONE', ( #66675, #10743, #50160, #28381 ) ) ;
#17194=CIRCLE ( 'NONE', #30379, 31.99999999999999645 ) ;
#17196=DIRECTION ( 'NONE',  ( -1.000000000000000000, -0.000000000000000000, 0.000000000000000000 ) ) ;
#17219=ORIENTED_EDGE ( 'NONE', *, *, #25725, .T. ) ;
#17224=DIRECTION ( 'NONE',  ( -1.000000000000000000, 0.000000000000000000, 0.000000000000000000 ) ) ;
#17225=ORIENTED_EDGE ( 'NONE', *, *, #31760, .T. ) ;
#17228=VERTEX_POINT ( 'NONE', #43489 ) ;
#17234=ORIENTED_EDGE ( 'NONE', *, *, #65020, .F. ) ;
#17243=CARTESIAN_POINT ( 'NONE',  ( 5.000000000000002665, 78.73519480814985627, -22.90783923731548199 ) ) ;
#17245=DIRECTION ( 'NONE',  ( 0.000000000000000000, 0.000000000000000000, 1.000000000000000000 ) ) ;
#17252=FACE_OUTER_BOUND ( 'NONE', #64578, .T. ) ;
#17254=CARTESIAN_POINT ( 'NONE',  ( 10.00000000000000000, -30.41916302227060598, -71.27951684758059514 ) ) ;
#17256=CARTESIAN_POINT ( 'NONE',  ( 10.00000000000000000, 55.20638768913831029, -51.02545421589267960 ) ) ;
#17260=CARTESIAN_POINT ( 'NONE',  ( 0.000000000000000000, -34.94270380257586339, -74.18225833017926618 ) ) ;
#17264=EDGE_CURVE ( 'NONE', #26699, #28789, #17043, .T. ) ;
#17265=EDGE_CURVE ( 'NONE', #28789, #808, #40049, .T. ) ;
#17269=CARTESIAN_POINT ( 'NONE',  ( 5.000000000000000000, -60.67117009219176538, 55.16347631943019536 ) ) ;
#17276=VERTEX_POINT ( 'NONE', #51701 ) ;
#17282=VERTEX_POINT ( 'NONE', #27266 ) ;
#17295=CARTESIAN_POINT ( 'NONE',  ( 0.000000000000000000, -75.11764819372145041, -2.946379043147127064 ) ) ;
#17320=ORIENTED_EDGE ( 'NONE', *, *, #35904, .T. ) ;
#17331=CARTESIAN_POINT ( 'NONE',  ( 10.00000000000000000, 41.76106447765580043, -62.50884508063379741 ) ) ;
#17353=AXIS2_PLACEMENT_3D ( 'NONE', #68503, #47050, #35742 ) ;
#17358=CIRCLE ( 'NONE', #43783, 82.00000000000000000 ) ;
#17359=VECTOR ( 'NONE', #49796, 1000.000000000000000 ) ;
#17360=AXIS2_PLACEMENT_3D ( 'NONE', #18805, #42498, #7904 ) ;
#17365=ORIENTED_EDGE ( 'NONE', *, *, #64006, .T. ) ;
#17387=CARTESIAN_POINT ( 'NONE',  ( 10.00000000000000000, -50.95692526931286181, -58.39081064771806240 ) ) ;
#17390=VERTEX_POINT ( 'NONE', #12939 ) ;
#17396=CYLINDRICAL_SURFACE ( 'NONE', #37813, 82.00000000000000000 ) ;
#17418=DIRECTION ( 'NONE',  ( -1.000000000000000000, 0.000000000000000000, -0.000000000000000000 ) ) ;
#17422=VERTEX_POINT ( 'NONE', #35875 ) ;
#17423=AXIS2_PLACEMENT_3D ( 'NONE', #19078, #42764, #25096 ) ;
#17426=CARTESIAN_POINT ( 'NONE',  ( 10.00000000000000000, 68.67312586194995561, 35.91791733033500122 ) ) ;
#17427=EDGE_CURVE ( 'NONE', #50699, #53610, #292, .T. ) ;
#17431=CARTESIAN_POINT ( 'NONE',  ( 10.00000000000000000, -81.34940948281344220, 10.30890764327356557 ) ) ;
#17433=EDGE_CURVE ( 'NONE', #21187, #69267, #47542, .T. ) ;
#17434=VERTEX_POINT ( 'NONE', #52063 ) ;
#17455=EDGE_CURVE ( 'NONE', #50464, #54897, #47907, .T. ) ;
#17456=CARTESIAN_POINT ( 'NONE',  ( 0.000000000000000000, 0.000000000000000000, 0.000000000000000000 ) ) ;
#17475=VECTOR ( 'NONE', #29061, 1000.000000000000000 ) ;
#17478=VERTEX_POINT ( 'NONE', #17851 ) ;
#17481=ORIENTED_EDGE ( 'NONE', *, *, #43471, .F. ) ;
#17486=CARTESIAN_POINT ( 'NONE',  ( 5.000000000000000000, 63.97538442413426907, 51.29473840253247374 ) ) ;
#17529=CARTESIAN_POINT ( 'NONE',  ( -10.00000000000000000, 0.000000000000000000, 0.000000000000000000 ) ) ;
#17530=LINE ( 'NONE', #5165, #27370 ) ;
#17532=CIRCLE ( 'NONE', #21111, 31.99999999999999289 ) ;
#17543=CARTESIAN_POINT ( 'NONE',  ( 0.000000000000000000, -50.95692526931372157, 58.39081064771733054 ) ) ;
#17546=EDGE_CURVE ( 'NONE', #26445, #44855, #13589, .T. ) ;
#17558=CARTESIAN_POINT ( 'NONE',  ( 10.00000000000000000, -62.50329211542407393, -41.76937507738853839 ) ) ;
#17559=AXIS2_PLACEMENT_3D ( 'NONE', #6781, #11668, #22982 ) ;
#17562=ORIENTED_EDGE ( 'NONE', *, *, #56033, .T. ) ;
#17563=EDGE_CURVE ( 'NONE', #18038, #70403, #19327, .T. ) ;
#17571=AXIS2_PLACEMENT_3D ( 'NONE', #54379, #3640, #55490 ) ;
#17577=ORIENTED_EDGE ( 'NONE', *, *, #23037, .F. ) ;
#17581=ORIENTED_EDGE ( 'NONE', *, *, #43340, .F. ) ;
#17601=ADVANCED_FACE ( 'NONE', ( #31348 ), #59949, .T. ) ;
#17602=CARTESIAN_POINT ( 'NONE',  ( 10.00000000000000000, 81.34940948281349904, -10.30890764327296871 ) ) ;
#17603=CARTESIAN_POINT ( 'NONE',  ( 0.000000000000000000, 16.00000000000000000, 2.500000000000000000 ) ) ;
#17606=ORIENTED_EDGE ( 'NONE', *, *, #37516, .F. ) ;
#17618=CYLINDRICAL_SURFACE ( 'NONE', #22998, 31.99999999999998579 ) ;
#17625=AXIS2_PLACEMENT_3D ( 'NONE', #41009, #35709, #51905 ) ;
#17630=AXIS2_PLACEMENT_3D ( 'NONE', #18879, #41818, #25281 ) ;
#17634=CIRCLE ( 'NONE', #22420, 82.00000000000000000 ) ;
#17648=ORIENTED_EDGE ( 'NONE', *, *, #34115, .T. ) ;
#17651=ORIENTED_EDGE ( 'NONE', *, *, #52515, .F. ) ;
#17659=ORIENTED_EDGE ( 'NONE', *, *, #33857, .F. ) ;
#17661=DIRECTION ( 'NONE',  ( 1.000000000000000000, -0.000000000000000000, -0.000000000000000000 ) ) ;
#17669=CIRCLE ( 'NONE', #27206, 77.49899999999999523 ) ;
#17670=VERTEX_POINT ( 'NONE', #37747 ) ;
#17693=ORIENTED_EDGE ( 'NONE', *, *, #28562, .F. ) ;
#17695=DIRECTION ( 'NONE',  ( 0.000000000000000000, 0.000000000000000000, 1.000000000000000000 ) ) ;
#17710=DIRECTION ( 'NONE',  ( 0.000000000000000000, -0.1564344650402381132, 0.9876883405951365491 ) ) ;
#17711=DIRECTION ( 'NONE',  ( 0.000000000000000000, -0.9723699203976740035, -0.2334453638559161881 ) ) ;
#17726=EDGE_CURVE ( 'NONE', #70845, #61965, #42543, .T. ) ;
#17737=EDGE_LOOP ( 'NONE', ( #73718, #34304, #47330, #54382 ) ) ;
#17740=VERTEX_POINT ( 'NONE', #73037 ) ;
#17741=CIRCLE ( 'NONE', #58587, 31.99999999999999645 ) ;
#17743=ORIENTED_EDGE ( 'NONE', *, *, #60536, .T. ) ;
#17747=EDGE_CURVE ( 'NONE', #55747, #32327, #25689, .T. ) ;
#17764=DIRECTION ( 'NONE',  ( 1.000000000000000000, 0.000000000000000000, 0.000000000000000000 ) ) ;
#17774=CARTESIAN_POINT ( 'NONE',  ( 0.000000000000000000, -46.11716303203136391, -67.80270845531939017 ) ) ;
#17777=CIRCLE ( 'NONE', #59809, 31.99999999999999645 ) ;
#17783=AXIS2_PLACEMENT_3D ( 'NONE', #14825, #37776, #60709 ) ;
#17795=AXIS2_PLACEMENT_3D ( 'NONE', #73685, #28945, #39874 ) ;
#17797=CARTESIAN_POINT ( 'NONE',  ( 10.00000000000000000, -75.16055320797043748, 18.89407956138229494 ) ) ;
#17805=ADVANCED_FACE ( 'NONE', ( #16284 ), #49742, .T. ) ;
#17813=CARTESIAN_POINT ( 'NONE',  ( 0.000000000000000000, -55.19960302592029677, -51.03279382321147750 ) ) ;
#17819=DIRECTION ( 'NONE',  ( -1.000000000000000000, -0.000000000000000000, 0.000000000000000000 ) ) ;
#17826=AXIS2_PLACEMENT_3D ( 'NONE', #9109, #30920, #71880 ) ;
#17828=DIRECTION ( 'NONE',  ( -1.000000000000000000, 0.000000000000000000, 0.000000000000000000 ) ) ;
#17835=ADVANCED_FACE ( 'NONE', ( #53094 ), #51975, .T. ) ;
#17837=ORIENTED_EDGE ( 'NONE', *, *, #72162, .T. ) ;
#17843=EDGE_LOOP ( 'NONE', ( #29594, #47996, #64349, #25770 ) ) ;
#17845=ORIENTED_EDGE ( 'NONE', *, *, #7054, .T. ) ;
#17851=CARTESIAN_POINT ( 'NONE',  ( 0.000000000000000000, -5.256550761632340141, -77.32052557432847095 ) ) ;
#17873=CARTESIAN_POINT ( 'NONE',  ( 10.00000000000000000, -80.55351364060599906, 15.33399622253456940 ) ) ;
#17876=VERTEX_POINT ( 'NONE', #1634 ) ;
#17884=ORIENTED_EDGE ( 'NONE', *, *, #25407, .T. ) ;
#17905=AXIS2_PLACEMENT_3D ( 'NONE', #25180, #13879, #36818 ) ;
#17916=CIRCLE ( 'NONE', #21494, 77.49899999999999523 ) ;
#17927=CARTESIAN_POINT ( 'NONE',  ( 10.00000000000000000, -74.65374052328654386, 8.840884882374837161 ) ) ;
#17929=LINE ( 'NONE', #12650, #3910 ) ;
#17936=ORIENTED_EDGE ( 'NONE', *, *, #41577, .F. ) ;
#17951=DIRECTION ( 'NONE',  ( -1.000000000000000000, 0.000000000000000000, 0.000000000000000000 ) ) ;
#17955=EDGE_LOOP ( 'NONE', ( #57031, #48737, #67294, #35434 ) ) ;
#17957=CARTESIAN_POINT ( 'NONE',  ( 10.00000000000000000, 24.73286445877703699, 73.44644590900070114 ) ) ;
#17958=AXIS2_PLACEMENT_3D ( 'NONE', #31541, #54484, #37576 ) ;
#17967=ORIENTED_EDGE ( 'NONE', *, *, #20573, .T. ) ;
#17971=ORIENTED_EDGE ( 'NONE', *, *, #6556, .T. ) ;
#17979=ORIENTED_EDGE ( 'NONE', *, *, #49533, .T. ) ;
#17984=DIRECTION ( 'NONE',  ( -1.000000000000000000, -0.000000000000000000, -0.000000000000000000 ) ) ;
#17994=EDGE_CURVE ( 'NONE', #58503, #4038, #30505, .T. ) ;
#17995=CYLINDRICAL_SURFACE ( 'NONE', #34929, 77.49899999999999523 ) ;
#17996=CIRCLE ( 'NONE', #21631, 82.00000000000000000 ) ;
#18002=ORIENTED_EDGE ( 'NONE', *, *, #30449, .F. ) ;
#18004=ADVANCED_FACE ( 'NONE', ( #10092 ), #44697, .T. ) ;
#18019=EDGE_CURVE ( 'NONE', #10962, #59827, #40197, .T. ) ;
#18020=CARTESIAN_POINT ( 'NONE',  ( 10.00000000000000000, 0.000000000000000000, 0.000000000000000000 ) ) ;
#18021=ORIENTED_EDGE ( 'NONE', *, *, #4124, .T. ) ;
#18035=CARTESIAN_POINT ( 'NONE',  ( 0.000000000000000000, 0.000000000000000000, 0.000000000000000000 ) ) ;
#18038=VERTEX_POINT ( 'NONE', #54570 ) ;
#18045=VECTOR ( 'NONE', #18715, 1000.000000000000000 ) ;
#18047=PRESENTATION_STYLE_ASSIGNMENT (( #24072 ) ) ;
#18048=ORIENTED_EDGE ( 'NONE', *, *, #56789, .F. ) ;
#18050=AXIS2_PLACEMENT_3D ( 'NONE', #41563, #64504, #12979 ) ;
#18054=VECTOR ( 'NONE', #60861, 1000.000000000000000 ) ;
#18056=DIRECTION ( 'NONE',  ( 1.000000000000000000, 0.000000000000000000, 0.000000000000000000 ) ) ;
#18059=ORIENTED_EDGE ( 'NONE', *, *, #60727, .T. ) ;
#18067=CARTESIAN_POINT ( 'NONE',  ( 5.000000000000002665, 71.87247863392414615, 39.47590169984871267 ) ) ;
#18070=AXIS2_PLACEMENT_3D ( 'NONE', #33303, #5514, #56258 ) ;
#18071=CARTESIAN_POINT ( 'NONE',  ( 0.000000000000000000, 0.000000000000000000, 0.000000000000000000 ) ) ;
#18083=DIRECTION ( 'NONE',  ( -1.000000000000000000, 0.000000000000000000, -0.000000000000000000 ) ) ;
#18090=DIRECTION ( 'NONE',  ( -1.000000000000000000, -0.000000000000000000, -0.000000000000000000 ) ) ;
#18096=ORIENTED_EDGE ( 'NONE', *, *, #17427, .T. ) ;
#18100=CARTESIAN_POINT ( 'NONE',  ( 0.000000000000000000, 2.543863470248389103, 81.96053171279903893 ) ) ;
#18105=EDGE_CURVE ( 'NONE', #64362, #21174, #63027, .T. ) ;
#18118=VERTEX_POINT ( 'NONE', #34139 ) ;
#18126=DIRECTION ( 'NONE',  ( 0.000000000000000000, -1.000000000000000000, -0.000000000000000000 ) ) ;
#18133=ORIENTED_EDGE ( 'NONE', *, *, #66239, .F. ) ;
#18140=CARTESIAN_POINT ( 'NONE',  ( 5.000000000000002665, 80.28980883073758434, 16.65972982744963460 ) ) ;
#18146=CARTESIAN_POINT ( 'NONE',  ( 10.00000000000000000, -55.19960302592029677, -51.03279382321147750 ) ) ;
#18148=CARTESIAN_POINT ( 'NONE',  ( 10.00000000000000000, 76.41127070299292257, -12.93880638057232346 ) ) ;
#18158=DIRECTION ( 'NONE',  ( -1.000000000000000000, 0.000000000000000000, -0.000000000000000000 ) ) ;
#18163=EDGE_CURVE ( 'NONE', #23521, #67020, #623, .T. ) ;
#18168=CARTESIAN_POINT ( 'NONE',  ( 10.00000000000000000, -64.81221759200306565, -50.23322058963418613 ) ) ;
#18190=CARTESIAN_POINT ( 'NONE',  ( 5.000000000000002665, 16.65972982744934683, 80.28980883073764119 ) ) ;
#18191=EDGE_CURVE ( 'NONE', #23472, #31131, #28161, .T. ) ;
#18199=ORIENTED_EDGE ( 'NONE', *, *, #17265, .T. ) ;
#18201=DIRECTION ( 'NONE',  ( -1.000000000000000000, 0.000000000000000000, -0.000000000000000000 ) ) ;
#18208=AXIS2_PLACEMENT_3D ( 'NONE', #46169, #24342, #34887 ) ;
#18214=ORIENTED_EDGE ( 'NONE', *, *, #30146, .T. ) ;
#18217=ORIENTED_EDGE ( 'NONE', *, *, #26924, .T. ) ;
#18224=DIRECTION ( 'NONE',  ( -1.000000000000000000, 0.000000000000000000, -0.000000000000000000 ) ) ;
#18229=CARTESIAN_POINT ( 'NONE',  ( 0.000000000000000000, -73.73191006444582740, 14.66109333815435889 ) ) ;
#18244=ORIENTED_EDGE ( 'NONE', *, *, #33938, .T. ) ;
#18248=EDGE_CURVE ( 'NONE', #7152, #32052, #7766, .T. ) ;
#18258=DIRECTION ( 'NONE',  ( 1.000000000000000000, 0.000000000000000000, 0.000000000000000000 ) ) ;
#18265=CARTESIAN_POINT ( 'NONE',  ( 10.00000000000000000, 70.52718814184260054, 26.02418014898334420 ) ) ;
#18286=ORIENTED_EDGE ( 'NONE', *, *, #51928, .T. ) ;
#18303=AXIS2_PLACEMENT_3D ( 'NONE', #36225, #36594, #25329 ) ;
#18315=EDGE_LOOP ( 'NONE', ( #41329, #1462, #61379, #11004 ) ) ;
#18317=ORIENTED_EDGE ( 'NONE', *, *, #57732, .T. ) ;
#18328=CIRCLE ( 'NONE', #57987, 31.99999999999999645 ) ;
#18336=ORIENTED_EDGE ( 'NONE', *, *, #51082, .T. ) ;
#18338=ORIENTED_EDGE ( 'NONE', *, *, #58926, .F. ) ;
#18353=EDGE_CURVE ( 'NONE', #65113, #28369, #41267, .T. ) ;
#18355=CARTESIAN_POINT ( 'NONE',  ( 0.000000000000000000, -58.39081064771713869, -50.95692526931392052 ) ) ;
#18364=DIRECTION ( 'NONE',  ( 0.000000000000000000, 0.4539904997395476927, -0.8910065241883674547 ) ) ;
#18366=DIRECTION ( 'NONE',  ( -1.000000000000000000, -0.000000000000000000, -0.000000000000000000 ) ) ;
#18367=DIRECTION ( 'NONE',  ( 0.000000000000000000, 0.000000000000000000, 1.000000000000000000 ) ) ;
#18385=CARTESIAN_POINT ( 'NONE',  ( 0.000000000000000000, 1.530808498934191521E-15, -12.50000000000000000 ) ) ;
#18387=ORIENTED_EDGE ( 'NONE', *, *, #31715, .F. ) ;
#18388=DIRECTION ( 'NONE',  ( -1.000000000000000000, 0.000000000000000000, -0.000000000000000000 ) ) ;
#18395=AXIS2_PLACEMENT_3D ( 'NONE', #26206, #72437, #15300 ) ;
#18399=ORIENTED_EDGE ( 'NONE', *, *, #51550, .F. ) ;
#18411=VERTEX_POINT ( 'NONE', #42009 ) ;
#18417=DIRECTION ( 'NONE',  ( -1.000000000000000000, -0.000000000000000000, -0.000000000000000000 ) ) ;
#18418=VECTOR ( 'NONE', #70516, 1000.000000000000000 ) ;
#18427=CARTESIAN_POINT ( 'NONE',  ( 10.00000000000000000, 68.27212725128275395, -31.46837873495001503 ) ) ;
#18431=AXIS2_PLACEMENT_3D ( 'NONE', #49511, #72433, #20936 ) ;
#18436=CARTESIAN_POINT ( 'NONE',  ( 0.000000000000000000, 0.000000000000000000, 0.000000000000000000 ) ) ;
#18438=EDGE_CURVE ( 'NONE', #58910, #57911, #27284, .T. ) ;
#18440=DIRECTION ( 'NONE',  ( 0.000000000000000000, -0.6494480483301903195, 0.7604059656000252687 ) ) ;
#18445=DIRECTION ( 'NONE',  ( 0.000000000000000000, 0.000000000000000000, 1.000000000000000000 ) ) ;
#18452=AXIS2_PLACEMENT_3D ( 'NONE', #25759, #30643, #1397 ) ;
#18453=ORIENTED_EDGE ( 'NONE', *, *, #72287, .F. ) ;
#18456=CARTESIAN_POINT ( 'NONE',  ( 0.000000000000000000, 14.67089635893713684, 73.72996012237443608 ) ) ;
#18476=ORIENTED_EDGE ( 'NONE', *, *, #46671, .T. ) ;
#18478=EDGE_CURVE ( 'NONE', #19205, #57325, #24620, .T. ) ;
#18482=EDGE_CURVE ( 'NONE', #42263, #65194, #53431, .T. ) ;
#18484=CARTESIAN_POINT ( 'NONE',  ( -10.00000000000000000, 0.000000000000000000, 0.000000000000000000 ) ) ;
#18488=ORIENTED_EDGE ( 'NONE', *, *, #65963, .T. ) ;
#18493=ORIENTED_EDGE ( 'NONE', *, *, #71995, .T. ) ;
#18497=CARTESIAN_POINT ( 'NONE',  ( 10.00000000000000000, 0.000000000000000000, 0.000000000000000000 ) ) ;
#18498=DIRECTION ( 'NONE',  ( -1.000000000000000000, 0.000000000000000000, 0.000000000000000000 ) ) ;
#18510=LINE ( 'NONE', #18148, #63840 ) ;
#18515=CARTESIAN_POINT ( 'NONE',  ( 5.000000000000002665, -80.28980883073747066, -16.65972982745018172 ) ) ;
#18521=VECTOR ( 'NONE', #9800, 1000.000000000000000 ) ;
#18533=ORIENTED_EDGE ( 'NONE', *, *, #35725, .T. ) ;
#18534=FACE_OUTER_BOUND ( 'NONE', #25258, .T. ) ;
#18539=FACE_OUTER_BOUND ( 'NONE', #21260, .T. ) ;
#18544=CIRCLE ( 'NONE', #60575, 82.00000000000000000 ) ;
#18545=DIRECTION ( 'NONE',  ( 0.000000000000000000, 0.000000000000000000, -1.000000000000000000 ) ) ;
#18547=CARTESIAN_POINT ( 'NONE',  ( 0.000000000000000000, -41.76937507738745836, -62.50329211542482710 ) ) ;
#18553=CARTESIAN_POINT ( 'NONE',  ( 0.000000000000000000, 54.21277698773675979, 55.38113227695801299 ) ) ;
#18557=ORIENTED_EDGE ( 'NONE', *, *, #26560, .F. ) ;
#18558=CYLINDRICAL_SURFACE ( 'NONE', #6704, 77.49899999999999523 ) ;
#18574=VECTOR ( 'NONE', #64706, 1000.000000000000000 ) ;
#18580=ORIENTED_EDGE ( 'NONE', *, *, #12819, .F. ) ;
#18592=CARTESIAN_POINT ( 'NONE',  ( 10.00000000000000000, -11.30684508768395524, 76.66974797899831628 ) ) ;
#18595=VERTEX_POINT ( 'NONE', #46084 ) ;
#18611=CIRCLE ( 'NONE', #18649, 31.99999999999998934 ) ;
#18625=DIRECTION ( 'NONE',  ( -1.000000000000000000, 0.000000000000000000, -0.000000000000000000 ) ) ;
#18643=ORIENTED_EDGE ( 'NONE', *, *, #57470, .F. ) ;
#18645=ORIENTED_EDGE ( 'NONE', *, *, #33530, .T. ) ;
#18649=AXIS2_PLACEMENT_3D ( 'NONE', #13720, #36286, #59987 ) ;
#18651=ORIENTED_EDGE ( 'NONE', *, *, #30135, .F. ) ;
#18655=CARTESIAN_POINT ( 'NONE',  ( 10.00000000000000000, -81.50828551894232987, 8.966570791700396725 ) ) ;
#18656=DIRECTION ( 'NONE',  ( -1.000000000000000000, 0.000000000000000000, 0.000000000000000000 ) ) ;
#18658=DIRECTION ( 'NONE',  ( -1.000000000000000000, -0.000000000000000000, -0.000000000000000000 ) ) ;
#18659=ADVANCED_FACE ( 'NONE', ( #73151 ), #16016, .T. ) ;
#18660=CYLINDRICAL_SURFACE ( 'NONE', #12962, 82.00000000000000000 ) ;
#18668=CARTESIAN_POINT ( 'NONE',  ( 10.00000000000000000, 0.000000000000000000, 0.000000000000000000 ) ) ;
#18672=EDGE_CURVE ( 'NONE', #19363, #33442, #51719, .T. ) ;
#18682=ORIENTED_EDGE ( 'NONE', *, *, #49704, .F. ) ;
#18685=DIRECTION ( 'NONE',  ( -1.000000000000000000, 0.000000000000000000, 0.000000000000000000 ) ) ;
#18693=ORIENTED_EDGE ( 'NONE', *, *, #22703, .T. ) ;
#18694=ORIENTED_EDGE ( 'NONE', *, *, #42771, .F. ) ;
#18696=DIRECTION ( 'NONE',  ( 0.000000000000000000, -0.7604059656000368150, 0.6494480483301767748 ) ) ;
#18698=VECTOR ( 'NONE', #69298, 1000.000000000000000 ) ;
#18701=EDGE_LOOP ( 'NONE', ( #63607, #5987, #39483, #5834 ) ) ;
#18705=DIRECTION ( 'NONE',  ( -1.000000000000000000, 0.000000000000000000, 0.000000000000000000 ) ) ;
#18709=DIRECTION ( 'NONE',  ( -1.000000000000000000, -0.000000000000000000, 0.000000000000000000 ) ) ;
#18710=VECTOR ( 'NONE', #2796, 1000.000000000000000 ) ;
#18711=CARTESIAN_POINT ( 'NONE',  ( 10.00000000000000000, 51.02545421589324803, 55.20638768913779870 ) ) ;
#18714=CARTESIAN_POINT ( 'NONE',  ( 10.00000000000000000, -20.41045688087876897, 72.35160999960810102 ) ) ;
#18715=DIRECTION ( 'NONE',  ( -1.000000000000000000, 0.000000000000000000, -0.000000000000000000 ) ) ;
#18732=CYLINDRICAL_SURFACE ( 'NONE', #10701, 82.00000000000000000 ) ;
#18736=CIRCLE ( 'NONE', #72773, 31.99999999999999289 ) ;
#18737=EDGE_CURVE ( 'NONE', #43844, #10067, #23892, .T. ) ;
#18757=ORIENTED_EDGE ( 'NONE', *, *, #67886, .T. ) ;
#18761=EDGE_CURVE ( 'NONE', #1076, #48015, #59208, .T. ) ;
#18763=CARTESIAN_POINT ( 'NONE',  ( 0.000000000000000000, 46.54456581323888997, -59.03342792756214408 ) ) ;
#18765=CARTESIAN_POINT ( 'NONE',  ( 10.00000000000000000, 51.29473840253223926, 63.97538442413446091 ) ) ;
#18769=ORIENTED_EDGE ( 'NONE', *, *, #31985, .T. ) ;
#18776=ORIENTED_EDGE ( 'NONE', *, *, #65667, .T. ) ;
#18780=ORIENTED_EDGE ( 'NONE', *, *, #12987, .F. ) ;
#18782=DIRECTION ( 'NONE',  ( 0.000000000000000000, 0.000000000000000000, 1.000000000000000000 ) ) ;
#18795=FACE_OUTER_BOUND ( 'NONE', #48475, .T. ) ;
#18804=AXIS2_PLACEMENT_3D ( 'NONE', #51834, #23271, #69138 ) ;
#18805=CARTESIAN_POINT ( 'NONE',  ( 0.000000000000000000, 0.000000000000000000, 0.000000000000000000 ) ) ;
#18808=DIRECTION ( 'NONE',  ( -1.000000000000000000, 0.000000000000000000, 0.000000000000000000 ) ) ;
#18809=DIRECTION ( 'NONE',  ( -1.000000000000000000, 0.000000000000000000, 0.000000000000000000 ) ) ;
#18813=ADVANCED_FACE ( 'NONE', ( #47557 ), #58460, .T. ) ;
#18819=FACE_OUTER_BOUND ( 'NONE', #38095, .T. ) ;
#18822=CARTESIAN_POINT ( 'NONE',  ( 5.000000000000000000, 68.55367621811141987, 44.99326035066078333 ) ) ;
#18834=VERTEX_POINT ( 'NONE', #19344 ) ;
#18852=CARTESIAN_POINT ( 'NONE',  ( 5.000000000000000000, -46.11716303203234446, 67.80270845531873647 ) ) ;
#18872=EDGE_LOOP ( 'NONE', ( #2706, #20154, #9732, #272 ) ) ;
#18876=CARTESIAN_POINT ( 'NONE',  ( 5.000000000000000000, -33.71516098798685590, -74.74816331893465815 ) ) ;
#18877=DIRECTION ( 'NONE',  ( -1.000000000000000000, -0.000000000000000000, -0.000000000000000000 ) ) ;
#18879=CARTESIAN_POINT ( 'NONE',  ( 10.00000000000000000, 51.03279382321166224, -55.19960302592011914 ) ) ;
#18881=DIRECTION ( 'NONE',  ( -1.000000000000000000, -0.000000000000000000, -0.000000000000000000 ) ) ;
#18882=FACE_OUTER_BOUND ( 'NONE', #10558, .T. ) ;
#18906=EDGE_CURVE ( 'NONE', #15896, #34394, #41474, .T. ) ;
#18921=AXIS2_PLACEMENT_3D ( 'NONE', #32446, #22289, #62146 ) ;
#18927=ADVANCED_FACE ( 'NONE', ( #8813 ), #8451, .T. ) ;
#18928=ORIENTED_EDGE ( 'NONE', *, *, #18482, .F. ) ;
#18930=EDGE_CURVE ( 'NONE', #46225, #69079, #39106, .T. ) ;
#18935=EDGE_CURVE ( 'NONE', #55001, #2989, #38497, .T. ) ;
#18944=CIRCLE ( 'NONE', #60980, 32.00000000000000000 ) ;
#18975=CIRCLE ( 'NONE', #39449, 31.99999999999999289 ) ;
#18976=VECTOR ( 'NONE', #72254, 1000.000000000000000 ) ;
#18985=CARTESIAN_POINT ( 'NONE',  ( 10.00000000000000000, 0.000000000000000000, 0.000000000000000000 ) ) ;
#18986=CARTESIAN_POINT ( 'NONE',  ( 10.00000000000000000, -26.01480285779785362, -70.53064760720343429 ) ) ;
#18987=EDGE_CURVE ( 'NONE', #35888, #43637, #3936, .T. ) ;
#18989=CARTESIAN_POINT ( 'NONE',  ( 5.000000000000002665, -81.96053171279901051, -2.543863470249246195 ) ) ;
#18998=VECTOR ( 'NONE', #31433, 1000.000000000000000 ) ;
#19000=AXIS2_PLACEMENT_3D ( 'NONE', #73457, #23093, #21963 ) ;
#19009=CIRCLE ( 'NONE', #61037, 82.00000000000000000 ) ;
#19013=EDGE_LOOP ( 'NONE', ( #31689, #36309, #13296, #45215 ) ) ;
#19017=CYLINDRICAL_SURFACE ( 'NONE', #42987, 77.49899999999999523 ) ;
#19019=EDGE_CURVE ( 'NONE', #38362, #21255, #66345, .T. ) ;
#19021=AXIS2_PLACEMENT_3D ( 'NONE', #53081, #71087, #1256 ) ;
#19031=CARTESIAN_POINT ( 'NONE',  ( 10.00000000000000000, 75.11725578898472122, -2.956366410619845730 ) ) ;
#19033=DIRECTION ( 'NONE',  ( 1.000000000000000000, -0.000000000000000000, -0.000000000000000000 ) ) ;
#19035=EDGE_LOOP ( 'NONE', ( #43775, #52289, #73779, #50401 ) ) ;
#19036=ORIENTED_EDGE ( 'NONE', *, *, #40981, .F. ) ;
#19041=FACE_OUTER_BOUND ( 'NONE', #63553, .T. ) ;
#19045=DIRECTION ( 'NONE',  ( -1.000000000000000000, 0.000000000000000000, 0.000000000000000000 ) ) ;
#19056=VECTOR ( 'NONE', #49329, 1000.000000000000000 ) ;
#19061=ORIENTED_EDGE ( 'NONE', *, *, #29963, .T. ) ;
#19062=DIRECTION ( 'NONE',  ( -1.000000000000000000, 0.000000000000000000, 0.000000000000000000 ) ) ;
#19072=VERTEX_POINT ( 'NONE', #74184 ) ;
#19075=VECTOR ( 'NONE', #70379, 1000.000000000000000 ) ;
#19078=CARTESIAN_POINT ( 'NONE',  ( 0.000000000000000000, 31.47745569255140552, 68.26794271651274926 ) ) ;
#19080=AXIS2_PLACEMENT_3D ( 'NONE', #51508, #62, #45892 ) ;
#19088=VECTOR ( 'NONE', #30033, 1000.000000000000000 ) ;
#19090=VECTOR ( 'NONE', #39178, 1000.000000000000000 ) ;
#19092=ADVANCED_FACE ( 'NONE', ( #179 ), #44888, .T. ) ;
#19105=ORIENTED_EDGE ( 'NONE', *, *, #32566, .T. ) ;
#19108=CYLINDRICAL_SURFACE ( 'NONE', #61163, 12.50000000000000000 ) ;
#19112=FACE_OUTER_BOUND ( 'NONE', #7037, .T. ) ;
#19114=EDGE_CURVE ( 'NONE', #70845, #25521, #33211, .T. ) ;
#19129=ORIENTED_EDGE ( 'NONE', *, *, #22169, .T. ) ;
#19131=CYLINDRICAL_SURFACE ( 'NONE', #60976, 82.00000000000000000 ) ;
#19141=DIRECTION ( 'NONE',  ( -1.000000000000000000, -0.000000000000000000, -0.000000000000000000 ) ) ;
#19143=ORIENTED_EDGE ( 'NONE', *, *, #22939, .F. ) ;
#19159=CARTESIAN_POINT ( 'NONE',  ( 10.00000000000000000, -73.73191006444582740, 14.66109333815435889 ) ) ;
#19171=VECTOR ( 'NONE', #35438, 1000.000000000000000 ) ;
#19175=DIRECTION ( 'NONE',  ( 0.000000000000000000, 0.000000000000000000, 1.000000000000000000 ) ) ;
#19176=VECTOR ( 'NONE', #30575, 1000.000000000000000 ) ;
#19177=DIRECTION ( 'NONE',  ( 0.000000000000000000, 0.3090169943749482839, -0.9510565162951533091 ) ) ;
#19182=DIRECTION ( 'NONE',  ( 1.000000000000000000, 0.000000000000000000, 0.000000000000000000 ) ) ;
#19185=CARTESIAN_POINT ( 'NONE',  ( 0.000000000000000000, 0.000000000000000000, 0.000000000000000000 ) ) ;
#19186=AXIS2_PLACEMENT_3D ( 'NONE', #72777, #14166, #38598 ) ;
#19187=CYLINDRICAL_SURFACE ( 'NONE', #6478, 32.00000000000000000 ) ;
#19190=DIRECTION ( 'NONE',  ( -1.000000000000000000, 0.000000000000000000, -0.000000000000000000 ) ) ;
#19192=CARTESIAN_POINT ( 'NONE',  ( 0.000000000000000000, -16.65972982744991882, 80.28980883073752750 ) ) ;
#19195=AXIS2_PLACEMENT_3D ( 'NONE', #2968, #66103, #71709 ) ;
#19199=VERTEX_POINT ( 'NONE', #11041 ) ;
#19203=CARTESIAN_POINT ( 'NONE',  ( 10.00000000000000000, 77.49459641780886443, -0.8261519478433788644 ) ) ;
#19205=VERTEX_POINT ( 'NONE', #28314 ) ;
#19218=ORIENTED_EDGE ( 'NONE', *, *, #15788, .T. ) ;
#19220=AXIS2_PLACEMENT_3D ( 'NONE', #43220, #49198, #72128 ) ;
#19224=VERTEX_POINT ( 'NONE', #51988 ) ;
#19226=VERTEX_POINT ( 'NONE', #63667 ) ;
#19227=DIRECTION ( 'NONE',  ( -1.000000000000000000, -0.000000000000000000, -0.000000000000000000 ) ) ;
#19228=VERTEX_POINT ( 'NONE', #41457 ) ;
#19229=EDGE_CURVE ( 'NONE', #45970, #32140, #6513, .T. ) ;
#19231=ORIENTED_EDGE ( 'NONE', *, *, #40951, .T. ) ;
#19237=LINE ( 'NONE', #70353, #55784 ) ;
#19253=CARTESIAN_POINT ( 'NONE',  ( 10.00000000000000000, -5.256550761633413060, 77.32052557432841411 ) ) ;
#19255=CARTESIAN_POINT ( 'NONE',  ( 0.000000000000000000, -74.65491531819124305, 8.830959090342128448 ) ) ;
#19264=DIRECTION ( 'NONE',  ( -1.000000000000000000, -0.000000000000000000, 0.000000000000000000 ) ) ;
#19271=DIRECTION ( 'NONE',  ( 0.000000000000000000, 0.000000000000000000, 1.000000000000000000 ) ) ;
#19272=EDGE_CURVE ( 'NONE', #30261, #10249, #23432, .T. ) ;
#19284=EDGE_CURVE ( 'NONE', #59685, #5395, #22256, .T. ) ;
#19288=DIRECTION ( 'NONE',  ( -1.000000000000000000, 0.000000000000000000, 0.000000000000000000 ) ) ;
#19290=DIRECTION ( 'NONE',  ( -1.000000000000000000, -0.000000000000000000, -0.000000000000000000 ) ) ;
#19298=FACE_OUTER_BOUND ( 'NONE', #65101, .T. ) ;
#19301=CARTESIAN_POINT ( 'NONE',  ( 10.00000000000000000, 0.000000000000000000, 0.000000000000000000 ) ) ;
#19304=CARTESIAN_POINT ( 'NONE',  ( 10.00000000000000000, 50.95692526931328104, 58.39081064771769292 ) ) ;
#19306=DIRECTION ( 'NONE',  ( -1.000000000000000000, 0.000000000000000000, 0.000000000000000000 ) ) ;
#19310=DIRECTION ( 'NONE',  ( 0.000000000000000000, 0.5877852522924684742, 0.8090169943749506709 ) ) ;
#19322=CIRCLE ( 'NONE', #33721, 31.99999999999998579 ) ;
#19327=LINE ( 'NONE', #71568, #73714 ) ;
#19329=ADVANCED_FACE ( 'NONE', ( #6155 ), #35079, .T. ) ;
#19333=EDGE_CURVE ( 'NONE', #6059, #35621, #60697, .T. ) ;
#19339=CARTESIAN_POINT ( 'NONE',  ( 0.000000000000000000, -36.72794159290288718, 65.59268652807197952 ) ) ;
#19344=CARTESIAN_POINT ( 'NONE',  ( 10.00000000000000000, -34.44570377933549565, -69.42325613327476219 ) ) ;
#19345=EDGE_CURVE ( 'NONE', #21124, #53528, #63133, .T. ) ;
#19357=DIRECTION ( 'NONE',  ( -1.000000000000000000, 0.000000000000000000, 0.000000000000000000 ) ) ;
#19363=VERTEX_POINT ( 'NONE', #908 ) ;
#19365=CYLINDRICAL_SURFACE ( 'NONE', #65474, 31.99999999999999289 ) ;
#19367=LINE ( 'NONE', #18989, #50019 ) ;
#19370=DIRECTION ( 'NONE',  ( -1.000000000000000000, 0.000000000000000000, 0.000000000000000000 ) ) ;
#19384=CIRCLE ( 'NONE', #38609, 32.00000000000000000 ) ;
#19392=CARTESIAN_POINT ( 'NONE',  ( 10.00000000000000000, 74.65491531819118620, -8.830959090342659579 ) ) ;
#19403=CARTESIAN_POINT ( 'NONE',  ( 10.00000000000000000, 55.20638768913760686, 51.02545421589343988 ) ) ;
#19409=ORIENTED_EDGE ( 'NONE', *, *, #51082, .F. ) ;
#19432=CARTESIAN_POINT ( 'NONE',  ( 10.00000000000000000, 75.11764819372149304, 29.05362095685338986 ) ) ;
#19438=CARTESIAN_POINT ( 'NONE',  ( 10.00000000000000000, -63.18004540533059554, 44.88180994100355292 ) ) ;
#19448=LINE ( 'NONE', #3305, #52239 ) ;
#19458=CARTESIAN_POINT ( 'NONE',  ( 0.000000000000000000, 73.95703589264006439, -23.16143007188350822 ) ) ;
#19460=CYLINDRICAL_SURFACE ( 'NONE', #50809, 77.49899999999999523 ) ;
#19462=CYLINDRICAL_SURFACE ( 'NONE', #9879, 31.99999999999999289 ) ;
#19473=DIRECTION ( 'NONE',  ( 0.000000000000000000, 0.000000000000000000, -1.000000000000000000 ) ) ;
#19480=AXIS2_PLACEMENT_3D ( 'NONE', #35903, #59217, #17245 ) ;
#19482=ORIENTED_EDGE ( 'NONE', *, *, #7259, .T. ) ;
#19484=CIRCLE ( 'NONE', #29155, 32.00000000000000000 ) ;
#19527=ORIENTED_EDGE ( 'NONE', *, *, #4268, .T. ) ;
#19530=ORIENTED_EDGE ( 'NONE', *, *, #42382, .F. ) ;
#19533=CARTESIAN_POINT ( 'NONE',  ( 10.00000000000000000, -68.26794271651239399, -31.47745569255214093 ) ) ;
#19540=DIRECTION ( 'NONE',  ( 0.000000000000000000, 0.000000000000000000, 1.000000000000000000 ) ) ;
#19569=AXIS2_PLACEMENT_3D ( 'NONE', #70485, #53971, #25395 ) ;
#19581=AXIS2_PLACEMENT_3D ( 'NONE', #32235, #65372, #42803 ) ;
#19582=ORIENTED_EDGE ( 'NONE', *, *, #4422, .T. ) ;
#19588=CARTESIAN_POINT ( 'NONE',  ( 10.00000000000000000, -72.35160999960801576, -20.41045688087902121 ) ) ;
#19599=ORIENTED_EDGE ( 'NONE', *, *, #51162, .T. ) ;
#19602=CARTESIAN_POINT ( 'NONE',  ( 10.00000000000000000, 23.16143007188532366, -73.95703589263949596 ) ) ;
#19603=CARTESIAN_POINT ( 'NONE',  ( 0.000000000000000000, 55.20638768913760686, 51.02545421589343988 ) ) ;
#19606=ORIENTED_EDGE ( 'NONE', *, *, #1593, .T. ) ;
#19619=CARTESIAN_POINT ( 'NONE',  ( 5.000000000000000000, 33.71516098798849015, -74.74816331893393340 ) ) ;
#19627=ORIENTED_EDGE ( 'NONE', *, *, #50517, .F. ) ;
#19640=CIRCLE ( 'NONE', #71248, 12.50000000000000000 ) ;
#19643=DIRECTION ( 'NONE',  ( -1.000000000000000000, 0.000000000000000000, -0.000000000000000000 ) ) ;
#19648=FACE_OUTER_BOUND ( 'NONE', #61909, .T. ) ;
#19653=CARTESIAN_POINT ( 'NONE',  ( 0.000000000000000000, 0.000000000000000000, 0.000000000000000000 ) ) ;
#19660=EDGE_CURVE ( 'NONE', #70270, #56502, #47374, .T. ) ;
#19661=CARTESIAN_POINT ( 'NONE',  ( 10.00000000000000000, -12.93880638057259169, -76.41127070299286572 ) ) ;
#19668=EDGE_CURVE ( 'NONE', #8349, #56500, #22158, .T. ) ;
#19669=DIRECTION ( 'NONE',  ( -1.000000000000000000, -0.000000000000000000, -0.000000000000000000 ) ) ;
#19671=EDGE_CURVE ( 'NONE', #14488, #15472, #35356, .T. ) ;
#19680=ORIENTED_EDGE ( 'NONE', *, *, #68235, .F. ) ;
#19682=DIRECTION ( 'NONE',  ( 0.000000000000000000, 0.8910065241883690090, -0.4539904997395446395 ) ) ;
#19686=AXIS2_PLACEMENT_3D ( 'NONE', #71144, #24927, #70397 ) ;
#19687=EDGE_LOOP ( 'NONE', ( #10613, #18059, #48429, #73756 ) ) ;
#19690=ORIENTED_EDGE ( 'NONE', *, *, #33634, .F. ) ;
#19694=CARTESIAN_POINT ( 'NONE',  ( 0.000000000000000000, 0.000000000000000000, 0.000000000000000000 ) ) ;
#19701=EDGE_CURVE ( 'NONE', #72850, #39929, #32914, .T. ) ;
#19704=AXIS2_PLACEMENT_3D ( 'NONE', #38279, #67223, #20981 ) ;
#19712=CARTESIAN_POINT ( 'NONE',  ( 10.00000000000000000, 0.000000000000000000, 0.000000000000000000 ) ) ;
#19714=VECTOR ( 'NONE', #14843, 1000.000000000000000 ) ;
#19725=CARTESIAN_POINT ( 'NONE',  ( 0.000000000000000000, 0.000000000000000000, 0.000000000000000000 ) ) ;
#19732=DIRECTION ( 'NONE',  ( -1.000000000000000000, 0.000000000000000000, 0.000000000000000000 ) ) ;
#19735=DIRECTION ( 'NONE',  ( 1.000000000000000000, 0.000000000000000000, 0.000000000000000000 ) ) ;
#19743=ORIENTED_EDGE ( 'NONE', *, *, #72795, .T. ) ;
#19746=DIRECTION ( 'NONE',  ( 0.000000000000000000, -0.7071067811865536790, 0.7071067811865412445 ) ) ;
#19751=EDGE_CURVE ( 'NONE', #15472, #37783, #72824, .T. ) ;
#19755=AXIS2_PLACEMENT_3D ( 'NONE', #19603, #66231, #42189 ) ;
#19758=EDGE_CURVE ( 'NONE', #17434, #73771, #49538, .T. ) ;
#19761=VERTEX_POINT ( 'NONE', #60110 ) ;
#19764=CARTESIAN_POINT ( 'NONE',  ( 10.00000000000000000, 55.20638768913831029, -51.02545421589267960 ) ) ;
#19766=CYLINDRICAL_SURFACE ( 'NONE', #52059, 31.99999999999999289 ) ;
#19774=ORIENTED_EDGE ( 'NONE', *, *, #17563, .F. ) ;
#19775=ORIENTED_EDGE ( 'NONE', *, *, #26337, .T. ) ;
#19788=ORIENTED_EDGE ( 'NONE', *, *, #62696, .F. ) ;
#19798=ORIENTED_EDGE ( 'NONE', *, *, #58943, .T. ) ;
#19803=EDGE_LOOP ( 'NONE', ( #20859, #65932, #52840, #35180 ) ) ;
#19809=AXIS2_PLACEMENT_3D ( 'NONE', #46581, #34935, #11611 ) ;
#19823=DIRECTION ( 'NONE',  ( 1.000000000000000000, 0.000000000000000000, 0.000000000000000000 ) ) ;
#19835=DIRECTION ( 'NONE',  ( 0.000000000000000000, 0.000000000000000000, 1.000000000000000000 ) ) ;
#19838=CARTESIAN_POINT ( 'NONE',  ( -10.00000000000000000, 0.000000000000000000, 0.000000000000000000 ) ) ;
#19842=CIRCLE ( 'NONE', #4261, 77.49899999999998101 ) ;
#19849=DIRECTION ( 'NONE',  ( 0.000000000000000000, 0.2334453638559058908, -0.9723699203976764460 ) ) ;
#19850=CARTESIAN_POINT ( 'NONE',  ( 0.000000000000000000, 28.89263327155850192, -71.91182617369156560 ) ) ;
#19854=AXIS2_PLACEMENT_3D ( 'NONE', #27668, #16013, #22403 ) ;
#19857=VERTEX_POINT ( 'NONE', #55022 ) ;
#19861=AXIS2_PLACEMENT_3D ( 'NONE', #1715, #45711, #17117 ) ;
#19863=CARTESIAN_POINT ( 'NONE',  ( 10.00000000000000000, 8.966570791701860443, -81.50828551894217355 ) ) ;
#19885=EDGE_LOOP ( 'NONE', ( #66743, #35843, #68236, #61852 ) ) ;
#19892=CARTESIAN_POINT ( 'NONE',  ( 0.000000000000000000, 0.000000000000000000, 0.000000000000000000 ) ) ;
#19893=DIRECTION ( 'NONE',  ( -1.000000000000000000, -0.000000000000000000, 0.000000000000000000 ) ) ;
#19897=ORIENTED_EDGE ( 'NONE', *, *, #13058, .F. ) ;
#19900=DIRECTION ( 'NONE',  ( 0.000000000000000000, 0.000000000000000000, 1.000000000000000000 ) ) ;
#19901=CARTESIAN_POINT ( 'NONE',  ( 0.000000000000000000, -74.74816331893454446, 33.71516098798714722 ) ) ;
#19904=CYLINDRICAL_SURFACE ( 'NONE', #54070, 77.49899999999999523 ) ;
#19905=LINE ( 'NONE', #55613, #69989 ) ;
#19909=CARTESIAN_POINT ( 'NONE',  ( 0.000000000000000000, 39.78640506895604290, 66.50666863322015843 ) ) ;
#19915=CARTESIAN_POINT ( 'NONE',  ( 10.00000000000000000, 14.66109333815460225, 73.73191006444577056 ) ) ;
#19916=CARTESIAN_POINT ( 'NONE',  ( 0.000000000000000000, 78.73519480814955784, 22.90783923731657268 ) ) ;
#19924=EDGE_CURVE ( 'NONE', #16380, #58612, #16181, .T. ) ;
#19951=VERTEX_POINT ( 'NONE', #33947 ) ;
#19955=LINE ( 'NONE', #49633, #7681 ) ;
#19964=EDGE_LOOP ( 'NONE', ( #17606, #5381, #25613, #23865 ) ) ;
#19972=AXIS2_PLACEMENT_3D ( 'NONE', #25267, #70357, #47816 ) ;
#19980=ORIENTED_EDGE ( 'NONE', *, *, #15523, .F. ) ;
#19981=AXIS2_PLACEMENT_3D ( 'NONE', #31934, #65431, #37595 ) ;
#19983=ORIENTED_EDGE ( 'NONE', *, *, #58677, .T. ) ;
#19994=AXIS2_PLACEMENT_3D ( 'NONE', #57140, #33069, #21803 ) ;
#20000=CARTESIAN_POINT ( 'NONE',  ( 10.00000000000000000, 0.000000000000000000, 0.000000000000000000 ) ) ;
#20017=EDGE_CURVE ( 'NONE', #45142, #39027, #70061, .T. ) ;
#20018=CIRCLE ( 'NONE', #40476, 32.00000000000000000 ) ;
#20022=CIRCLE ( 'NONE', #24815, 82.00000000000000000 ) ;
#20027=VECTOR ( 'NONE', #13615, 1000.000000000000000 ) ;
#20028=LINE ( 'NONE', #19661, #20496 ) ;
#20034=AXIS2_PLACEMENT_3D ( 'NONE', #72882, #43974, #21386 ) ;
#20035=DIRECTION ( 'NONE',  ( -1.000000000000000000, 0.000000000000000000, 0.000000000000000000 ) ) ;
#20037=DIRECTION ( 'NONE',  ( -1.000000000000000000, 0.000000000000000000, 0.000000000000000000 ) ) ;
#20041=EDGE_CURVE ( 'NONE', #60073, #23222, #62542, .T. ) ;
#20043=AXIS2_PLACEMENT_3D ( 'NONE', #24674, #52135, #6648 ) ;
#20044=ORIENTED_EDGE ( 'NONE', *, *, #14004, .T. ) ;
#20045=ORIENTED_EDGE ( 'NONE', *, *, #10343, .T. ) ;
#20063=DIRECTION ( 'NONE',  ( -1.000000000000000000, -0.000000000000000000, -0.000000000000000000 ) ) ;
#20084=DIRECTION ( 'NONE',  ( 0.000000000000000000, 0.000000000000000000, 1.000000000000000000 ) ) ;
#20086=AXIS2_PLACEMENT_3D ( 'NONE', #26737, #60961, #14723 ) ;
#20090=CYLINDRICAL_SURFACE ( 'NONE', #17783, 82.00000000000000000 ) ;
#20103=FACE_OUTER_BOUND ( 'NONE', #22552, .T. ) ;
#20106=CARTESIAN_POINT ( 'NONE',  ( 10.00000000000000000, -14.67089635893658794, -73.72996012237454977 ) ) ;
#20117=CARTESIAN_POINT ( 'NONE',  ( -10.00000000000000000, 0.000000000000000000, 0.000000000000000000 ) ) ;
#20124=AXIS2_PLACEMENT_3D ( 'NONE', #21335, #46151, #52507 ) ;
#20137=DIRECTION ( 'NONE',  ( 1.000000000000000000, 0.000000000000000000, 0.000000000000000000 ) ) ;
#20143=LINE ( 'NONE', #60398, #18998 ) ;
#20144=CIRCLE ( 'NONE', #60995, 31.99999999999998934 ) ;
#20149=CARTESIAN_POINT ( 'NONE',  ( 10.00000000000000000, 0.000000000000000000, 0.000000000000000000 ) ) ;
#20151=AXIS2_PLACEMENT_3D ( 'NONE', #58143, #1419, #69786 ) ;
#20154=ORIENTED_EDGE ( 'NONE', *, *, #30107, .T. ) ;
#20156=EDGE_CURVE ( 'NONE', #40784, #45539, #25642, .T. ) ;
#20157=ORIENTED_EDGE ( 'NONE', *, *, #16964, .F. ) ;
#20175=EDGE_CURVE ( 'NONE', #68980, #4178, #1696, .T. ) ;
#20185=CARTESIAN_POINT ( 'NONE',  ( -10.00000000000000000, 0.000000000000000000, 0.000000000000000000 ) ) ;
#20187=VECTOR ( 'NONE', #39256, 1000.000000000000000 ) ;
#20199=CARTESIAN_POINT ( 'NONE',  ( 0.000000000000000000, 64.81221759200343513, 50.23322058963371006 ) ) ;
#20205=CIRCLE ( 'NONE', #30998, 77.49900000000000944 ) ;
#20211=EDGE_CURVE ( 'NONE', #11722, #60065, #62915, .T. ) ;
#20218=CARTESIAN_POINT ( 'NONE',  ( 10.00000000000000000, 0.000000000000000000, 0.000000000000000000 ) ) ;
#20229=ORIENTED_EDGE ( 'NONE', *, *, #7905, .T. ) ;
#20231=DIRECTION ( 'NONE',  ( -1.000000000000000000, -0.000000000000000000, -0.000000000000000000 ) ) ;
#20232=AXIS2_PLACEMENT_3D ( 'NONE', #71410, #19182, #25202 ) ;
#20238=EDGE_LOOP ( 'NONE', ( #68129, #37578, #2152, #53624 ) ) ;
#20250=DIRECTION ( 'NONE',  ( -1.000000000000000000, 0.000000000000000000, 0.000000000000000000 ) ) ;
#20254=CIRCLE ( 'NONE', #38303, 31.99999999999999289 ) ;
#20256=ORIENTED_EDGE ( 'NONE', *, *, #31215, .F. ) ;
#20268=ORIENTED_EDGE ( 'NONE', *, *, #59491, .T. ) ;
#20275=CARTESIAN_POINT ( 'NONE',  ( 10.00000000000000000, 76.41127070299273782, 12.93880638057342836 ) ) ;
#20280=DIRECTION ( 'NONE',  ( 1.000000000000000000, 0.000000000000000000, 0.000000000000000000 ) ) ;
#20282=DIRECTION ( 'NONE',  ( 1.000000000000000000, 0.000000000000000000, 0.000000000000000000 ) ) ;
#20299=VECTOR ( 'NONE', #72159, 1000.000000000000000 ) ;
#20304=ADVANCED_FACE ( 'NONE', ( #5591 ), #73982, .T. ) ;
#20312=AXIS2_PLACEMENT_3D ( 'NONE', #47416, #42516, #8677 ) ;
#20315=AXIS2_PLACEMENT_3D ( 'NONE', #34570, #69167, #62809 ) ;
#20326=ORIENTED_EDGE ( 'NONE', *, *, #24507, .F. ) ;
#20328=EDGE_LOOP ( 'NONE', ( #49283, #40959, #25066, #73306 ) ) ;
#20346=ORIENTED_EDGE ( 'NONE', *, *, #55522, .F. ) ;
#20369=CARTESIAN_POINT ( 'NONE',  ( 10.00000000000000000, -41.76937507738745836, -62.50329211542482710 ) ) ;
#20378=AXIS2_PLACEMENT_3D ( 'NONE', #4750, #73881, #72753 ) ;
#20382=CIRCLE ( 'NONE', #38416, 31.99999999999999289 ) ;
#20383=AXIS2_PLACEMENT_3D ( 'NONE', #72810, #25855, #49525 ) ;
#20390=CARTESIAN_POINT ( 'NONE',  ( 0.000000000000000000, 0.000000000000000000, 0.000000000000000000 ) ) ;
#20391=ORIENTED_EDGE ( 'NONE', *, *, #12478, .F. ) ;
#20392=EDGE_CURVE ( 'NONE', #54097, #65643, #40088, .T. ) ;
#20401=DIRECTION ( 'NONE',  ( -1.000000000000000000, -0.000000000000000000, -0.000000000000000000 ) ) ;
#20413=AXIS2_PLACEMENT_3D ( 'NONE', #70027, #5799, #58022 ) ;
#20418=CARTESIAN_POINT ( 'NONE',  ( 10.00000000000000000, -14.67089635893764665, 73.72996012237435082 ) ) ;
#20424=ORIENTED_EDGE ( 'NONE', *, *, #26121, .F. ) ;
#20433=EDGE_LOOP ( 'NONE', ( #20624, #15650, #58807, #70244 ) ) ;
#20435=VERTEX_POINT ( 'NONE', #64563 ) ;
#20451=DIRECTION ( 'NONE',  ( 0.000000000000000000, 0.000000000000000000, 1.000000000000000000 ) ) ;
#20452=DIRECTION ( 'NONE',  ( 0.000000000000000000, 0.000000000000000000, 1.000000000000000000 ) ) ;
#20455=CARTESIAN_POINT ( 'NONE',  ( 0.000000000000000000, -24.73286445877757345, 73.44644590900053061 ) ) ;
#20456=EDGE_CURVE ( 'NONE', #71442, #49949, #6679, .T. ) ;
#20459=ORIENTED_EDGE ( 'NONE', *, *, #64946, .F. ) ;
#20473=ORIENTED_EDGE ( 'NONE', *, *, #67246, .T. ) ;
#20475=ADVANCED_FACE ( 'NONE', ( #35610 ), #23602, .T. ) ;
#20479=CARTESIAN_POINT ( 'NONE',  ( 10.00000000000000000, -2.946379043146863719, 75.11764819372146462 ) ) ;
#20485=CIRCLE ( 'NONE', #62518, 31.99999999999998934 ) ;
#20493=CARTESIAN_POINT ( 'NONE',  ( 10.00000000000000000, 23.16143007188426850, 73.95703589263983702 ) ) ;
#20495=DIRECTION ( 'NONE',  ( -1.000000000000000000, 0.000000000000000000, 0.000000000000000000 ) ) ;
#20496=VECTOR ( 'NONE', #54264, 1000.000000000000000 ) ;
#20501=CYLINDRICAL_SURFACE ( 'NONE', #14627, 77.49899999999999523 ) ;
#20507=ORIENTED_EDGE ( 'NONE', *, *, #38353, .T. ) ;
#20515=AXIS2_PLACEMENT_3D ( 'NONE', #73451, #44902, #67075 ) ;
#20516=ORIENTED_EDGE ( 'NONE', *, *, #35004, .T. ) ;
#20521=CARTESIAN_POINT ( 'NONE',  ( 5.000000000000000000, 21.60688246758696707, -79.10210256391346206 ) ) ;
#20522=CARTESIAN_POINT ( 'NONE',  ( 0.000000000000000000, -68.27212725128254078, -31.46837873495049465 ) ) ;
#20524=ADVANCED_FACE ( 'NONE', ( #41625 ), #36351, .T. ) ;
#20551=DIRECTION ( 'NONE',  ( -1.000000000000000000, -0.000000000000000000, 0.000000000000000000 ) ) ;
#20556=DIRECTION ( 'NONE',  ( 0.000000000000000000, 0.3826834323650907810, -0.9238795325112864054 ) ) ;
#20560=CYLINDRICAL_SURFACE ( 'NONE', #13343, 77.49899999999999523 ) ;
#20570=AXIS2_PLACEMENT_3D ( 'NONE', #49399, #47921, #72325 ) ;
#20573=EDGE_CURVE ( 'NONE', #32327, #3906, #61153, .T. ) ;
#20576=AXIS2_PLACEMENT_3D ( 'NONE', #71134, #24912, #8372 ) ;
#20585=AXIS2_PLACEMENT_3D ( 'NONE', #59293, #350, #23241 ) ;
#20592=AXIS2_PLACEMENT_3D ( 'NONE', #25019, #37050, #23920 ) ;
#20600=CARTESIAN_POINT ( 'NONE',  ( 10.00000000000000000, 0.000000000000000000, 0.000000000000000000 ) ) ;
#20611=EDGE_CURVE ( 'NONE', #42748, #50561, #59667, .T. ) ;
#20619=FACE_OUTER_BOUND ( 'NONE', #69649, .T. ) ;
#20624=ORIENTED_EDGE ( 'NONE', *, *, #36515, .T. ) ;
#20634=VERTEX_POINT ( 'NONE', #43128 ) ;
#20643=DIRECTION ( 'NONE',  ( -1.000000000000000000, -0.000000000000000000, 0.000000000000000000 ) ) ;
#20647=CARTESIAN_POINT ( 'NONE',  ( 10.00000000000000000, 0.000000000000000000, 0.000000000000000000 ) ) ;
#20654=DIRECTION ( 'NONE',  ( -1.000000000000000000, 0.000000000000000000, 0.000000000000000000 ) ) ;
#20657=DIRECTION ( 'NONE',  ( 0.000000000000000000, 0.000000000000000000, 1.000000000000000000 ) ) ;
#20671=DIRECTION ( 'NONE',  ( 0.000000000000000000, 0.000000000000000000, -1.000000000000000000 ) ) ;
#20680=LINE ( 'NONE', #38343, #32252 ) ;
#20687=ORIENTED_EDGE ( 'NONE', *, *, #67763, .F. ) ;
#20690=DIRECTION ( 'NONE',  ( 1.000000000000000000, -0.000000000000000000, -0.000000000000000000 ) ) ;
#20694=ORIENTED_EDGE ( 'NONE', *, *, #44984, .T. ) ;
#20702=ORIENTED_EDGE ( 'NONE', *, *, #60967, .T. ) ;
#20715=EDGE_LOOP ( 'NONE', ( #59163, #5941, #43105, #22645 ) ) ;
#20720=EDGE_LOOP ( 'NONE', ( #56536, #41689, #23190, #24956 ) ) ;
#20723=CARTESIAN_POINT ( 'NONE',  ( 0.000000000000000000, -62.20884554313985149, -46.21855187248698371 ) ) ;
#20725=CIRCLE ( 'NONE', #20576, 77.49899999999999523 ) ;
#20734=DIRECTION ( 'NONE',  ( -1.000000000000000000, 0.000000000000000000, 0.000000000000000000 ) ) ;
#20737=DIRECTION ( 'NONE',  ( -1.000000000000000000, 0.000000000000000000, 0.000000000000000000 ) ) ;
#20746=FACE_OUTER_BOUND ( 'NONE', #25820, .T. ) ;
#20751=LINE ( 'NONE', #54601, #13375 ) ;
#20771=ADVANCED_FACE ( 'NONE', ( #32923 ), #45351, .T. ) ;
#20779=AXIS2_PLACEMENT_3D ( 'NONE', #4737, #67497, #15622 ) ;
#20792=ORIENTED_EDGE ( 'NONE', *, *, #68531, .T. ) ;
#20794=FACE_OUTER_BOUND ( 'NONE', #24136, .T. ) ;
#20797=VERTEX_POINT ( 'NONE', #39331 ) ;
#20801=CYLINDRICAL_SURFACE ( 'NONE', #40507, 31.99999999999999289 ) ;
#20815=DIRECTION ( 'NONE',  ( -1.000000000000000000, 0.000000000000000000, 0.000000000000000000 ) ) ;
#20824=DIRECTION ( 'NONE',  ( 1.000000000000000000, 0.000000000000000000, 0.000000000000000000 ) ) ;
#20837=CARTESIAN_POINT ( 'NONE',  ( 10.00000000000000000, 63.18004540533092239, -44.88180994100307686 ) ) ;
#20859=ORIENTED_EDGE ( 'NONE', *, *, #43161, .T. ) ;
#20863=LINE ( 'NONE', #4337, #17359 ) ;
#20879=CARTESIAN_POINT ( 'NONE',  ( 10.00000000000000000, -74.65491531819111515, -8.830959090343204920 ) ) ;
#20880=DIRECTION ( 'NONE',  ( -1.000000000000000000, 0.000000000000000000, -0.000000000000000000 ) ) ;
#20910=ORIENTED_EDGE ( 'NONE', *, *, #70875, .T. ) ;
#20917=CARTESIAN_POINT ( 'NONE',  ( 10.00000000000000000, 0.000000000000000000, 0.000000000000000000 ) ) ;
#20919=DIRECTION ( 'NONE',  ( -1.000000000000000000, -0.000000000000000000, 0.000000000000000000 ) ) ;
#20922=EDGE_LOOP ( 'NONE', ( #23646, #11933, #71927, #64521 ) ) ;
#20925=DIRECTION ( 'NONE',  ( 0.000000000000000000, 0.9876883405951371042, 0.1564344650402347547 ) ) ;
#20928=ORIENTED_EDGE ( 'NONE', *, *, #63241, .F. ) ;
#20929=DIRECTION ( 'NONE',  ( 0.000000000000000000, 0.000000000000000000, -1.000000000000000000 ) ) ;
#20932=AXIS2_PLACEMENT_3D ( 'NONE', #65018, #13497, #63912 ) ;
#20936=DIRECTION ( 'NONE',  ( 0.000000000000000000, 1.000000000000000000, 3.469446951953614978E-15 ) ) ;
#20938=CARTESIAN_POINT ( 'NONE',  ( 10.00000000000000000, -49.70050353004933896, 59.46389618801946852 ) ) ;
#20945=EDGE_LOOP ( 'NONE', ( #59905, #26063, #23758, #54024 ) ) ;
#20946=AXIS2_PLACEMENT_3D ( 'NONE', #28715, #51656, #201 ) ;
#20957=FACE_OUTER_BOUND ( 'NONE', #65990, .T. ) ;
#20958=DIRECTION ( 'NONE',  ( 0.000000000000000000, 0.000000000000000000, 1.000000000000000000 ) ) ;
#20973=ORIENTED_EDGE ( 'NONE', *, *, #19671, .F. ) ;
#20981=DIRECTION ( 'NONE',  ( 0.000000000000000000, -0.7604059656000228262, -0.6494480483301932061 ) ) ;
#20982=ORIENTED_EDGE ( 'NONE', *, *, #17265, .F. ) ;
#20983=CARTESIAN_POINT ( 'NONE',  ( 10.00000000000000000, 36.73666225445988687, -65.58780272294035285 ) ) ;
#20990=DIRECTION ( 'NONE',  ( 1.000000000000000000, -0.000000000000000000, 0.000000000000000000 ) ) ;
#20992=AXIS2_PLACEMENT_3D ( 'NONE', #16158, #66556, #61287 ) ;
#20997=ORIENTED_EDGE ( 'NONE', *, *, #58852, .T. ) ;
#21001=ORIENTED_EDGE ( 'NONE', *, *, #68235, .T. ) ;
#21025=LINE ( 'NONE', #27030, #66453 ) ;
#21027=ADVANCED_FACE ( 'NONE', ( #31361 ), #60698, .T. ) ;
#21029=LINE ( 'NONE', #31939, #44848 ) ;
#21043=VECTOR ( 'NONE', #19473, 1000.000000000000000 ) ;
#21048=CARTESIAN_POINT ( 'NONE',  ( 0.000000000000000000, 81.50828551894240093, -8.966570791699803422 ) ) ;
#21060=ORIENTED_EDGE ( 'NONE', *, *, #15076, .F. ) ;
#21064=CARTESIAN_POINT ( 'NONE',  ( 10.00000000000000000, 0.000000000000000000, 0.000000000000000000 ) ) ;
#21065=ORIENTED_EDGE ( 'NONE', *, *, #57804, .F. ) ;
#21070=ORIENTED_EDGE ( 'NONE', *, *, #10625, .T. ) ;
#21091=CARTESIAN_POINT ( 'NONE',  ( 10.00000000000000000, 62.50884508063487033, -41.76106447765422303 ) ) ;
#21092=CARTESIAN_POINT ( 'NONE',  ( 10.00000000000000000, 26.02418014898310261, 70.52718814184268581 ) ) ;
#21094=DIRECTION ( 'NONE',  ( 0.000000000000000000, 0.000000000000000000, 1.000000000000000000 ) ) ;
#21098=EDGE_LOOP ( 'NONE', ( #55732, #12826, #2898, #10515 ) ) ;
#21101=DIRECTION ( 'NONE',  ( 0.000000000000000000, 0.3826834323650841752, 0.9238795325112891810 ) ) ;
#21105=EDGE_CURVE ( 'NONE', #46694, #67190, #42266, .T. ) ;
#21111=AXIS2_PLACEMENT_3D ( 'NONE', #48933, #71860, #54952 ) ;
#21113=ORIENTED_EDGE ( 'NONE', *, *, #29756, .T. ) ;
#21117=CARTESIAN_POINT ( 'NONE',  ( 5.000000000000000000, -59.75363087400113926, 56.15606465354937882 ) ) ;
#21119=DIRECTION ( 'NONE',  ( 0.000000000000000000, 0.7071067811865439090, 0.7071067811865512365 ) ) ;
#21124=VERTEX_POINT ( 'NONE', #3935 ) ;
#21126=DIRECTION ( 'NONE',  ( 1.000000000000000000, 0.000000000000000000, -0.000000000000000000 ) ) ;
#21127=CARTESIAN_POINT ( 'NONE',  ( 10.00000000000000000, -71.21200624218823805, 40.65526001592589722 ) ) ;
#21135=ORIENTED_EDGE ( 'NONE', *, *, #35801, .F. ) ;
#21146=DIRECTION ( 'NONE',  ( 0.000000000000000000, 0.000000000000000000, 1.000000000000000000 ) ) ;
#21148=AXIS2_PLACEMENT_3D ( 'NONE', #58739, #12122, #52343 ) ;
#21157=VERTEX_POINT ( 'NONE', #65424 ) ;
#21162=VERTEX_POINT ( 'NONE', #25550 ) ;
#21165=VERTEX_POINT ( 'NONE', #12783 ) ;
#21168=DIRECTION ( 'NONE',  ( 0.000000000000000000, 0.000000000000000000, 1.000000000000000000 ) ) ;
#21170=LINE ( 'NONE', #67796, #67221 ) ;
#21171=DIRECTION ( 'NONE',  ( 0.000000000000000000, 0.000000000000000000, 1.000000000000000000 ) ) ;
#21174=VERTEX_POINT ( 'NONE', #8261 ) ;
#21187=VERTEX_POINT ( 'NONE', #7160 ) ;
#21201=AXIS2_PLACEMENT_3D ( 'NONE', #66219, #48175, #48902 ) ;
#21202=EDGE_CURVE ( 'NONE', #24336, #14991, #30807, .T. ) ;
#21213=EDGE_CURVE ( 'NONE', #60043, #9438, #30440, .T. ) ;
#21219=FACE_OUTER_BOUND ( 'NONE', #4278, .T. ) ;
#21223=CIRCLE ( 'NONE', #50039, 31.99999999999999289 ) ;
#21230=VERTEX_POINT ( 'NONE', #71401 ) ;
#21235=VERTEX_POINT ( 'NONE', #20275 ) ;
#21238=CARTESIAN_POINT ( 'NONE',  ( 10.00000000000000000, 81.34940948281335693, 10.30890764327412690 ) ) ;
#21248=ORIENTED_EDGE ( 'NONE', *, *, #60456, .F. ) ;
#21255=VERTEX_POINT ( 'NONE', #19901 ) ;
#21259=AXIS2_PLACEMENT_3D ( 'NONE', #74115, #39927, #23008 ) ;
#21260=EDGE_LOOP ( 'NONE', ( #27713, #58341, #598, #38242 ) ) ;
#21285=ORIENTED_EDGE ( 'NONE', *, *, #72815, .T. ) ;
#21288=EDGE_CURVE ( 'NONE', #8336, #39875, #37494, .T. ) ;
#21301=EDGE_CURVE ( 'NONE', #50464, #26778, #3850, .T. ) ;
#21307=CYLINDRICAL_SURFACE ( 'NONE', #2364, 32.00000000000000000 ) ;
#21309=AXIS2_PLACEMENT_3D ( 'NONE', #39923, #16233, #28245 ) ;
#21310=FACE_OUTER_BOUND ( 'NONE', #2407, .T. ) ;
#21315=CARTESIAN_POINT ( 'NONE',  ( 0.000000000000000000, -68.27212725128298132, 31.46837873494953541 ) ) ;
#21316=DIRECTION ( 'NONE',  ( -1.000000000000000000, 0.000000000000000000, 0.000000000000000000 ) ) ;
#21319=AXIS2_PLACEMENT_3D ( 'NONE', #19403, #65290, #13762 ) ;
#21323=VECTOR ( 'NONE', #36565, 1000.000000000000000 ) ;
#21331=ORIENTED_EDGE ( 'NONE', *, *, #19701, .F. ) ;
#21332=DIRECTION ( 'NONE',  ( 0.000000000000000000, 0.9876883405951371042, 0.1564344650402347547 ) ) ;
#21333=EDGE_LOOP ( 'NONE', ( #66923, #71925, #21618, #18096 ) ) ;
#21334=ORIENTED_EDGE ( 'NONE', *, *, #2521, .T. ) ;
#21335=CARTESIAN_POINT ( 'NONE',  ( 0.000000000000000000, -68.26794271651286294, 31.47745569255117104 ) ) ;
#21355=CARTESIAN_POINT ( 'NONE',  ( 0.000000000000000000, 76.66974797899835892, 11.30684508768368346 ) ) ;
#21363=ADVANCED_FACE ( 'NONE', ( #50332 ), #49584, .T. ) ;
#21385=AXIS2_PLACEMENT_3D ( 'NONE', #73729, #33893, #56837 ) ;
#21386=DIRECTION ( 'NONE',  ( 0.000000000000000000, 0.07845909572784529051, -0.9969173337331279638 ) ) ;
#21388=DIRECTION ( 'NONE',  ( -1.000000000000000000, 0.000000000000000000, -0.000000000000000000 ) ) ;
#21390=AXIS2_PLACEMENT_3D ( 'NONE', #31407, #71624, #52214 ) ;
#21395=EDGE_CURVE ( 'NONE', #46506, #73838, #11136, .T. ) ;
#21419=AXIS2_PLACEMENT_3D ( 'NONE', #11066, #22726, #44916 ) ;
#21423=DIRECTION ( 'NONE',  ( -1.000000000000000000, 0.000000000000000000, -0.000000000000000000 ) ) ;
#21424=CIRCLE ( 'NONE', #56290, 31.99999999999998934 ) ;
#21429=DIRECTION ( 'NONE',  ( -1.000000000000000000, -0.000000000000000000, -0.000000000000000000 ) ) ;
#21433=DIRECTION ( 'NONE',  ( -1.000000000000000000, -0.000000000000000000, 0.000000000000000000 ) ) ;
#21444=ORIENTED_EDGE ( 'NONE', *, *, #73940, .F. ) ;
#21445=EDGE_CURVE ( 'NONE', #57978, #58272, #340, .T. ) ;
#21449=CARTESIAN_POINT ( 'NONE',  ( 10.00000000000000000, -35.91791733033525702, 68.67312586194982771 ) ) ;
#21465=AXIS2_PLACEMENT_3D ( 'NONE', #37966, #61276, #68026 ) ;
#21467=DIRECTION ( 'NONE',  ( -1.000000000000000000, -0.000000000000000000, 0.000000000000000000 ) ) ;
#21470=AXIS2_PLACEMENT_3D ( 'NONE', #13898, #65433, #36108 ) ;
#21471=EDGE_LOOP ( 'NONE', ( #6289, #60911, #7303, #30891 ) ) ;
#21472=DIRECTION ( 'NONE',  ( 1.000000000000000000, 0.000000000000000000, 0.000000000000000000 ) ) ;
#21494=AXIS2_PLACEMENT_3D ( 'NONE', #74322, #34101, #4435 ) ;
#21498=DIRECTION ( 'NONE',  ( 0.000000000000000000, -0.6494480483301739993, -0.7604059656000390355 ) ) ;
#21507=ORIENTED_EDGE ( 'NONE', *, *, #18737, .F. ) ;
#21512=AXIS2_PLACEMENT_3D ( 'NONE', #12190, #41149, #29110 ) ;
#21513=EDGE_CURVE ( 'NONE', #18038, #53602, #27916, .T. ) ;
#21516=AXIS2_PLACEMENT_3D ( 'NONE', #13612, #65504, #64761 ) ;
#21519=CARTESIAN_POINT ( 'NONE',  ( 0.000000000000000000, 62.50884508063487033, -41.76106447765422303 ) ) ;
#21523=ADVANCED_FACE ( 'NONE', ( #45084 ), #68006, .T. ) ;
#21526=EDGE_CURVE ( 'NONE', #9779, #15045, #11082, .T. ) ;
#21544=DIRECTION ( 'NONE',  ( -1.000000000000000000, 0.000000000000000000, 0.000000000000000000 ) ) ;
#21545=DIRECTION ( 'NONE',  ( -1.000000000000000000, 0.000000000000000000, 0.000000000000000000 ) ) ;
#21557=LINE ( 'NONE', #32466, #61086 ) ;
#21558=ADVANCED_FACE ( 'NONE', ( #24632 ), #51079, .T. ) ;
#21587=AXIS2_PLACEMENT_3D ( 'NONE', #55917, #27717, #4432 ) ;
#21592=CIRCLE ( 'NONE', #34091, 77.49899999999999523 ) ;
#21601=VECTOR ( 'NONE', #38239, 1000.000000000000000 ) ;
#21602=AXIS2_PLACEMENT_3D ( 'NONE', #69276, #56896, #52723 ) ;
#21604=CIRCLE ( 'NONE', #64884, 82.00000000000000000 ) ;
#21610=ORIENTED_EDGE ( 'NONE', *, *, #53378, .T. ) ;
#21618=ORIENTED_EDGE ( 'NONE', *, *, #36425, .F. ) ;
#21621=VERTEX_POINT ( 'NONE', #43793 ) ;
#21622=DIRECTION ( 'NONE',  ( -1.000000000000000000, 0.000000000000000000, 0.000000000000000000 ) ) ;
#21623=DIRECTION ( 'NONE',  ( -1.000000000000000000, 0.000000000000000000, 0.000000000000000000 ) ) ;
#21625=AXIS2_PLACEMENT_3D ( 'NONE', #11718, #34663, #27538 ) ;
#21626=CARTESIAN_POINT ( 'NONE',  ( 5.000000000000002665, 34.94270380257741948, -74.18225833017852722 ) ) ;
#21631=AXIS2_PLACEMENT_3D ( 'NONE', #20390, #25656, #19271 ) ;
#21635=AXIS2_PLACEMENT_3D ( 'NONE', #46850, #18625, #65254 ) ;
#21664=ORIENTED_EDGE ( 'NONE', *, *, #34449, .F. ) ;
#21665=AXIS2_PLACEMENT_3D ( 'NONE', #30358, #8920, #36746 ) ;
#21675=DIRECTION ( 'NONE',  ( -1.000000000000000000, 0.000000000000000000, 0.000000000000000000 ) ) ;
#21679=DIRECTION ( 'NONE',  ( -1.000000000000000000, 0.000000000000000000, -0.000000000000000000 ) ) ;
#21683=CARTESIAN_POINT ( 'NONE',  ( 10.00000000000000000, 0.000000000000000000, 0.000000000000000000 ) ) ;
#21695=EDGE_CURVE ( 'NONE', #10267, #46506, #13479, .T. ) ;
#21708=CIRCLE ( 'NONE', #48127, 82.00000000000000000 ) ;
#21711=CARTESIAN_POINT ( 'NONE',  ( 5.000000000000002665, 74.18225833017937987, -34.94270380257560049 ) ) ;
#21734=CARTESIAN_POINT ( 'NONE',  ( 50.00005079999999680, 0.000000000000000000, 0.000000000000000000 ) ) ;
#21737=ADVANCED_FACE ( 'NONE', ( #59978 ), #66352, .T. ) ;
#21742=DIRECTION ( 'NONE',  ( -1.000000000000000000, -0.000000000000000000, -0.000000000000000000 ) ) ;
#21752=ORIENTED_EDGE ( 'NONE', *, *, #17546, .T. ) ;
#21757=DIRECTION ( 'NONE',  ( -1.000000000000000000, -0.000000000000000000, -0.000000000000000000 ) ) ;
#21760=ORIENTED_EDGE ( 'NONE', *, *, #22870, .T. ) ;
#21764=CARTESIAN_POINT ( 'NONE',  ( 10.00000000000000000, 65.59268652807210742, 36.72794159290264560 ) ) ;
#21768=DIRECTION ( 'NONE',  ( 0.000000000000000000, 0.000000000000000000, 1.000000000000000000 ) ) ;
#21773=DIRECTION ( 'NONE',  ( 0.000000000000000000, 0.000000000000000000, 1.000000000000000000 ) ) ;
#21780=CARTESIAN_POINT ( 'NONE',  ( 0.000000000000000000, 77.32052557432849937, -5.256550761632002633 ) ) ;
#21788=CARTESIAN_POINT ( 'NONE',  ( 10.00000000000000000, 39.78640506895604290, 66.50666863322015843 ) ) ;
#21794=CIRCLE ( 'NONE', #12185, 31.99999999999999645 ) ;
#21803=DIRECTION ( 'NONE',  ( 0.000000000000000000, 0.000000000000000000, 1.000000000000000000 ) ) ;
#21809=ORIENTED_EDGE ( 'NONE', *, *, #1808, .F. ) ;
#21811=EDGE_LOOP ( 'NONE', ( #39774, #43846, #9617, #65122 ) ) ;
#21812=AXIS2_PLACEMENT_3D ( 'NONE', #10197, #26378, #44798 ) ;
#21816=CARTESIAN_POINT ( 'NONE',  ( 5.000000000000002665, 29.01471420065674423, -76.69515212745984911 ) ) ;
#21834=ORIENTED_EDGE ( 'NONE', *, *, #62697, .F. ) ;
#21837=FACE_OUTER_BOUND ( 'NONE', #66867, .T. ) ;
#21845=ORIENTED_EDGE ( 'NONE', *, *, #49527, .T. ) ;
#21855=ORIENTED_EDGE ( 'NONE', *, *, #5278, .T. ) ;
#21857=VERTEX_POINT ( 'NONE', #21954 ) ;
#21864=DIRECTION ( 'NONE',  ( 0.000000000000000000, 0.000000000000000000, 1.000000000000000000 ) ) ;
#21872=CARTESIAN_POINT ( 'NONE',  ( 10.00000000000000000, 55.19960302592066625, 51.03279382321107249 ) ) ;
#21876=DIRECTION ( 'NONE',  ( 0.000000000000000000, -0.9969173337331271867, -0.07845909572785568498 ) ) ;
#21880=DIRECTION ( 'NONE',  ( 0.000000000000000000, 0.000000000000000000, -1.000000000000000000 ) ) ;
#21889=CARTESIAN_POINT ( 'NONE',  ( 0.000000000000000000, 77.49459641780886443, 0.8261519478433866359 ) ) ;
#21900=ORIENTED_EDGE ( 'NONE', *, *, #28793, .T. ) ;
#21908=AXIS2_PLACEMENT_3D ( 'NONE', #30628, #369, #22898 ) ;
#21916=ORIENTED_EDGE ( 'NONE', *, *, #69707, .T. ) ;
#21917=EDGE_LOOP ( 'NONE', ( #11030, #24788, #12591, #13743 ) ) ;
#21924=AXIS2_PLACEMENT_3D ( 'NONE', #3848, #15101, #27112 ) ;
#21954=CARTESIAN_POINT ( 'NONE',  ( 0.000000000000000000, -2.543863470247813119, -81.96053171279905314 ) ) ;
#21955=DIRECTION ( 'NONE',  ( 0.000000000000000000, 0.000000000000000000, -1.000000000000000000 ) ) ;
#21963=DIRECTION ( 'NONE',  ( 0.000000000000000000, 0.000000000000000000, 1.000000000000000000 ) ) ;
#21967=ADVANCED_FACE ( 'NONE', ( #35813 ), #11765, .T. ) ;
#21986=ORIENTED_EDGE ( 'NONE', *, *, #34064, .T. ) ;
#21993=VERTEX_POINT ( 'NONE', #18168 ) ;
#22016=CARTESIAN_POINT ( 'NONE',  ( 0.000000000000000000, -20.41045688087772092, -72.35160999960838524 ) ) ;
#22019=ORIENTED_EDGE ( 'NONE', *, *, #23636, .F. ) ;
#22024=VECTOR ( 'NONE', #59264, 1000.000000000000000 ) ;
#22028=CARTESIAN_POINT ( 'NONE',  ( 0.000000000000000000, 63.97538442413498672, -51.29473840253155714 ) ) ;
#22033=ORIENTED_EDGE ( 'NONE', *, *, #54305, .F. ) ;
#22040=ORIENTED_EDGE ( 'NONE', *, *, #21213, .F. ) ;
#22063=AXIS2_PLACEMENT_3D ( 'NONE', #37428, #43065, #38526 ) ;
#22065=CARTESIAN_POINT ( 'NONE',  ( 10.00000000000000000, -55.38113227695820484, 54.21277698773656084 ) ) ;
#22087=EDGE_LOOP ( 'NONE', ( #34154, #61338, #53199, #19775 ) ) ;
#22089=EDGE_CURVE ( 'NONE', #3728, #29240, #20725, .T. ) ;
#22090=CARTESIAN_POINT ( 'NONE',  ( 0.000000000000000000, 0.000000000000000000, 0.000000000000000000 ) ) ;
#22091=CARTESIAN_POINT ( 'NONE',  ( 0.000000000000000000, 14.67089635893819377, -73.72996012237423713 ) ) ;
#22098=ORIENTED_EDGE ( 'NONE', *, *, #49828, .F. ) ;
#22111=CARTESIAN_POINT ( 'NONE',  ( 10.00000000000000000, 36.72794159290334903, -65.59268652807170952 ) ) ;
#22114=DIRECTION ( 'NONE',  ( -1.000000000000000000, -0.000000000000000000, 0.000000000000000000 ) ) ;
#22122=FACE_OUTER_BOUND ( 'NONE', #2021, .T. ) ;
#22137=ORIENTED_EDGE ( 'NONE', *, *, #36168, .F. ) ;
#22150=DIRECTION ( 'NONE',  ( 0.000000000000000000, 0.000000000000000000, 1.000000000000000000 ) ) ;
#22151=EDGE_CURVE ( 'NONE', #26342, #50832, #55395, .T. ) ;
#22158=CIRCLE ( 'NONE', #40195, 77.49900000000000944 ) ;
#22161=VECTOR ( 'NONE', #18685, 1000.000000000000000 ) ;
#22166=DIRECTION ( 'NONE',  ( 0.000000000000000000, -0.7604059656000228262, -0.6494480483301932061 ) ) ;
#22169=EDGE_CURVE ( 'NONE', #26809, #70270, #20751, .T. ) ;
#22174=VECTOR ( 'NONE', #23671, 1000.000000000000000 ) ;
#22178=EDGE_CURVE ( 'NONE', #10732, #12767, #19384, .T. ) ;
#22188=FACE_OUTER_BOUND ( 'NONE', #3, .T. ) ;
#22189=VERTEX_POINT ( 'NONE', #14376 ) ;
#22194=EDGE_LOOP ( 'NONE', ( #61683, #8697, #49632, #37501 ) ) ;
#22200=ORIENTED_EDGE ( 'NONE', *, *, #69530, .T. ) ;
#22204=ORIENTED_EDGE ( 'NONE', *, *, #64439, .T. ) ;
#22211=ORIENTED_EDGE ( 'NONE', *, *, #38465, .T. ) ;
#22217=AXIS2_PLACEMENT_3D ( 'NONE', #61562, #26220, #19835 ) ;
#22227=EDGE_CURVE ( 'NONE', #33646, #24236, #44630, .T. ) ;
#22228=DIRECTION ( 'NONE',  ( 0.000000000000000000, -1.000000000000000000, -1.047444401652940007E-14 ) ) ;
#22234=ADVANCED_FACE ( 'NONE', ( #66979, #3853 ), #15105, .F. ) ;
#22236=DIRECTION ( 'NONE',  ( 0.000000000000000000, 0.3826834323650907810, -0.9238795325112864054 ) ) ;
#22239=DIRECTION ( 'NONE',  ( 1.000000000000000000, 0.000000000000000000, 0.000000000000000000 ) ) ;
#22242=EDGE_LOOP ( 'NONE', ( #2520, #32574, #56191, #639 ) ) ;
#22243=VECTOR ( 'NONE', #28032, 1000.000000000000000 ) ;
#22245=AXIS2_PLACEMENT_3D ( 'NONE', #19838, #13092, #59341 ) ;
#22252=AXIS2_PLACEMENT_3D ( 'NONE', #56743, #28144, #45836 ) ;
#22255=CARTESIAN_POINT ( 'NONE',  ( 0.000000000000000000, 0.000000000000000000, 0.000000000000000000 ) ) ;
#22256=CIRCLE ( 'NONE', #64288, 32.00000000000000000 ) ;
#22262=ADVANCED_FACE ( 'NONE', ( #16592 ), #74102, .T. ) ;
#22264=VECTOR ( 'NONE', #44156, 1000.000000000000000 ) ;
#22269=DIRECTION ( 'NONE',  ( -1.000000000000000000, 0.000000000000000000, -0.000000000000000000 ) ) ;
#22279=CIRCLE ( 'NONE', #16260, 82.00000000000000000 ) ;
#22289=DIRECTION ( 'NONE',  ( -1.000000000000000000, 0.000000000000000000, -0.000000000000000000 ) ) ;
#22294=ORIENTED_EDGE ( 'NONE', *, *, #46211, .T. ) ;
#22295=AXIS2_PLACEMENT_3D ( 'NONE', #47905, #30970, #9158 ) ;
#22303=DIRECTION ( 'NONE',  ( 0.000000000000000000, 0.000000000000000000, 1.000000000000000000 ) ) ;
#22316=DIRECTION ( 'NONE',  ( 0.000000000000000000, 0.000000000000000000, 1.000000000000000000 ) ) ;
#22341=DIRECTION ( 'NONE',  ( 0.000000000000000000, 0.000000000000000000, -1.000000000000000000 ) ) ;
#22344=EDGE_CURVE ( 'NONE', #24857, #47239, #4595, .T. ) ;
#22351=DIRECTION ( 'NONE',  ( -1.000000000000000000, -0.000000000000000000, 0.000000000000000000 ) ) ;
#22354=EDGE_CURVE ( 'NONE', #14707, #44617, #60252, .T. ) ;
#22355=EDGE_CURVE ( 'NONE', #70908, #18595, #47039, .T. ) ;
#22363=EDGE_LOOP ( 'NONE', ( #26137, #30722, #27171, #49462 ) ) ;
#22374=CARTESIAN_POINT ( 'NONE',  ( 10.00000000000000000, 2.946379043147425492, -75.11764819372145041 ) ) ;
#22386=DIRECTION ( 'NONE',  ( -1.000000000000000000, 0.000000000000000000, 0.000000000000000000 ) ) ;
#22391=ORIENTED_EDGE ( 'NONE', *, *, #26510, .F. ) ;
#22399=EDGE_LOOP ( 'NONE', ( #34974, #71024, #67591, #2655 ) ) ;
#22403=DIRECTION ( 'NONE',  ( 0.000000000000000000, -0.3826834323650969427, 0.9238795325112838519 ) ) ;
#22404=EDGE_CURVE ( 'NONE', #37315, #70629, #57198, .T. ) ;
#22406=DIRECTION ( 'NONE',  ( -1.000000000000000000, 0.000000000000000000, 0.000000000000000000 ) ) ;
#22417=EDGE_CURVE ( 'NONE', #22556, #1777, #11322, .T. ) ;
#22420=AXIS2_PLACEMENT_3D ( 'NONE', #12706, #1117, #11974 ) ;
#22430=VECTOR ( 'NONE', #71343, 1000.000000000000000 ) ;
#22439=DIRECTION ( 'NONE',  ( -1.000000000000000000, -0.000000000000000000, 0.000000000000000000 ) ) ;
#22477=DIRECTION ( 'NONE',  ( 0.000000000000000000, 0.000000000000000000, 1.000000000000000000 ) ) ;
#22495=ORIENTED_EDGE ( 'NONE', *, *, #39813, .T. ) ;
#22498=DIRECTION ( 'NONE',  ( -1.000000000000000000, -0.000000000000000000, -0.000000000000000000 ) ) ;
#22507=VERTEX_POINT ( 'NONE', #12065 ) ;
#22516=VECTOR ( 'NONE', #45132, 1000.000000000000000 ) ;
#22545=CARTESIAN_POINT ( 'NONE',  ( 10.00000000000000000, 0.000000000000000000, 0.000000000000000000 ) ) ;
#22549=EDGE_LOOP ( 'NONE', ( #37991, #348, #59005, #40714 ) ) ;
#22550=ORIENTED_EDGE ( 'NONE', *, *, #19668, .T. ) ;
#22552=EDGE_LOOP ( 'NONE', ( #10847, #41766, #6300, #13665 ) ) ;
#22555=AXIS2_PLACEMENT_3D ( 'NONE', #2631, #20231, #31146 ) ;
#22556=VERTEX_POINT ( 'NONE', #41021 ) ;
#22558=AXIS2_PLACEMENT_3D ( 'NONE', #4045, #54412, #43153 ) ;
#22565=AXIS2_PLACEMENT_3D ( 'NONE', #31372, #54322, #54686 ) ;
#22567=VECTOR ( 'NONE', #65904, 1000.000000000000000 ) ;
#22571=EDGE_CURVE ( 'NONE', #36763, #38273, #72239, .T. ) ;
#22576=ORIENTED_EDGE ( 'NONE', *, *, #19701, .T. ) ;
#22580=CARTESIAN_POINT ( 'NONE',  ( 10.00000000000000000, 0.000000000000000000, 0.000000000000000000 ) ) ;
#22584=CIRCLE ( 'NONE', #38187, 31.99999999999998579 ) ;
#22614=CARTESIAN_POINT ( 'NONE',  ( 10.00000000000000000, 0.000000000000000000, 0.000000000000000000 ) ) ;
#22616=AXIS2_PLACEMENT_3D ( 'NONE', #14509, #31057, #70525 ) ;
#22621=CYLINDRICAL_SURFACE ( 'NONE', #21385, 77.49899999999999523 ) ;
#22645=ORIENTED_EDGE ( 'NONE', *, *, #36645, .T. ) ;
#22655=ORIENTED_EDGE ( 'NONE', *, *, #7460, .F. ) ;
#22657=EDGE_LOOP ( 'NONE', ( #15568, #56252, #66649, #41157 ) ) ;
#22667=EDGE_LOOP ( 'NONE', ( #47702, #49567, #5774, #58983 ) ) ;
#22673=ORIENTED_EDGE ( 'NONE', *, *, #59887, .F. ) ;
#22703=EDGE_CURVE ( 'NONE', #62914, #16336, #55456, .T. ) ;
#22722=LINE ( 'NONE', #23452, #28214 ) ;
#22726=DIRECTION ( 'NONE',  ( -1.000000000000000000, -0.000000000000000000, -0.000000000000000000 ) ) ;
#22731=AXIS2_PLACEMENT_3D ( 'NONE', #1860, #47674, #36760 ) ;
#22735=DIRECTION ( 'NONE',  ( 0.000000000000000000, 0.000000000000000000, 1.000000000000000000 ) ) ;
#22744=ORIENTED_EDGE ( 'NONE', *, *, #43136, .F. ) ;
#22750=AXIS2_PLACEMENT_3D ( 'NONE', #65700, #25834, #41644 ) ;
#22751=CIRCLE ( 'NONE', #64774, 31.99999999999999645 ) ;
#22755=VERTEX_POINT ( 'NONE', #38706 ) ;
#22759=CARTESIAN_POINT ( 'NONE',  ( 0.000000000000000000, 0.000000000000000000, 0.000000000000000000 ) ) ;
#22768=EDGE_LOOP ( 'NONE', ( #57365, #2143, #23481, #45311 ) ) ;
#22769=CARTESIAN_POINT ( 'NONE',  ( 0.000000000000000000, 81.34940948281351325, -10.30890764327296161 ) ) ;
#22796=DIRECTION ( 'NONE',  ( 1.000000000000000000, -0.000000000000000000, -0.000000000000000000 ) ) ;
#22808=ORIENTED_EDGE ( 'NONE', *, *, #53406, .T. ) ;
#22813=DIRECTION ( 'NONE',  ( 0.000000000000000000, 0.000000000000000000, 1.000000000000000000 ) ) ;
#22820=CARTESIAN_POINT ( 'NONE',  ( 0.000000000000000000, -74.18225833017913828, 34.94270380257611919 ) ) ;
#22834=CIRCLE ( 'NONE', #64859, 82.00000000000000000 ) ;
#22837=CARTESIAN_POINT ( 'NONE',  ( 0.000000000000000000, 55.16347631943042984, 60.67117009219157353 ) ) ;
#22842=ADVANCED_FACE ( 'NONE', ( #57483 ), #11976, .T. ) ;
#22861=AXIS2_PLACEMENT_3D ( 'NONE', #50761, #44394, #45523 ) ;
#22870=EDGE_CURVE ( 'NONE', #18595, #9035, #43516, .T. ) ;
#22898=DIRECTION ( 'NONE',  ( 0.000000000000000000, 0.000000000000000000, 1.000000000000000000 ) ) ;
#22911=DIRECTION ( 'NONE',  ( -1.000000000000000000, 0.000000000000000000, 0.000000000000000000 ) ) ;
#22918=AXIS2_PLACEMENT_3D ( 'NONE', #6056, #18056, #27845 ) ;
#22939=EDGE_CURVE ( 'NONE', #5395, #45876, #58211, .T. ) ;
#22949=CARTESIAN_POINT ( 'NONE',  ( 10.00000000000000000, -56.15606465354917987, -59.75363087400133111 ) ) ;
#22956=EDGE_CURVE ( 'NONE', #47239, #21165, #63948, .T. ) ;
#22963=ORIENTED_EDGE ( 'NONE', *, *, #56789, .T. ) ;
#22981=CARTESIAN_POINT ( 'NONE',  ( 0.000000000000000000, -34.44570377933648331, 69.42325613327426481 ) ) ;
#22982=DIRECTION ( 'NONE',  ( 0.000000000000000000, 0.6494480483301793283, 0.7604059656000345946 ) ) ;
#22986=DIRECTION ( 'NONE',  ( -1.000000000000000000, -0.000000000000000000, 0.000000000000000000 ) ) ;
#22997=CIRCLE ( 'NONE', #30167, 82.00000000000000000 ) ;
#22998=AXIS2_PLACEMENT_3D ( 'NONE', #11971, #16505, #22150 ) ;
#23006=EDGE_CURVE ( 'NONE', #64863, #51313, #68401, .T. ) ;
#23008=DIRECTION ( 'NONE',  ( 0.000000000000000000, -0.3826834323650970537, 0.9238795325112838519 ) ) ;
#23012=LINE ( 'NONE', #16993, #34548 ) ;
#23016=AXIS2_PLACEMENT_3D ( 'NONE', #34703, #1289, #68930 ) ;
#23022=EDGE_LOOP ( 'NONE', ( #59141, #4244, #7953, #62668 ) ) ;
#23029=CARTESIAN_POINT ( 'NONE',  ( 10.00000000000000000, 0.000000000000000000, 0.000000000000000000 ) ) ;
#23037=EDGE_CURVE ( 'NONE', #50966, #65467, #13474, .T. ) ;
#23038=ADVANCED_FACE ( 'NONE', ( #36016 ), #19462, .T. ) ;
#23042=ORIENTED_EDGE ( 'NONE', *, *, #41191, .F. ) ;
#23074=VECTOR ( 'NONE', #44052, 1000.000000000000000 ) ;
#23090=CARTESIAN_POINT ( 'NONE',  ( 10.00000000000000000, 46.21855187248629449, 62.20884554314036308 ) ) ;
#23093=DIRECTION ( 'NONE',  ( -1.000000000000000000, 0.000000000000000000, 0.000000000000000000 ) ) ;
#23094=CARTESIAN_POINT ( 'NONE',  ( 0.000000000000000000, -54.21277698773715059, 55.38113227695762930 ) ) ;
#23097=ADVANCED_FACE ( 'NONE', ( #45712 ), #29861, .T. ) ;
#23101=ORIENTED_EDGE ( 'NONE', *, *, #16645, .F. ) ;
#23104=AXIS2_PLACEMENT_3D ( 'NONE', #52181, #6698, #5983 ) ;
#23110=ORIENTED_EDGE ( 'NONE', *, *, #54305, .T. ) ;
#23115=CIRCLE ( 'NONE', #33889, 77.49899999999999523 ) ;
#23124=VERTEX_POINT ( 'NONE', #58825 ) ;
#23126=EDGE_LOOP ( 'NONE', ( #6040, #27084, #37480, #44401 ) ) ;
#23127=CARTESIAN_POINT ( 'NONE',  ( 10.00000000000000000, -70.52718814184240159, -26.02418014898383802 ) ) ;
#23133=ORIENTED_EDGE ( 'NONE', *, *, #41345, .T. ) ;
#23137=EDGE_LOOP ( 'NONE', ( #4665, #46863, #56132, #44486 ) ) ;
#23148=ORIENTED_EDGE ( 'NONE', *, *, #26203, .T. ) ;
#23149=CARTESIAN_POINT ( 'NONE',  ( 0.000000000000000000, -73.44644590900077219, 24.73286445877675632 ) ) ;
#23153=ORIENTED_EDGE ( 'NONE', *, *, #40250, .F. ) ;
#23160=ORIENTED_EDGE ( 'NONE', *, *, #73381, .T. ) ;
#23163=CARTESIAN_POINT ( 'NONE',  ( 10.00000000000000000, 59.03342792756328095, -46.54456581323744757 ) ) ;
#23166=ORIENTED_EDGE ( 'NONE', *, *, #330, .T. ) ;
#23171=ORIENTED_EDGE ( 'NONE', *, *, #68867, .T. ) ;
#23174=CIRCLE ( 'NONE', #35124, 32.00000000000000711 ) ;
#23179=FACE_OUTER_BOUND ( 'NONE', #55924, .T. ) ;
#23188=CARTESIAN_POINT ( 'NONE',  ( 10.00000000000000000, 59.46389618801964616, 49.70050353004912580 ) ) ;
#23190=ORIENTED_EDGE ( 'NONE', *, *, #37965, .F. ) ;
#23203=EDGE_CURVE ( 'NONE', #38625, #4854, #12208, .T. ) ;
#23222=VERTEX_POINT ( 'NONE', #57719 ) ;
#23223=CIRCLE ( 'NONE', #27982, 31.99999999999999289 ) ;
#23239=EDGE_LOOP ( 'NONE', ( #3798, #33751, #13103, #20473 ) ) ;
#23241=DIRECTION ( 'NONE',  ( 0.000000000000000000, 0.000000000000000000, 1.000000000000000000 ) ) ;
#23244=ORIENTED_EDGE ( 'NONE', *, *, #2782, .T. ) ;
#23260=DIRECTION ( 'NONE',  ( 0.000000000000000000, 0.000000000000000000, 1.000000000000000000 ) ) ;
#23263=AXIS2_PLACEMENT_3D ( 'NONE', #41981, #13759, #36696 ) ;
#23267=CARTESIAN_POINT ( 'NONE',  ( 10.00000000000000000, 59.03342792756328095, -46.54456581323744757 ) ) ;
#23271=DIRECTION ( 'NONE',  ( -1.000000000000000000, 0.000000000000000000, 0.000000000000000000 ) ) ;
#23272=EDGE_CURVE ( 'NONE', #44625, #45506, #57973, .T. ) ;
#23288=CYLINDRICAL_SURFACE ( 'NONE', #21390, 31.99999999999999289 ) ;
#23296=ORIENTED_EDGE ( 'NONE', *, *, #69999, .F. ) ;
#23322=EDGE_LOOP ( 'NONE', ( #54266, #55590, #35223, #45885 ) ) ;
#23330=EDGE_CURVE ( 'NONE', #52246, #27844, #41188, .T. ) ;
#23333=EDGE_CURVE ( 'NONE', #15290, #49569, #66360, .T. ) ;
#23335=ORIENTED_EDGE ( 'NONE', *, *, #71887, .T. ) ;
#23352=EDGE_CURVE ( 'NONE', #25525, #60600, #47145, .T. ) ;
#23355=CARTESIAN_POINT ( 'NONE',  ( 10.00000000000000000, 77.16300072079698680, -27.74655509720590274 ) ) ;
#23357=CYLINDRICAL_SURFACE ( 'NONE', #35852, 31.99999999999999289 ) ;
#23366=DIRECTION ( 'NONE',  ( -1.000000000000000000, 0.000000000000000000, 0.000000000000000000 ) ) ;
#23367=CARTESIAN_POINT ( 'NONE',  ( 10.00000000000000000, -36.72794159290197769, -65.59268652807249111 ) ) ;
#23370=ADVANCED_FACE ( 'NONE', ( #39289 ), #11085, .T. ) ;
#23379=CYLINDRICAL_SURFACE ( 'NONE', #17353, 31.99999999999999289 ) ;
#23381=AXIS2_PLACEMENT_3D ( 'NONE', #14379, #54606, #72251 ) ;
#23384=DIRECTION ( 'NONE',  ( -1.000000000000000000, 0.000000000000000000, -0.000000000000000000 ) ) ;
#23390=EDGE_LOOP ( 'NONE', ( #63896, #2335, #21065, #14173 ) ) ;
#23409=ORIENTED_EDGE ( 'NONE', *, *, #36584, .F. ) ;
#23411=AXIS2_PLACEMENT_3D ( 'NONE', #5948, #47264, #52902 ) ;
#23416=DIRECTION ( 'NONE',  ( 0.000000000000000000, -0.4539904997395350361, -0.8910065241883738940 ) ) ;
#23424=ORIENTED_EDGE ( 'NONE', *, *, #51618, .F. ) ;
#23426=AXIS2_PLACEMENT_3D ( 'NONE', #32689, #55636, #4152 ) ;
#23428=CIRCLE ( 'NONE', #48639, 77.49900000000000944 ) ;
#23432=LINE ( 'NONE', #1288, #27063 ) ;
#23436=DIRECTION ( 'NONE',  ( 0.000000000000000000, 0.000000000000000000, 1.000000000000000000 ) ) ;
#23437=CIRCLE ( 'NONE', #63063, 31.99999999999998934 ) ;
#23439=ORIENTED_EDGE ( 'NONE', *, *, #20211, .F. ) ;
#23447=DIRECTION ( 'NONE',  ( -1.000000000000000000, -0.000000000000000000, -0.000000000000000000 ) ) ;
#23449=ORIENTED_EDGE ( 'NONE', *, *, #46457, .T. ) ;
#23452=CARTESIAN_POINT ( 'NONE',  ( 10.00000000000000000, 63.18004540533092239, -44.88180994100307686 ) ) ;
#23455=AXIS2_PLACEMENT_3D ( 'NONE', #40366, #51270, #35101 ) ;
#23468=CARTESIAN_POINT ( 'NONE',  ( 0.000000000000000000, -81.90746397400386059, -3.894527615418773347 ) ) ;
#23472=VERTEX_POINT ( 'NONE', #6196 ) ;
#23474=DIRECTION ( 'NONE',  ( -1.000000000000000000, -0.000000000000000000, 0.000000000000000000 ) ) ;
#23475=AXIS2_PLACEMENT_3D ( 'NONE', #57736, #13334, #23513 ) ;
#23479=ORIENTED_EDGE ( 'NONE', *, *, #46671, .F. ) ;
#23481=ORIENTED_EDGE ( 'NONE', *, *, #50167, .F. ) ;
#23484=AXIS2_PLACEMENT_3D ( 'NONE', #5786, #17418, #40351 ) ;
#23492=VERTEX_POINT ( 'NONE', #19304 ) ;
#23496=VECTOR ( 'NONE', #37354, 1000.000000000000000 ) ;
#23497=DIRECTION ( 'NONE',  ( 0.000000000000000000, 0.000000000000000000, 1.000000000000000000 ) ) ;
#23499=ADVANCED_FACE ( 'NONE', ( #12181 ), #6558, .T. ) ;
#23501=FACE_OUTER_BOUND ( 'NONE', #12839, .T. ) ;
#23506=CYLINDRICAL_SURFACE ( 'NONE', #32647, 82.00000000000000000 ) ;
#23513=DIRECTION ( 'NONE',  ( 0.000000000000000000, 0.07845909572783790753, 0.9969173337331285190 ) ) ;
#23521=VERTEX_POINT ( 'NONE', #7299 ) ;
#23522=ORIENTED_EDGE ( 'NONE', *, *, #72158, .F. ) ;
#23534=DIRECTION ( 'NONE',  ( -1.000000000000000000, 0.000000000000000000, 0.000000000000000000 ) ) ;
#23541=CARTESIAN_POINT ( 'NONE',  ( 10.00000000000000000, -62.50329211542407393, -41.76937507738853839 ) ) ;
#23549=CARTESIAN_POINT ( 'NONE',  ( 0.000000000000000000, 75.11764819372149304, -2.946379043146603482 ) ) ;
#23560=CARTESIAN_POINT ( 'NONE',  ( 10.00000000000000000, 0.000000000000000000, 0.000000000000000000 ) ) ;
#23569=FACE_OUTER_BOUND ( 'NONE', #34403, .T. ) ;
#23573=EDGE_CURVE ( 'NONE', #45686, #63002, #17144, .T. ) ;
#23581=AXIS2_PLACEMENT_3D ( 'NONE', #1635, #1996, #13603 ) ;
#23582=CYLINDRICAL_SURFACE ( 'NONE', #68981, 77.49899999999999523 ) ;
#23583=EDGE_CURVE ( 'NONE', #31033, #47197, #24223, .T. ) ;
#23595=AXIS2_PLACEMENT_3D ( 'NONE', #66081, #8170, #2941 ) ;
#23602=CYLINDRICAL_SURFACE ( 'NONE', #18208, 32.00000000000000000 ) ;
#23606=ORIENTED_EDGE ( 'NONE', *, *, #31985, .F. ) ;
#23616=VERTEX_POINT ( 'NONE', #64077 ) ;
#23626=ADVANCED_FACE ( 'NONE', ( #7660 ), #30578, .T. ) ;
#23635=DIRECTION ( 'NONE',  ( -1.000000000000000000, 0.000000000000000000, 0.000000000000000000 ) ) ;
#23636=EDGE_CURVE ( 'NONE', #11405, #7655, #68823, .T. ) ;
#23637=AXIS2_PLACEMENT_3D ( 'NONE', #9364, #27388, #50330 ) ;
#23645=CIRCLE ( 'NONE', #2056, 77.49900000000000944 ) ;
#23646=ORIENTED_EDGE ( 'NONE', *, *, #72287, .T. ) ;
#23649=DIRECTION ( 'NONE',  ( -1.000000000000000000, 0.000000000000000000, 0.000000000000000000 ) ) ;
#23665=ORIENTED_EDGE ( 'NONE', *, *, #14699, .T. ) ;
#23669=CARTESIAN_POINT ( 'NONE',  ( 5.000000000000000000, 46.11716303203188261, 67.80270845531904911 ) ) ;
#23671=DIRECTION ( 'NONE',  ( -1.000000000000000000, 0.000000000000000000, 0.000000000000000000 ) ) ;
#23674=ADVANCED_FACE ( 'NONE', ( #71906 ), #49711, .T. ) ;
#23679=VECTOR ( 'NONE', #18705, 1000.000000000000000 ) ;
#23687=ORIENTED_EDGE ( 'NONE', *, *, #7165, .F. ) ;
#23690=ORIENTED_EDGE ( 'NONE', *, *, #27988, .F. ) ;
#23698=EDGE_LOOP ( 'NONE', ( #20982, #24932, #43056, #72648 ) ) ;
#23703=FACE_OUTER_BOUND ( 'NONE', #64373, .T. ) ;
#23713=CYLINDRICAL_SURFACE ( 'NONE', #31515, 31.99999999999999289 ) ;
#23714=CIRCLE ( 'NONE', #32124, 77.49899999999999523 ) ;
#23720=DIRECTION ( 'NONE',  ( 0.000000000000000000, 0.000000000000000000, 1.000000000000000000 ) ) ;
#23724=FACE_OUTER_BOUND ( 'NONE', #23698, .T. ) ;
#23730=DIRECTION ( 'NONE',  ( -1.000000000000000000, -0.000000000000000000, -0.000000000000000000 ) ) ;
#23734=AXIS2_PLACEMENT_3D ( 'NONE', #59216, #31001, #65604 ) ;
#23739=CARTESIAN_POINT ( 'NONE',  ( 0.000000000000000000, 33.71516098798849015, -74.74816331893394761 ) ) ;
#23744=ORIENTED_EDGE ( 'NONE', *, *, #63338, .T. ) ;
#23747=CARTESIAN_POINT ( 'NONE',  ( 10.00000000000000000, -46.11716303203234446, 67.80270845531873647 ) ) ;
#23758=ORIENTED_EDGE ( 'NONE', *, *, #26796, .T. ) ;
#23760=CARTESIAN_POINT ( 'NONE',  ( 10.00000000000000000, -55.19960302592104284, 51.03279382321070301 ) ) ;
#23762=EDGE_CURVE ( 'NONE', #7032, #14681, #37722, .T. ) ;
#23776=CARTESIAN_POINT ( 'NONE',  ( 10.00000000000000000, 44.88180994100376608, 63.18004540533043922 ) ) ;
#23783=ADVANCED_FACE ( 'NONE', ( #55369 ), #61007, .T. ) ;
#23790=VECTOR ( 'NONE', #15994, 1000.000000000000000 ) ;
#23791=CARTESIAN_POINT ( 'NONE',  ( 10.00000000000000000, 33.71516098798847594, -74.74816331893393340 ) ) ;
#23797=CARTESIAN_POINT ( 'NONE',  ( 0.000000000000000000, 74.65374052328660071, -8.840884882374309583 ) ) ;
#23814=DIRECTION ( 'NONE',  ( -1.000000000000000000, -0.000000000000000000, 0.000000000000000000 ) ) ;
#23817=DIRECTION ( 'NONE',  ( -1.000000000000000000, 0.000000000000000000, 0.000000000000000000 ) ) ;
#23818=AXIS2_PLACEMENT_3D ( 'NONE', #49483, #71289, #31072 ) ;
#23819=CARTESIAN_POINT ( 'NONE',  ( 0.000000000000000000, 0.000000000000000000, 0.000000000000000000 ) ) ;
#23822=AXIS2_PLACEMENT_3D ( 'NONE', #47882, #59173, #7662 ) ;
#23830=ORIENTED_EDGE ( 'NONE', *, *, #29973, .T. ) ;
#23833=LINE ( 'NONE', #18190, #40221 ) ;
#23839=DIRECTION ( 'NONE',  ( -1.000000000000000000, 0.000000000000000000, -0.000000000000000000 ) ) ;
#23846=CARTESIAN_POINT ( 'NONE',  ( 5.000000000000002665, -68.55367621811173251, 44.99326035066031437 ) ) ;
#23859=ORIENTED_EDGE ( 'NONE', *, *, #18438, .F. ) ;
#23865=ORIENTED_EDGE ( 'NONE', *, *, #70191, .F. ) ;
#23880=FACE_OUTER_BOUND ( 'NONE', #51583, .T. ) ;
#23886=ORIENTED_EDGE ( 'NONE', *, *, #73993, .F. ) ;
#23892=LINE ( 'NONE', #7700, #54616 ) ;
#23895=VERTEX_POINT ( 'NONE', #46227 ) ;
#23906=CARTESIAN_POINT ( 'NONE',  ( 5.000000000000002665, -74.18225833017864090, -34.94270380257719211 ) ) ;
#23909=DIRECTION ( 'NONE',  ( -1.000000000000000000, 0.000000000000000000, 0.000000000000000000 ) ) ;
#23910=AXIS2_PLACEMENT_3D ( 'NONE', #63149, #7467, #64612 ) ;
#23912=CARTESIAN_POINT ( 'NONE',  ( 0.000000000000000000, -77.32052557432845674, 5.256550761632577284 ) ) ;
#23920=DIRECTION ( 'NONE',  ( 0.000000000000000000, 0.000000000000000000, 1.000000000000000000 ) ) ;
#23922=VERTEX_POINT ( 'NONE', #57512 ) ;
#23930=CIRCLE ( 'NONE', #11890, 77.49900000000000944 ) ;
#23940=ORIENTED_EDGE ( 'NONE', *, *, #67126, .F. ) ;
#23944=CARTESIAN_POINT ( 'NONE',  ( 0.000000000000000000, -55.19960302592104284, 51.03279382321070301 ) ) ;
#23949=FACE_OUTER_BOUND ( 'NONE', #69969, .T. ) ;
#23961=CARTESIAN_POINT ( 'NONE',  ( 0.000000000000000000, 35.91791733033475253, 68.67312586195009771 ) ) ;
#23978=AXIS2_PLACEMENT_3D ( 'NONE', #69918, #18417, #42476 ) ;
#23984=CIRCLE ( 'NONE', #25212, 31.99999999999999289 ) ;
#23985=CARTESIAN_POINT ( 'NONE',  ( 0.000000000000000000, -27.74655509720617275, -77.16300072079690153 ) ) ;
#23989=CIRCLE ( 'NONE', #33571, 31.99999999999999289 ) ;
#23997=ORIENTED_EDGE ( 'NONE', *, *, #42435, .F. ) ;
#24019=DIRECTION ( 'NONE',  ( 0.000000000000000000, -0.3826834323650772363, -0.9238795325112919565 ) ) ;
#24025=CARTESIAN_POINT ( 'NONE',  ( 0.000000000000000000, 75.11725578898467859, 2.956366410620910656 ) ) ;
#24036=AXIS2_PLACEMENT_3D ( 'NONE', #53814, #2359, #71090 ) ;
#24045=VERTEX_POINT ( 'NONE', #19850 ) ;
#24050=AXIS2_PLACEMENT_3D ( 'NONE', #35647, #30742, #58973 ) ;
#24051=ADVANCED_FACE ( 'NONE', ( #48434 ), #60834, .T. ) ;
#24053=CYLINDRICAL_SURFACE ( 'NONE', #56151, 31.99999999999999289 ) ;
#24061=CARTESIAN_POINT ( 'NONE',  ( 0.000000000000000000, 70.53064760720316428, -26.01480285779861035 ) ) ;
#24062=EDGE_CURVE ( 'NONE', #42442, #21857, #50819, .T. ) ;
#24070=VECTOR ( 'NONE', #49513, 1000.000000000000000 ) ;
#24072=SURFACE_STYLE_USAGE ( .BOTH. , #29308 ) ;
#24077=ORIENTED_EDGE ( 'NONE', *, *, #34957, .T. ) ;
#24085=DIRECTION ( 'NONE',  ( -1.000000000000000000, -0.000000000000000000, 0.000000000000000000 ) ) ;
#24124=EDGE_CURVE ( 'NONE', #29107, #57325, #56686, .T. ) ;
#24136=EDGE_LOOP ( 'NONE', ( #55271, #52681, #67349, #34059 ) ) ;
#24138=EDGE_LOOP ( 'NONE', ( #18244, #17659, #37355, #54020 ) ) ;
#24154=EDGE_LOOP ( 'NONE', ( #40388, #34027, #11273, #43927 ) ) ;
#24156=ORIENTED_EDGE ( 'NONE', *, *, #21105, .T. ) ;
#24161=CARTESIAN_POINT ( 'NONE',  ( 0.000000000000000000, 29.01471420065674423, -76.69515212745984911 ) ) ;
#24163=DIRECTION ( 'NONE',  ( 0.000000000000000000, -0.9723699203976741146, -0.2334453638559159938 ) ) ;
#24166=ORIENTED_EDGE ( 'NONE', *, *, #39758, .T. ) ;
#24168=ORIENTED_EDGE ( 'NONE', *, *, #67013, .F. ) ;
#24172=CARTESIAN_POINT ( 'NONE',  ( 5.000000000000000000, 2.543863470248396208, 81.96053171279903893 ) ) ;
#24180=LINE ( 'NONE', #47834, #19075 ) ;
#24183=ORIENTED_EDGE ( 'NONE', *, *, #23762, .F. ) ;
#24196=CARTESIAN_POINT ( 'NONE',  ( 10.00000000000000000, -73.73191006444582740, 14.66109333815435889 ) ) ;
#24197=AXIS2_PLACEMENT_3D ( 'NONE', #183, #11045, #51630 ) ;
#24208=EDGE_CURVE ( 'NONE', #27575, #38312, #71252, .T. ) ;
#24211=CARTESIAN_POINT ( 'NONE',  ( 5.000000000000002665, 22.90783923731741112, -78.73519480814930205 ) ) ;
#24223=LINE ( 'NONE', #58056, #26719 ) ;
#24236=VERTEX_POINT ( 'NONE', #57793 ) ;
#24249=DIRECTION ( 'NONE',  ( -1.000000000000000000, 0.000000000000000000, 0.000000000000000000 ) ) ;
#24256=ORIENTED_EDGE ( 'NONE', *, *, #58943, .F. ) ;
#24275=LINE ( 'NONE', #35176, #61774 ) ;
#24281=CARTESIAN_POINT ( 'NONE',  ( 10.00000000000000000, -69.42325613327466272, 34.44570377933573724 ) ) ;
#24282=VECTOR ( 'NONE', #22911, 1000.000000000000000 ) ;
#24306=EDGE_CURVE ( 'NONE', #28882, #4362, #70034, .T. ) ;
#24315=CARTESIAN_POINT ( 'NONE',  ( 10.00000000000000000, 28.89263327155850902, -71.91182617369157981 ) ) ;
#24317=DIRECTION ( 'NONE',  ( 0.000000000000000000, 0.000000000000000000, 1.000000000000000000 ) ) ;
#24328=CARTESIAN_POINT ( 'NONE',  ( 10.00000000000000000, -49.70050353004846500, -59.46389618802017907 ) ) ;
#24336=VERTEX_POINT ( 'NONE', #25787 ) ;
#24342=DIRECTION ( 'NONE',  ( -1.000000000000000000, 0.000000000000000000, 0.000000000000000000 ) ) ;
#24355=LINE ( 'NONE', #13436, #30012 ) ;
#24362=EDGE_CURVE ( 'NONE', #36877, #60490, #58079, .T. ) ;
#24368=CARTESIAN_POINT ( 'NONE',  ( -10.00000000000000000, 0.000000000000000000, 0.000000000000000000 ) ) ;
#24369=CARTESIAN_POINT ( 'NONE',  ( 10.00000000000000000, 73.73191006444572793, -14.66109333815486515 ) ) ;
#24371=CARTESIAN_POINT ( 'NONE',  ( 10.00000000000000000, 0.000000000000000000, 0.000000000000000000 ) ) ;
#24373=CARTESIAN_POINT ( 'NONE',  ( -10.00000000000000000, 0.000000000000000000, 0.000000000000000000 ) ) ;
#24374=ADVANCED_FACE ( 'NONE', ( #30674 ), #19766, .T. ) ;
#24382=ADVANCED_FACE ( 'NONE', ( #70517 ), #25048, .T. ) ;
#24384=CIRCLE ( 'NONE', #54434, 31.99999999999999289 ) ;
#24389=FACE_OUTER_BOUND ( 'NONE', #9780, .T. ) ;
#24394=EDGE_LOOP ( 'NONE', ( #22211, #6216, #61901, #31803 ) ) ;
#24396=ORIENTED_EDGE ( 'NONE', *, *, #71170, .T. ) ;
#24411=ORIENTED_EDGE ( 'NONE', *, *, #26585, .F. ) ;
#24416=ORIENTED_EDGE ( 'NONE', *, *, #27334, .T. ) ;
#24426=ADVANCED_FACE ( 'NONE', ( #64913 ), #48716, .T. ) ;
#24427=VECTOR ( 'NONE', #16451, 1000.000000000000000 ) ;
#24437=DIRECTION ( 'NONE',  ( 0.000000000000000000, -0.1564344650402170744, -0.9876883405951398798 ) ) ;
#24443=DIRECTION ( 'NONE',  ( 0.000000000000000000, 0.000000000000000000, 1.000000000000000000 ) ) ;
#24446=CARTESIAN_POINT ( 'NONE',  ( 10.00000000000000000, -76.66974797899844418, 11.30684508768314522 ) ) ;
#24452=DIRECTION ( 'NONE',  ( -1.000000000000000000, 0.000000000000000000, -0.000000000000000000 ) ) ;
#24455=CARTESIAN_POINT ( 'NONE',  ( 0.000000000000000000, -36.73666225445940370, 65.58780272294062286 ) ) ;
#24460=EDGE_CURVE ( 'NONE', #32358, #59815, #16059, .T. ) ;
#24461=DIRECTION ( 'NONE',  ( -1.000000000000000000, -0.000000000000000000, -0.000000000000000000 ) ) ;
#24466=DIRECTION ( 'NONE',  ( 0.000000000000000000, 0.000000000000000000, 1.000000000000000000 ) ) ;
#24467=CYLINDRICAL_SURFACE ( 'NONE', #53897, 31.99999999999998579 ) ;
#24468=CYLINDRICAL_SURFACE ( 'NONE', #11761, 31.99999999999999289 ) ;
#24469=FACE_OUTER_BOUND ( 'NONE', #65006, .T. ) ;
#24474=DIRECTION ( 'NONE',  ( 0.000000000000000000, -0.07845909572783058006, -0.9969173337331290741 ) ) ;
#24477=CIRCLE ( 'NONE', #43705, 31.99999999999999289 ) ;
#24480=FACE_OUTER_BOUND ( 'NONE', #52437, .T. ) ;
#24489=CARTESIAN_POINT ( 'NONE',  ( 10.00000000000000000, 0.000000000000000000, 0.000000000000000000 ) ) ;
#24500=DIRECTION ( 'NONE',  ( 0.000000000000000000, 0.7604059656000323741, -0.6494480483301819929 ) ) ;
#24507=EDGE_CURVE ( 'NONE', #68917, #59010, #5246, .T. ) ;
#24526=ADVANCED_FACE ( 'NONE', ( #62235 ), #56219, .T. ) ;
#24532=DIRECTION ( 'NONE',  ( -1.000000000000000000, 0.000000000000000000, 0.000000000000000000 ) ) ;
#24534=DIRECTION ( 'NONE',  ( -1.000000000000000000, -0.000000000000000000, 0.000000000000000000 ) ) ;
#24535=CARTESIAN_POINT ( 'NONE',  ( 10.00000000000000000, 59.03961581697465277, -46.53671651293886669 ) ) ;
#24563=CARTESIAN_POINT ( 'NONE',  ( 10.00000000000000000, -51.29473840253269401, 63.97538442413405591 ) ) ;
#24564=ADVANCED_FACE ( 'NONE', ( #47797 ), #13941, .T. ) ;
#24565=AXIS2_PLACEMENT_3D ( 'NONE', #25141, #70982, #66478 ) ;
#24567=AXIS2_PLACEMENT_3D ( 'NONE', #68909, #25625, #7600 ) ;
#24570=VERTEX_POINT ( 'NONE', #5477 ) ;
#24588=ORIENTED_EDGE ( 'NONE', *, *, #34209, .F. ) ;
#24596=EDGE_LOOP ( 'NONE', ( #67989, #12727, #61703, #21001 ) ) ;
#24600=VECTOR ( 'NONE', #4246, 1000.000000000000000 ) ;
#24601=DIRECTION ( 'NONE',  ( 0.000000000000000000, 0.000000000000000000, 1.000000000000000000 ) ) ;
#24606=CARTESIAN_POINT ( 'NONE',  ( 10.00000000000000000, -8.830959090341869100, -74.65491531819127147 ) ) ;
#24611=ORIENTED_EDGE ( 'NONE', *, *, #27702, .F. ) ;
#24614=ADVANCED_FACE ( 'NONE', ( #70714 ), #36511, .T. ) ;
#24620=CIRCLE ( 'NONE', #40237, 77.49900000000000944 ) ;
#24623=ORIENTED_EDGE ( 'NONE', *, *, #5529, .F. ) ;
#24632=FACE_OUTER_BOUND ( 'NONE', #16053, .T. ) ;
#24640=EDGE_CURVE ( 'NONE', #10916, #36728, #16111, .T. ) ;
#24641=AXIS2_PLACEMENT_3D ( 'NONE', #30324, #1805, #335 ) ;
#24642=DIRECTION ( 'NONE',  ( 0.000000000000000000, 0.000000000000000000, -1.000000000000000000 ) ) ;
#24643=LINE ( 'NONE', #43059, #34627 ) ;
#24648=DIRECTION ( 'NONE',  ( -1.000000000000000000, 0.000000000000000000, 0.000000000000000000 ) ) ;
#24652=AXIS2_PLACEMENT_3D ( 'NONE', #64293, #43505, #49484 ) ;
#24661=AXIS2_PLACEMENT_3D ( 'NONE', #41557, #57379, #29897 ) ;
#24665=AXIS2_PLACEMENT_3D ( 'NONE', #69291, #6873, #70013 ) ;
#24672=DIRECTION ( 'NONE',  ( 0.000000000000000000, 0.000000000000000000, 1.000000000000000000 ) ) ;
#24674=CARTESIAN_POINT ( 'NONE',  ( 0.000000000000000000, 0.000000000000000000, 0.000000000000000000 ) ) ;
#24675=LINE ( 'NONE', #24315, #18418 ) ;
#24682=EDGE_CURVE ( 'NONE', #54289, #48877, #61735, .T. ) ;
#24709=ORIENTED_EDGE ( 'NONE', *, *, #50315, .T. ) ;
#24715=ORIENTED_EDGE ( 'NONE', *, *, #73691, .F. ) ;
#24726=VERTEX_POINT ( 'NONE', #31244 ) ;
#24737=CARTESIAN_POINT ( 'NONE',  ( 10.00000000000000000, 0.000000000000000000, 0.000000000000000000 ) ) ;
#24742=EDGE_LOOP ( 'NONE', ( #10619, #15926, #63367, #52418 ) ) ;
#24752=CYLINDRICAL_SURFACE ( 'NONE', #64486, 32.00000000000000000 ) ;
#24769=ORIENTED_EDGE ( 'NONE', *, *, #28168, .F. ) ;
#24776=ORIENTED_EDGE ( 'NONE', *, *, #8913, .T. ) ;
#24780=ORIENTED_EDGE ( 'NONE', *, *, #69370, .F. ) ;
#24786=EDGE_CURVE ( 'NONE', #70328, #26342, #19955, .T. ) ;
#24788=ORIENTED_EDGE ( 'NONE', *, *, #58047, .F. ) ;
#24800=ADVANCED_FACE ( 'NONE', ( #72562 ), #15060, .T. ) ;
#24802=EDGE_CURVE ( 'NONE', #23521, #30219, #65839, .T. ) ;
#24804=CYLINDRICAL_SURFACE ( 'NONE', #25094, 32.00000000000000000 ) ;
#24805=VERTEX_POINT ( 'NONE', #61314 ) ;
#24809=EDGE_CURVE ( 'NONE', #61936, #37997, #49275, .T. ) ;
#24810=CARTESIAN_POINT ( 'NONE',  ( 10.00000000000000000, 26.02418014898407961, -70.52718814184231633 ) ) ;
#24811=VECTOR ( 'NONE', #25919, 1000.000000000000000 ) ;
#24815=AXIS2_PLACEMENT_3D ( 'NONE', #72202, #50755, #16550 ) ;
#24817=CIRCLE ( 'NONE', #74073, 31.99999999999999289 ) ;
#24819=FACE_OUTER_BOUND ( 'NONE', #69159, .T. ) ;
#24825=CARTESIAN_POINT ( 'NONE',  ( 0.000000000000000000, -75.54627589209931671, -17.28742895386164591 ) ) ;
#24827=AXIS2_PLACEMENT_3D ( 'NONE', #65792, #8267, #9011 ) ;
#24832=CYLINDRICAL_SURFACE ( 'NONE', #46560, 82.00000000000000000 ) ;
#24836=VERTEX_POINT ( 'NONE', #55660 ) ;
#24840=DIRECTION ( 'NONE',  ( 1.000000000000000000, -0.000000000000000000, -0.000000000000000000 ) ) ;
#24843=CARTESIAN_POINT ( 'NONE',  ( -10.00000000000000000, 0.000000000000000000, 0.000000000000000000 ) ) ;
#24848=ORIENTED_EDGE ( 'NONE', *, *, #61477, .F. ) ;
#24853=ORIENTED_EDGE ( 'NONE', *, *, #36217, .T. ) ;
#24857=VERTEX_POINT ( 'NONE', #72201 ) ;
#24863=EDGE_LOOP ( 'NONE', ( #72018, #68822, #47376, #25178 ) ) ;
#24865=CIRCLE ( 'NONE', #26041, 32.00000000000000000 ) ;
#24866=ORIENTED_EDGE ( 'NONE', *, *, #56873, .F. ) ;
#24868=DIRECTION ( 'NONE',  ( 0.000000000000000000, 0.000000000000000000, 1.000000000000000000 ) ) ;
#24871=LINE ( 'NONE', #41792, #69419 ) ;
#24874=CARTESIAN_POINT ( 'NONE',  ( 0.000000000000000000, 0.000000000000000000, 0.000000000000000000 ) ) ;
#24882=DIRECTION ( 'NONE',  ( 1.000000000000000000, -0.000000000000000000, -0.000000000000000000 ) ) ;
#24906=ORIENTED_EDGE ( 'NONE', *, *, #29338, .T. ) ;
#24912=DIRECTION ( 'NONE',  ( -1.000000000000000000, 0.000000000000000000, 0.000000000000000000 ) ) ;
#24917=ORIENTED_EDGE ( 'NONE', *, *, #61876, .T. ) ;
#24918=DIRECTION ( 'NONE',  ( 0.000000000000000000, 0.000000000000000000, 1.000000000000000000 ) ) ;
#24921=DIRECTION ( 'NONE',  ( 0.000000000000000000, -0.2334453638559126909, 0.9723699203976748917 ) ) ;
#24922=AXIS2_PLACEMENT_3D ( 'NONE', #32662, #60520, #55231 ) ;
#24927=DIRECTION ( 'NONE',  ( -1.000000000000000000, 0.000000000000000000, 0.000000000000000000 ) ) ;
#24929=EDGE_CURVE ( 'NONE', #14882, #9779, #5297, .T. ) ;
#24932=ORIENTED_EDGE ( 'NONE', *, *, #17264, .F. ) ;
#24937=CIRCLE ( 'NONE', #35714, 77.49900000000000944 ) ;
#24956=ORIENTED_EDGE ( 'NONE', *, *, #74005, .F. ) ;
#24974=DIRECTION ( 'NONE',  ( 0.000000000000000000, 0.000000000000000000, 1.000000000000000000 ) ) ;
#24982=ORIENTED_EDGE ( 'NONE', *, *, #8442, .F. ) ;
#24989=DIRECTION ( 'NONE',  ( -1.000000000000000000, -0.000000000000000000, 0.000000000000000000 ) ) ;
#24998=CARTESIAN_POINT ( 'NONE',  ( 10.00000000000000000, -46.54456581323847786, 59.03342792756247093 ) ) ;
#25004=VERTEX_POINT ( 'NONE', #59002 ) ;
#25010=DIRECTION ( 'NONE',  ( -1.000000000000000000, 0.000000000000000000, 0.000000000000000000 ) ) ;
#25014=DIRECTION ( 'NONE',  ( 1.000000000000000000, -0.000000000000000000, -0.000000000000000000 ) ) ;
#25016=AXIS2_PLACEMENT_3D ( 'NONE', #8091, #23534, #53583 ) ;
#25019=CARTESIAN_POINT ( 'NONE',  ( 10.00000000000000000, 74.65374052328660071, -8.840884882374309583 ) ) ;
#25041=EDGE_CURVE ( 'NONE', #1142, #3906, #44996, .T. ) ;
#25047=CIRCLE ( 'NONE', #14258, 31.99999999999999645 ) ;
#25048=CYLINDRICAL_SURFACE ( 'NONE', #23263, 77.49899999999999523 ) ;
#25049=CARTESIAN_POINT ( 'NONE',  ( 10.00000000000000000, 0.000000000000000000, 0.000000000000000000 ) ) ;
#25050=DIRECTION ( 'NONE',  ( -1.000000000000000000, 0.000000000000000000, 0.000000000000000000 ) ) ;
#25066=ORIENTED_EDGE ( 'NONE', *, *, #12819, .T. ) ;
#25075=AXIS2_PLACEMENT_3D ( 'NONE', #70675, #19190, #48505 ) ;
#25079=EDGE_LOOP ( 'NONE', ( #31259, #1552, #17971, #40675 ) ) ;
#25080=DIRECTION ( 'NONE',  ( -1.000000000000000000, 0.000000000000000000, 0.000000000000000000 ) ) ;
#25083=CIRCLE ( 'NONE', #1136, 77.49899999999999523 ) ;
#25094=AXIS2_PLACEMENT_3D ( 'NONE', #29688, #53019, #18782 ) ;
#25095=ORIENTED_EDGE ( 'NONE', *, *, #61209, .F. ) ;
#25096=DIRECTION ( 'NONE',  ( 0.000000000000000000, 0.000000000000000000, -1.000000000000000000 ) ) ;
#25103=DIRECTION ( 'NONE',  ( 0.000000000000000000, 0.2334453638559060296, -0.9723699203976764460 ) ) ;
#25105=AXIS2_PLACEMENT_3D ( 'NONE', #2982, #14219, #58610 ) ;
#25111=AXIS2_PLACEMENT_3D ( 'NONE', #45308, #45685, #57695 ) ;
#25114=EDGE_CURVE ( 'NONE', #5572, #40918, #1890, .T. ) ;
#25121=EDGE_CURVE ( 'NONE', #28563, #11928, #42082, .T. ) ;
#25124=ORIENTED_EDGE ( 'NONE', *, *, #6366, .T. ) ;
#25125=EDGE_CURVE ( 'NONE', #28680, #31033, #4153, .T. ) ;
#25126=VECTOR ( 'NONE', #28309, 1000.000000000000000 ) ;
#25127=LINE ( 'NONE', #65359, #21043 ) ;
#25129=DIRECTION ( 'NONE',  ( -1.000000000000000000, 0.000000000000000000, 0.000000000000000000 ) ) ;
#25132=AXIS2_PLACEMENT_3D ( 'NONE', #48308, #14463, #42671 ) ;
#25141=CARTESIAN_POINT ( 'NONE',  ( 10.00000000000000000, -74.65374052328654386, 8.840884882374837161 ) ) ;
#25145=VECTOR ( 'NONE', #28498, 1000.000000000000000 ) ;
#25151=EDGE_CURVE ( 'NONE', #11217, #72850, #48814, .T. ) ;
#25153=AXIS2_PLACEMENT_3D ( 'NONE', #66857, #15728, #14233 ) ;
#25154=SHAPE_REPRESENTATION_RELATIONSHIP ( 'NONE' , 'NONE' ,  #49787, #40864 ) ;
#25163=LINE ( 'NONE', #69898, #34491 ) ;
#25178=ORIENTED_EDGE ( 'NONE', *, *, #16916, .F. ) ;
#25180=CARTESIAN_POINT ( 'NONE',  ( 10.00000000000000000, 59.03961581697399907, 46.53671651293969802 ) ) ;
#25200=LINE ( 'NONE', #2303, #33235 ) ;
#25202=DIRECTION ( 'NONE',  ( 0.000000000000000000, 0.000000000000000000, -1.000000000000000000 ) ) ;
#25206=EDGE_CURVE ( 'NONE', #16727, #1777, #46175, .T. ) ;
#25210=CIRCLE ( 'NONE', #33627, 31.99999999999999289 ) ;
#25211=FACE_OUTER_BOUND ( 'NONE', #44270, .T. ) ;
#25212=AXIS2_PLACEMENT_3D ( 'NONE', #37407, #9557, #2844 ) ;
#25220=CARTESIAN_POINT ( 'NONE',  ( 10.00000000000000000, -59.03961581697367933, -46.53671651294010303 ) ) ;
#25224=DIRECTION ( 'NONE',  ( 1.000000000000000000, -0.000000000000000000, 0.000000000000000000 ) ) ;
#25227=EDGE_CURVE ( 'NONE', #42699, #37771, #64212, .T. ) ;
#25232=CIRCLE ( 'NONE', #47872, 82.00000000000000000 ) ;
#25249=DIRECTION ( 'NONE',  ( 0.000000000000000000, 0.000000000000000000, -1.000000000000000000 ) ) ;
#25251=ORIENTED_EDGE ( 'NONE', *, *, #69707, .F. ) ;
#25252=LINE ( 'NONE', #18852, #43041 ) ;
#25258=EDGE_LOOP ( 'NONE', ( #16160, #14981, #15744, #16063 ) ) ;
#25259=AXIS2_PLACEMENT_3D ( 'NONE', #34178, #74020, #16145 ) ;
#25267=CARTESIAN_POINT ( 'NONE',  ( 10.00000000000000000, 0.000000000000000000, 0.000000000000000000 ) ) ;
#25281=DIRECTION ( 'NONE',  ( 0.000000000000000000, 0.000000000000000000, 1.000000000000000000 ) ) ;
#25291=EDGE_CURVE ( 'NONE', #5465, #20634, #30534, .T. ) ;
#25292=DIRECTION ( 'NONE',  ( 0.000000000000000000, 0.000000000000000000, 1.000000000000000000 ) ) ;
#25297=EDGE_LOOP ( 'NONE', ( #33471, #25095, #13213, #39976 ) ) ;
#25299=EDGE_CURVE ( 'NONE', #5973, #17422, #61227, .T. ) ;
#25313=CIRCLE ( 'NONE', #133, 12.50000000000000000 ) ;
#25314=ORIENTED_EDGE ( 'NONE', *, *, #7165, .T. ) ;
#25326=DIRECTION ( 'NONE',  ( -1.000000000000000000, 0.000000000000000000, 0.000000000000000000 ) ) ;
#25328=VERTEX_POINT ( 'NONE', #62727 ) ;
#25329=DIRECTION ( 'NONE',  ( 0.000000000000000000, 0.000000000000000000, 1.000000000000000000 ) ) ;
#25332=DIRECTION ( 'NONE',  ( 0.000000000000000000, 0.7071067811865489050, -0.7071067811865462405 ) ) ;
#25345=AXIS2_PLACEMENT_3D ( 'NONE', #44635, #28059, #33706 ) ;
#25349=EDGE_LOOP ( 'NONE', ( #22963, #67230, #57829, #36537 ) ) ;
#25351=CARTESIAN_POINT ( 'NONE',  ( 0.000000000000000000, -80.55351364060578589, -15.33399622253568673 ) ) ;
#25356=LINE ( 'NONE', #3557, #32406 ) ;
#25369=AXIS2_PLACEMENT_3D ( 'NONE', #10869, #6349, #39443 ) ;
#25373=AXIS2_PLACEMENT_3D ( 'NONE', #24535, #3113, #26007 ) ;
#25380=EDGE_CURVE ( 'NONE', #69749, #52333, #5399, .T. ) ;
#25385=DIRECTION ( 'NONE',  ( 0.000000000000000000, 0.000000000000000000, 1.000000000000000000 ) ) ;
#25386=CARTESIAN_POINT ( 'NONE',  ( 10.00000000000000000, 3.894527615419054456, -81.90746397400386059 ) ) ;
#25387=ORIENTED_EDGE ( 'NONE', *, *, #15339, .T. ) ;
#25390=LINE ( 'NONE', #14087, #64296 ) ;
#25392=CARTESIAN_POINT ( 'NONE',  ( 10.00000000000000000, 49.70050353004977239, -59.46389618801908483 ) ) ;
#25393=CARTESIAN_POINT ( 'NONE',  ( 10.00000000000000000, 63.97538442413425486, 51.29473840253247374 ) ) ;
#25395=DIRECTION ( 'NONE',  ( 0.000000000000000000, 0.000000000000000000, 1.000000000000000000 ) ) ;
#25404=AXIS2_PLACEMENT_3D ( 'NONE', #32007, #13973, #7611 ) ;
#25407=EDGE_CURVE ( 'NONE', #23895, #57460, #72838, .T. ) ;
#25420=AXIS2_PLACEMENT_3D ( 'NONE', #69689, #19290, #41485 ) ;
#25424=CARTESIAN_POINT ( 'NONE',  ( 10.00000000000000000, -59.03961581697367933, -46.53671651294010303 ) ) ;
#25427=DIRECTION ( 'NONE',  ( -1.000000000000000000, -0.000000000000000000, -0.000000000000000000 ) ) ;
#25428=CYLINDRICAL_SURFACE ( 'NONE', #21319, 32.00000000000000000 ) ;
#25432=VERTEX_POINT ( 'NONE', #73224 ) ;
#25445=DIRECTION ( 'NONE',  ( -1.000000000000000000, 0.000000000000000000, 0.000000000000000000 ) ) ;
#25448=COLOUR_RGB ( '', 0.08235294, 0.09019608, 0.10196078) ;
#25471=AXIS2_PLACEMENT_3D ( 'NONE', #69072, #52139, #6653 ) ;
#25475=CARTESIAN_POINT ( 'NONE',  ( 5.000000000000000000, -71.21200624218768382, -40.65526001592689909 ) ) ;
#25476=LINE ( 'NONE', #69488, #18045 ) ;
#25481=CARTESIAN_POINT ( 'NONE',  ( 0.000000000000000000, -31.47745569255092235, -68.26794271651296242 ) ) ;
#25484=EDGE_CURVE ( 'NONE', #48015, #65118, #66557, .T. ) ;
#25497=AXIS2_PLACEMENT_3D ( 'NONE', #31373, #9189, #3577 ) ;
#25498=DIRECTION ( 'NONE',  ( 0.000000000000000000, 0.8526401643540935105, -0.5224985647159466895 ) ) ;
#25501=CIRCLE ( 'NONE', #51918, 82.00000000000000000 ) ;
#25507=LINE ( 'NONE', #36785, #19088 ) ;
#25512=AXIS2_PLACEMENT_3D ( 'NONE', #50043, #43338, #72970 ) ;
#25519=CARTESIAN_POINT ( 'NONE',  ( 10.00000000000000000, 62.50884508063427347, 41.76106447765511831 ) ) ;
#25521=VERTEX_POINT ( 'NONE', #52150 ) ;
#25525=VERTEX_POINT ( 'NONE', #24328 ) ;
#25527=EDGE_CURVE ( 'NONE', #12032, #33095, #73842, .T. ) ;
#25528=CARTESIAN_POINT ( 'NONE',  ( 0.000000000000000000, -76.69515212745996280, -29.01471420065644580 ) ) ;
#25532=ORIENTED_EDGE ( 'NONE', *, *, #52710, .T. ) ;
#25537=EDGE_CURVE ( 'NONE', #42721, #2983, #66614, .T. ) ;
#25539=ORIENTED_EDGE ( 'NONE', *, *, #36584, .T. ) ;
#25541=CARTESIAN_POINT ( 'NONE',  ( 10.00000000000000000, 51.29473840253317718, -63.97538442413367932 ) ) ;
#25542=EDGE_LOOP ( 'NONE', ( #15268, #23153, #38275, #54543 ) ) ;
#25543=DIRECTION ( 'NONE',  ( -1.000000000000000000, -0.000000000000000000, 0.000000000000000000 ) ) ;
#25547=DIRECTION ( 'NONE',  ( 0.000000000000000000, 0.000000000000000000, 1.000000000000000000 ) ) ;
#25550=CARTESIAN_POINT ( 'NONE',  ( 10.00000000000000000, 81.50828551894240093, -8.966570791699799869 ) ) ;
#25554=CARTESIAN_POINT ( 'NONE',  ( 0.000000000000000000, -36.72794159290197769, -65.59268652807249111 ) ) ;
#25571=AXIS2_PLACEMENT_3D ( 'NONE', #13076, #19823, #26580 ) ;
#25577=DIRECTION ( 'NONE',  ( -1.000000000000000000, 0.000000000000000000, 0.000000000000000000 ) ) ;
#25591=DIRECTION ( 'NONE',  ( 0.000000000000000000, 0.000000000000000000, 1.000000000000000000 ) ) ;
#25606=ADVANCED_FACE ( 'NONE', ( #60765 ), #42728, .T. ) ;
#25607=CIRCLE ( 'NONE', #67647, 77.49899999999999523 ) ;
#25608=ORIENTED_EDGE ( 'NONE', *, *, #35330, .T. ) ;
#25609=FACE_OUTER_BOUND ( 'NONE', #42269, .T. ) ;
#25612=EDGE_CURVE ( 'NONE', #23472, #2062, #31436, .T. ) ;
#25613=ORIENTED_EDGE ( 'NONE', *, *, #14407, .T. ) ;
#25625=DIRECTION ( 'NONE',  ( 1.000000000000000000, 0.000000000000000000, 0.000000000000000000 ) ) ;
#25628=DIRECTION ( 'NONE',  ( -1.000000000000000000, -0.000000000000000000, -0.000000000000000000 ) ) ;
#25636=CARTESIAN_POINT ( 'NONE',  ( 0.000000000000000000, 2.946379043147425492, -75.11764819372145041 ) ) ;
#25637=EDGE_CURVE ( 'NONE', #68597, #65643, #57066, .T. ) ;
#25639=DIRECTION ( 'NONE',  ( 0.000000000000000000, 0.000000000000000000, 1.000000000000000000 ) ) ;
#25642=CIRCLE ( 'NONE', #32868, 82.00000000000000000 ) ;
#25646=VERTEX_POINT ( 'NONE', #2174 ) ;
#25656=DIRECTION ( 'NONE',  ( -1.000000000000000000, -0.000000000000000000, -0.000000000000000000 ) ) ;
#25657=ORIENTED_EDGE ( 'NONE', *, *, #25114, .T. ) ;
#25662=AXIS2_PLACEMENT_3D ( 'NONE', #15985, #21623, #16360 ) ;
#25665=CARTESIAN_POINT ( 'NONE',  ( 5.000000000000002665, -81.90746397400393164, 3.894527615417586741 ) ) ;
#25666=DIRECTION ( 'NONE',  ( 0.000000000000000000, 0.5224985647159500202, -0.8526401643540916231 ) ) ;
#25671=CIRCLE ( 'NONE', #4125, 82.00000000000000000 ) ;
#25677=CARTESIAN_POINT ( 'NONE',  ( 0.000000000000000000, 0.000000000000000000, 0.000000000000000000 ) ) ;
#25678=LINE ( 'NONE', #55356, #27005 ) ;
#25684=CYLINDRICAL_SURFACE ( 'NONE', #2512, 77.49899999999999523 ) ;
#25689=CIRCLE ( 'NONE', #4143, 77.49900000000000944 ) ;
#25696=DIRECTION ( 'NONE',  ( -1.000000000000000000, 0.000000000000000000, 0.000000000000000000 ) ) ;
#25702=DIRECTION ( 'NONE',  ( -1.000000000000000000, 0.000000000000000000, -0.000000000000000000 ) ) ;
#25703=DIRECTION ( 'NONE',  ( 1.000000000000000000, 0.000000000000000000, 0.000000000000000000 ) ) ;
#25705=EDGE_CURVE ( 'NONE', #31131, #49474, #66411, .T. ) ;
#25725=EDGE_CURVE ( 'NONE', #20797, #43637, #67850, .T. ) ;
#25727=DIRECTION ( 'NONE',  ( -1.000000000000000000, 0.000000000000000000, 0.000000000000000000 ) ) ;
#25734=CIRCLE ( 'NONE', #73749, 31.99999999999999289 ) ;
#25736=EDGE_LOOP ( 'NONE', ( #37661, #66761, #14455, #328 ) ) ;
#25748=EDGE_CURVE ( 'NONE', #16527, #14919, #41435, .T. ) ;
#25755=LINE ( 'NONE', #48317, #42525 ) ;
#25759=CARTESIAN_POINT ( 'NONE',  ( 0.000000000000000000, -2.956366410620109519, -75.11725578898472122 ) ) ;
#25760=DIRECTION ( 'NONE',  ( 0.000000000000000000, 0.9876883405951383255, -0.1564344650402277048 ) ) ;
#25767=DIRECTION ( 'NONE',  ( 0.000000000000000000, 0.000000000000000000, 1.000000000000000000 ) ) ;
#25770=ORIENTED_EDGE ( 'NONE', *, *, #56745, .T. ) ;
#25773=ORIENTED_EDGE ( 'NONE', *, *, #16403, .T. ) ;
#25781=LINE ( 'NONE', #48712, #34791 ) ;
#25786=CARTESIAN_POINT ( 'NONE',  ( 5.000000000000000000, 59.75363087400153006, -56.15606465354897381 ) ) ;
#25787=CARTESIAN_POINT ( 'NONE',  ( 10.00000000000000000, -76.66974797899844418, 11.30684508768314522 ) ) ;
#25788=DIRECTION ( 'NONE',  ( 1.000000000000000000, -0.000000000000000000, 0.000000000000000000 ) ) ;
#25794=ORIENTED_EDGE ( 'NONE', *, *, #51850, .T. ) ;
#25804=ORIENTED_EDGE ( 'NONE', *, *, #53945, .T. ) ;
#25812=ADVANCED_FACE ( 'NONE', ( #56232 ), #11108, .T. ) ;
#25813=DIRECTION ( 'NONE',  ( 0.000000000000000000, 0.7071067811865439090, 0.7071067811865512365 ) ) ;
#25815=CARTESIAN_POINT ( 'NONE',  ( 10.00000000000000000, 0.000000000000000000, 0.000000000000000000 ) ) ;
#25817=ORIENTED_EDGE ( 'NONE', *, *, #57754, .F. ) ;
#25820=EDGE_LOOP ( 'NONE', ( #30061, #13694, #10541, #43010 ) ) ;
#25822=DIRECTION ( 'NONE',  ( 0.000000000000000000, 0.000000000000000000, 1.000000000000000000 ) ) ;
#25824=DIRECTION ( 'NONE',  ( 0.000000000000000000, 0.000000000000000000, 1.000000000000000000 ) ) ;
#25828=ORIENTED_EDGE ( 'NONE', *, *, #22956, .F. ) ;
#25834=DIRECTION ( 'NONE',  ( -1.000000000000000000, 0.000000000000000000, -0.000000000000000000 ) ) ;
#25835=CYLINDRICAL_SURFACE ( 'NONE', #74182, 31.99999999999999289 ) ;
#25839=CIRCLE ( 'NONE', #17423, 31.99999999999999289 ) ;
#25846=VECTOR ( 'NONE', #10754, 1000.000000000000000 ) ;
#25852=DIRECTION ( 'NONE',  ( 0.000000000000000000, 0.000000000000000000, 1.000000000000000000 ) ) ;
#25855=DIRECTION ( 'NONE',  ( -1.000000000000000000, 0.000000000000000000, 0.000000000000000000 ) ) ;
#25857=EDGE_CURVE ( 'NONE', #10249, #51767, #47449, .T. ) ;
#25863=EDGE_CURVE ( 'NONE', #71285, #38604, #10201, .T. ) ;
#25867=ADVANCED_FACE ( 'NONE', ( #45715 ), #10738, .T. ) ;
#25868=DIRECTION ( 'NONE',  ( 0.000000000000000000, 0.000000000000000000, 1.000000000000000000 ) ) ;
#25877=AXIS2_PLACEMENT_3D ( 'NONE', #63360, #46809, #58439 ) ;
#25884=DIRECTION ( 'NONE',  ( 1.000000000000000000, 0.000000000000000000, 0.000000000000000000 ) ) ;
#25890=CIRCLE ( 'NONE', #34323, 82.00000000000000000 ) ;
#25891=VERTEX_POINT ( 'NONE', #63011 ) ;
#25902=EDGE_CURVE ( 'NONE', #21235, #7032, #71468, .T. ) ;
#25919=DIRECTION ( 'NONE',  ( -1.000000000000000000, 0.000000000000000000, 0.000000000000000000 ) ) ;
#25925=DIRECTION ( 'NONE',  ( 0.000000000000000000, -0.2334453638559126909, 0.9723699203976748917 ) ) ;
#25929=LINE ( 'NONE', #65794, #5833 ) ;
#25936=FACE_OUTER_BOUND ( 'NONE', #68836, .T. ) ;
#25939=DIRECTION ( 'NONE',  ( 0.000000000000000000, 0.000000000000000000, 1.000000000000000000 ) ) ;
#25947=LINE ( 'NONE', #56003, #38355 ) ;
#25949=CARTESIAN_POINT ( 'NONE',  ( 0.000000000000000000, 34.44570377933695227, -69.42325613327405165 ) ) ;
#25969=ORIENTED_EDGE ( 'NONE', *, *, #34957, .F. ) ;
#25971=VERTEX_POINT ( 'NONE', #47174 ) ;
#25998=AXIS2_PLACEMENT_3D ( 'NONE', #62394, #27789, #73270 ) ;
#26002=DIRECTION ( 'NONE',  ( -1.000000000000000000, -0.000000000000000000, -0.000000000000000000 ) ) ;
#26007=DIRECTION ( 'NONE',  ( 0.000000000000000000, 0.000000000000000000, 1.000000000000000000 ) ) ;
#26014=CARTESIAN_POINT ( 'NONE',  ( 10.00000000000000000, 0.000000000000000000, 0.000000000000000000 ) ) ;
#26026=DIRECTION ( 'NONE',  ( 0.000000000000000000, 0.9969173337331276308, 0.07845909572784873220 ) ) ;
#26034=DIRECTION ( 'NONE',  ( -1.000000000000000000, 0.000000000000000000, 0.000000000000000000 ) ) ;
#26035=ORIENTED_EDGE ( 'NONE', *, *, #30626, .F. ) ;
#26039=VECTOR ( 'NONE', #51986, 1000.000000000000000 ) ;
#26041=AXIS2_PLACEMENT_3D ( 'NONE', #22016, #57723, #11111 ) ;
#26042=CARTESIAN_POINT ( 'NONE',  ( 0.000000000000000000, 0.000000000000000000, 0.000000000000000000 ) ) ;
#26043=ORIENTED_EDGE ( 'NONE', *, *, #33424, .T. ) ;
#26044=EDGE_CURVE ( 'NONE', #70238, #60373, #22279, .T. ) ;
#26045=DIRECTION ( 'NONE',  ( 0.000000000000000000, 0.000000000000000000, 1.000000000000000000 ) ) ;
#26048=AXIS2_PLACEMENT_3D ( 'NONE', #63606, #45195, #16988 ) ;
#26051=CARTESIAN_POINT ( 'NONE',  ( 10.00000000000000000, 68.27212725128275395, -31.46837873495001503 ) ) ;
#26053=CARTESIAN_POINT ( 'NONE',  ( 10.00000000000000000, 17.28742895386084655, 75.54627589209950145 ) ) ;
#26056=ORIENTED_EDGE ( 'NONE', *, *, #63614, .F. ) ;
#26061=CIRCLE ( 'NONE', #36854, 82.00000000000000000 ) ;
#26063=ORIENTED_EDGE ( 'NONE', *, *, #5621, .T. ) ;
#26074=ADVANCED_FACE ( 'NONE', ( #2087 ), #59950, .T. ) ;
#26087=VERTEX_POINT ( 'NONE', #47908 ) ;
#26098=AXIS2_PLACEMENT_3D ( 'NONE', #33485, #73341, #15461 ) ;
#26110=CARTESIAN_POINT ( 'NONE',  ( 5.000000000000002665, 81.34940948281351325, -10.30890764327296161 ) ) ;
#26111=CARTESIAN_POINT ( 'NONE',  ( 10.00000000000000000, 74.65374052328648702, 8.840884882375350529 ) ) ;
#26121=EDGE_CURVE ( 'NONE', #14707, #16927, #1868, .T. ) ;
#26137=ORIENTED_EDGE ( 'NONE', *, *, #68326, .F. ) ;
#26142=EDGE_CURVE ( 'NONE', #62606, #7429, #48681, .T. ) ;
#26145=DIRECTION ( 'NONE',  ( 0.000000000000000000, 0.000000000000000000, 1.000000000000000000 ) ) ;
#26147=CARTESIAN_POINT ( 'NONE',  ( 10.00000000000000000, -72.35432306680469594, -20.40083707022958848 ) ) ;
#26168=VERTEX_POINT ( 'NONE', #5404 ) ;
#26169=CARTESIAN_POINT ( 'NONE',  ( 0.000000000000000000, 63.97538442413426907, 51.29473840253247374 ) ) ;
#26179=DIRECTION ( 'NONE',  ( -1.000000000000000000, 0.000000000000000000, 0.000000000000000000 ) ) ;
#26192=CIRCLE ( 'NONE', #68230, 31.99999999999999289 ) ;
#26194=ADVANCED_FACE ( 'NONE', ( #16663 ), #9902, .T. ) ;
#26198=DIRECTION ( 'NONE',  ( -1.000000000000000000, 0.000000000000000000, 0.000000000000000000 ) ) ;
#26203=EDGE_CURVE ( 'NONE', #70758, #8427, #19842, .T. ) ;
#26206=CARTESIAN_POINT ( 'NONE',  ( 0.000000000000000000, -70.52718814184277107, 26.02418014898285037 ) ) ;
#26220=DIRECTION ( 'NONE',  ( -1.000000000000000000, -0.000000000000000000, -0.000000000000000000 ) ) ;
#26222=AXIS2_PLACEMENT_3D ( 'NONE', #60908, #26682, #71427 ) ;
#26230=ORIENTED_EDGE ( 'NONE', *, *, #60093, .F. ) ;
#26238=AXIS2_PLACEMENT_3D ( 'NONE', #37429, #37793, #65623 ) ;
#26244=AXIS2_PLACEMENT_3D ( 'NONE', #69580, #58300, #28603 ) ;
#26261=LINE ( 'NONE', #66142, #14397 ) ;
#26265=AXIS2_PLACEMENT_3D ( 'NONE', #7130, #19141, #30776 ) ;
#26274=CIRCLE ( 'NONE', #58700, 77.49899999999999523 ) ;
#26285=CARTESIAN_POINT ( 'NONE',  ( 5.000000000000002665, -79.10210256391383155, 21.60688246758557796 ) ) ;
#26287=EDGE_CURVE ( 'NONE', #11557, #11811, #66788, .T. ) ;
#26302=CIRCLE ( 'NONE', #21465, 31.99999999999999645 ) ;
#26304=VECTOR ( 'NONE', #6327, 1000.000000000000000 ) ;
#26320=VECTOR ( 'NONE', #64662, 1000.000000000000000 ) ;
#26327=CIRCLE ( 'NONE', #35938, 77.49899999999999523 ) ;
#26329=EDGE_CURVE ( 'NONE', #24236, #69181, #70355, .T. ) ;
#26332=APPLICATION_CONTEXT ( 'automotive_design' ) ;
#26337=EDGE_CURVE ( 'NONE', #25004, #14607, #18736, .T. ) ;
#26342=VERTEX_POINT ( 'NONE', #45627 ) ;
#26354=AXIS2_PLACEMENT_3D ( 'NONE', #60242, #9449, #37670 ) ;
#26359=CARTESIAN_POINT ( 'NONE',  ( 5.000000000000002665, -78.73519480814938731, -22.90783923731713756 ) ) ;
#26360=EDGE_LOOP ( 'NONE', ( #61115, #55014, #4924, #26425 ) ) ;
#26362=AXIS2_PLACEMENT_3D ( 'NONE', #10052, #5553, #51022 ) ;
#26365=CARTESIAN_POINT ( 'NONE',  ( 10.00000000000000000, -16.65972982744992592, 80.28980883073749908 ) ) ;
#26373=DIRECTION ( 'NONE',  ( 0.000000000000000000, 0.000000000000000000, 1.000000000000000000 ) ) ;
#26378=DIRECTION ( 'NONE',  ( -1.000000000000000000, 0.000000000000000000, -0.000000000000000000 ) ) ;
#26379=CARTESIAN_POINT ( 'NONE',  ( 0.000000000000000000, 11.30684508768339569, 76.66974797899841576 ) ) ;
#26390=CARTESIAN_POINT ( 'NONE',  ( 0.000000000000000000, 0.000000000000000000, 0.000000000000000000 ) ) ;
#26397=CARTESIAN_POINT ( 'NONE',  ( 0.000000000000000000, -65.64334221924882229, -41.19522573413803457 ) ) ;
#26406=CIRCLE ( 'NONE', #2476, 77.49899999999999523 ) ;
#26408=DIRECTION ( 'NONE',  ( 0.000000000000000000, 0.3826834323650905589, -0.9238795325112864054 ) ) ;
#26410=ORIENTED_EDGE ( 'NONE', *, *, #28095, .T. ) ;
#26425=ORIENTED_EDGE ( 'NONE', *, *, #64193, .F. ) ;
#26432=CIRCLE ( 'NONE', #29849, 32.00000000000000000 ) ;
#26433=ORIENTED_EDGE ( 'NONE', *, *, #15893, .T. ) ;
#26436=VERTEX_POINT ( 'NONE', #17034 ) ;
#26445=VERTEX_POINT ( 'NONE', #24161 ) ;
#26452=DIRECTION ( 'NONE',  ( 0.000000000000000000, 0.000000000000000000, 1.000000000000000000 ) ) ;
#26455=FACE_OUTER_BOUND ( 'NONE', #49706, .T. ) ;
#26463=CYLINDRICAL_SURFACE ( 'NONE', #20570, 32.00000000000000000 ) ;
#26471=AXIS2_PLACEMENT_3D ( 'NONE', #28809, #57384, #40457 ) ;
#26472=DIRECTION ( 'NONE',  ( 1.000000000000000000, 0.000000000000000000, 0.000000000000000000 ) ) ;
#26483=DIRECTION ( 'NONE',  ( -1.000000000000000000, -0.000000000000000000, -0.000000000000000000 ) ) ;
#26510=EDGE_CURVE ( 'NONE', #60490, #64515, #40379, .T. ) ;
#26513=CARTESIAN_POINT ( 'NONE',  ( 10.00000000000000000, -41.76106447765533147, 62.50884508063410294 ) ) ;
#26514=ORIENTED_EDGE ( 'NONE', *, *, #39505, .F. ) ;
#26521=CARTESIAN_POINT ( 'NONE',  ( -10.00000000000000000, 0.000000000000000000, 0.000000000000000000 ) ) ;
#26527=VERTEX_POINT ( 'NONE', #53461 ) ;
#26532=VECTOR ( 'NONE', #4773, 1000.000000000000000 ) ;
#26543=VERTEX_POINT ( 'NONE', #8340 ) ;
#26545=EDGE_CURVE ( 'NONE', #20634, #72495, #64432, .T. ) ;
#26560=EDGE_CURVE ( 'NONE', #67190, #48030, #62022, .T. ) ;
#26579=LINE ( 'NONE', #61179, #24070 ) ;
#26580=DIRECTION ( 'NONE',  ( 0.000000000000000000, 0.000000000000000000, -1.000000000000000000 ) ) ;
#26585=EDGE_CURVE ( 'NONE', #7032, #15962, #39203, .T. ) ;
#26591=FACE_OUTER_BOUND ( 'NONE', #25297, .T. ) ;
#26592=AXIS2_PLACEMENT_3D ( 'NONE', #28068, #45761, #40105 ) ;
#26593=CARTESIAN_POINT ( 'NONE',  ( 0.000000000000000000, 0.000000000000000000, 0.000000000000000000 ) ) ;
#26605=CARTESIAN_POINT ( 'NONE',  ( 5.000000000000000000, 74.74816331893477184, -33.71516098798660011 ) ) ;
#26607=CARTESIAN_POINT ( 'NONE',  ( 10.00000000000000000, 0.000000000000000000, 0.000000000000000000 ) ) ;
#26612=VERTEX_POINT ( 'NONE', #69512 ) ;
#26616=DIRECTION ( 'NONE',  ( -1.000000000000000000, -0.000000000000000000, 0.000000000000000000 ) ) ;
#26618=DIRECTION ( 'NONE',  ( -1.000000000000000000, 0.000000000000000000, 0.000000000000000000 ) ) ;
#26628=CYLINDRICAL_SURFACE ( 'NONE', #35719, 77.49899999999999523 ) ;
#26634=ORIENTED_EDGE ( 'NONE', *, *, #71995, .F. ) ;
#26640=AXIS2_PLACEMENT_3D ( 'NONE', #50418, #45169, #21094 ) ;
#26645=DIRECTION ( 'NONE',  ( 0.000000000000000000, -0.9723699203976789995, 0.2334453638558956767 ) ) ;
#26654=ADVANCED_FACE ( 'NONE', ( #45867 ), #6013, .T. ) ;
#26661=DIRECTION ( 'NONE',  ( 0.000000000000000000, 0.000000000000000000, -1.000000000000000000 ) ) ;
#26679=ORIENTED_EDGE ( 'NONE', *, *, #2089, .F. ) ;
#26680=FACE_OUTER_BOUND ( 'NONE', #65502, .T. ) ;
#26682=DIRECTION ( 'NONE',  ( -1.000000000000000000, 0.000000000000000000, 0.000000000000000000 ) ) ;
#26684=AXIS2_PLACEMENT_3D ( 'NONE', #61950, #26975, #38647 ) ;
#26686=VERTEX_POINT ( 'NONE', #35305 ) ;
#26699=VERTEX_POINT ( 'NONE', #28918 ) ;
#26719=VECTOR ( 'NONE', #46783, 1000.000000000000000 ) ;
#26721=VERTEX_POINT ( 'NONE', #52582 ) ;
#26727=ORIENTED_EDGE ( 'NONE', *, *, #45007, .T. ) ;
#26728=EDGE_CURVE ( 'NONE', #40918, #74142, #57238, .T. ) ;
#26736=CARTESIAN_POINT ( 'NONE',  ( 10.00000000000000000, -70.52718814184277107, 26.02418014898285037 ) ) ;
#26737=CARTESIAN_POINT ( 'NONE',  ( 10.00000000000000000, 36.73666225445894185, 65.58780272294090707 ) ) ;
#26740=CYLINDRICAL_SURFACE ( 'NONE', #26640, 77.49899999999999523 ) ;
#26742=AXIS2_PLACEMENT_3D ( 'NONE', #32112, #73070, #21955 ) ;
#26751=ADVANCED_FACE ( 'NONE', ( #19112 ), #24752, .T. ) ;
#26753=DIRECTION ( 'NONE',  ( 1.000000000000000000, 0.000000000000000000, -0.000000000000000000 ) ) ;
#26768=ORIENTED_EDGE ( 'NONE', *, *, #57980, .T. ) ;
#26770=CARTESIAN_POINT ( 'NONE',  ( 5.000000000000000000, 79.10210256391368944, 21.60688246758614284 ) ) ;
#26778=VERTEX_POINT ( 'NONE', #43466 ) ;
#26780=DIRECTION ( 'NONE',  ( 0.000000000000000000, -6.982962677686266711E-15, 1.000000000000000000 ) ) ;
#26796=EDGE_CURVE ( 'NONE', #2735, #688, #42060, .T. ) ;
#26809=VERTEX_POINT ( 'NONE', #9961 ) ;
#26816=DIRECTION ( 'NONE',  ( -1.000000000000000000, -0.000000000000000000, -0.000000000000000000 ) ) ;
#26818=CARTESIAN_POINT ( 'NONE',  ( 10.00000000000000000, -50.95692526931372157, 58.39081064771733054 ) ) ;
#26827=ORIENTED_EDGE ( 'NONE', *, *, #38320, .F. ) ;
#26836=CARTESIAN_POINT ( 'NONE',  ( 0.000000000000000000, -44.99326035066101781, 68.55367621811127776 ) ) ;
#26839=CARTESIAN_POINT ( 'NONE',  ( 0.000000000000000000, 62.50884508063427347, 41.76106447765511831 ) ) ;
#26850=DIRECTION ( 'NONE',  ( -1.000000000000000000, 0.000000000000000000, 0.000000000000000000 ) ) ;
#26857=DIRECTION ( 'NONE',  ( 0.000000000000000000, -0.7071067811865388020, -0.7071067811865561215 ) ) ;
#26859=CYLINDRICAL_SURFACE ( 'NONE', #64647, 82.00000000000000000 ) ;
#26865=DIRECTION ( 'NONE',  ( 0.000000000000000000, 0.000000000000000000, 1.000000000000000000 ) ) ;
#26869=DIRECTION ( 'NONE',  ( 0.000000000000000000, 0.000000000000000000, 1.000000000000000000 ) ) ;
#26880=AXIS2_PLACEMENT_3D ( 'NONE', #18484, #64730, #46696 ) ;
#26894=ORIENTED_EDGE ( 'NONE', *, *, #21526, .T. ) ;
#26907=ORIENTED_EDGE ( 'NONE', *, *, #13761, .F. ) ;
#26909=EDGE_LOOP ( 'NONE', ( #796, #3198, #2805, #27320 ) ) ;
#26918=DIRECTION ( 'NONE',  ( 0.000000000000000000, 0.000000000000000000, 1.000000000000000000 ) ) ;
#26924=EDGE_CURVE ( 'NONE', #17282, #26612, #906, .T. ) ;
#26926=CARTESIAN_POINT ( 'NONE',  ( 5.000000000000000000, 77.16300072079700101, -27.74655509720590629 ) ) ;
#26953=AXIS2_PLACEMENT_3D ( 'NONE', #57947, #111, #29354 ) ;
#26959=EDGE_LOOP ( 'NONE', ( #66384, #62223, #53020, #34147 ) ) ;
#26966=DIRECTION ( 'NONE',  ( 0.000000000000000000, 0.000000000000000000, 1.000000000000000000 ) ) ;
#26968=EDGE_CURVE ( 'NONE', #15280, #67382, #34422, .T. ) ;
#26972=CARTESIAN_POINT ( 'NONE',  ( 0.000000000000000000, -69.42325613327466272, 34.44570377933573724 ) ) ;
#26975=DIRECTION ( 'NONE',  ( -1.000000000000000000, 0.000000000000000000, -0.000000000000000000 ) ) ;
#27002=DIRECTION ( 'NONE',  ( 0.000000000000000000, 0.000000000000000000, 1.000000000000000000 ) ) ;
#27005=VECTOR ( 'NONE', #66286, 1000.000000000000000 ) ;
#27018=CARTESIAN_POINT ( 'NONE',  ( 10.00000000000000000, -20.40083707022829174, -72.35432306680507963 ) ) ;
#27020=DIRECTION ( 'NONE',  ( 0.000000000000000000, 0.7604059656000276002, 0.6494480483301876550 ) ) ;
#27023=CIRCLE ( 'NONE', #52258, 31.99999999999999645 ) ;
#27027=CARTESIAN_POINT ( 'NONE',  ( 0.000000000000000000, 21.60688246758585507, 79.10210256391376049 ) ) ;
#27030=CARTESIAN_POINT ( 'NONE',  ( 10.00000000000000000, 73.44644590900094272, -24.73286445877628026 ) ) ;
#27045=CIRCLE ( 'NONE', #19854, 31.99999999999999289 ) ;
#27046=CARTESIAN_POINT ( 'NONE',  ( 10.00000000000000000, 18.89407956138362010, -75.16055320797013906 ) ) ;
#27056=FACE_OUTER_BOUND ( 'NONE', #35807, .T. ) ;
#27057=EDGE_LOOP ( 'NONE', ( #72757, #14369, #48368, #17219 ) ) ;
#27061=EDGE_CURVE ( 'NONE', #39027, #66404, #24817, .T. ) ;
#27062=EDGE_LOOP ( 'NONE', ( #42665, #24853, #39563, #30422 ) ) ;
#27063=VECTOR ( 'NONE', #12869, 1000.000000000000000 ) ;
#27065=ORIENTED_EDGE ( 'NONE', *, *, #44136, .T. ) ;
#27070=EDGE_LOOP ( 'NONE', ( #22137, #1975, #42229, #24588 ) ) ;
#27076=EDGE_LOOP ( 'NONE', ( #58003, #50583, #17234, #40727 ) ) ;
#27078=ADVANCED_FACE ( 'NONE', ( #3111 ), #65876, .T. ) ;
#27080=CARTESIAN_POINT ( 'NONE',  ( 0.000000000000000000, 0.000000000000000000, 0.000000000000000000 ) ) ;
#27084=ORIENTED_EDGE ( 'NONE', *, *, #40302, .T. ) ;
#27086=DIRECTION ( 'NONE',  ( -1.000000000000000000, -0.000000000000000000, 0.000000000000000000 ) ) ;
#27098=EDGE_LOOP ( 'NONE', ( #28662, #12501, #38181, #72273 ) ) ;
#27104=DIRECTION ( 'NONE',  ( -1.000000000000000000, -0.000000000000000000, -0.000000000000000000 ) ) ;
#27105=CIRCLE ( 'NONE', #16278, 77.49899999999999523 ) ;
#27110=CYLINDRICAL_SURFACE ( 'NONE', #58860, 77.49899999999999523 ) ;
#27112=DIRECTION ( 'NONE',  ( 0.000000000000000000, 0.4539904997395413644, 0.8910065241883706744 ) ) ;
#27121=LINE ( 'NONE', #38795, #35291 ) ;
#27127=ADVANCED_FACE ( 'NONE', ( #36919 ), #70011, .T. ) ;
#27133=CARTESIAN_POINT ( 'NONE',  ( 10.00000000000000000, -39.47590169984793818, -71.87247863392455827 ) ) ;
#27134=ORIENTED_EDGE ( 'NONE', *, *, #65043, .T. ) ;
#27138=UNCERTAINTY_MEASURE_WITH_UNIT (LENGTH_MEASURE( 1.000000000000000082E-05 ), #37042, 'distance_accuracy_value', 'NONE');
#27142=FILL_AREA_STYLE_COLOUR ( '', #53503 ) ;
#27144=DIRECTION ( 'NONE',  ( 0.000000000000000000, 0.000000000000000000, 1.000000000000000000 ) ) ;
#27145=CARTESIAN_POINT ( 'NONE',  ( 10.00000000000000000, -26.01480285779885904, 70.53064760720306481 ) ) ;
#27146=EDGE_CURVE ( 'NONE', #56502, #61671, #65142, .T. ) ;
#27147=ORIENTED_EDGE ( 'NONE', *, *, #38614, .T. ) ;
#27150=CARTESIAN_POINT ( 'NONE',  ( 10.00000000000000000, -46.53671651293907274, -59.03961581697448935 ) ) ;
#27154=AXIS2_PLACEMENT_3D ( 'NONE', #67648, #61639, #10126 ) ;
#27159=PRODUCT ( 'big gear_ISO - Spur gear 2M 80T 20PA 10FW ---S80A75H50L20.0N', 'big gear_ISO - Spur gear 2M 80T 20PA 10FW ---S80A75H50L20.0N', '', ( #12850 ) ) ;
#27160=EDGE_CURVE ( 'NONE', #33095, #16927, #1646, .T. ) ;
#27161=AXIS2_PLACEMENT_3D ( 'NONE', #53854, #37685, #25292 ) ;
#27171=ORIENTED_EDGE ( 'NONE', *, *, #65347, .T. ) ;
#27177=DIRECTION ( 'NONE',  ( 0.000000000000000000, -0.6494480483301903195, 0.7604059656000251577 ) ) ;
#27180=DIRECTION ( 'NONE',  ( -1.000000000000000000, 0.000000000000000000, 0.000000000000000000 ) ) ;
#27195=ORIENTED_EDGE ( 'NONE', *, *, #18019, .F. ) ;
#27199=CARTESIAN_POINT ( 'NONE',  ( 0.000000000000000000, 81.90746397400387480, 3.894527615418187150 ) ) ;
#27204=CARTESIAN_POINT ( 'NONE',  ( 10.00000000000000000, -71.21200624218766961, -40.65526001592689909 ) ) ;
#27206=AXIS2_PLACEMENT_3D ( 'NONE', #44331, #60880, #3383 ) ;
#27214=CYLINDRICAL_SURFACE ( 'NONE', #29786, 77.49899999999999523 ) ;
#27266=CARTESIAN_POINT ( 'NONE',  ( 0.000000000000000000, 80.28980883073781172, -16.65972982744850839 ) ) ;
#27268=DIRECTION ( 'NONE',  ( 0.000000000000000000, 0.000000000000000000, 1.000000000000000000 ) ) ;
#27284=LINE ( 'NONE', #43507, #4240 ) ;
#27299=DIRECTION ( 'NONE',  ( -1.000000000000000000, -0.000000000000000000, -0.000000000000000000 ) ) ;
#27300=ORIENTED_EDGE ( 'NONE', *, *, #24460, .F. ) ;
#27301=ADVANCED_FACE ( 'NONE', ( #50033 ), #55320, .T. ) ;
#27311=EDGE_CURVE ( 'NONE', #1450, #11217, #45331, .T. ) ;
#27313=EDGE_CURVE ( 'NONE', #50235, #14882, #47675, .T. ) ;
#27314=CARTESIAN_POINT ( 'NONE',  ( 0.000000000000000000, 55.38113227695858143, -54.21277698773617715 ) ) ;
#27320=ORIENTED_EDGE ( 'NONE', *, *, #73652, .T. ) ;
#27324=EDGE_CURVE ( 'NONE', #70648, #18411, #16208, .T. ) ;
#27330=CARTESIAN_POINT ( 'NONE',  ( 0.000000000000000000, 0.000000000000000000, 0.000000000000000000 ) ) ;
#27331=FACE_OUTER_BOUND ( 'NONE', #2900, .T. ) ;
#27334=EDGE_CURVE ( 'NONE', #26778, #61936, #6894, .T. ) ;
#27339=ORIENTED_EDGE ( 'NONE', *, *, #44564, .F. ) ;
#27343=DIRECTION ( 'NONE',  ( 0.000000000000000000, -0.8090169943749403458, -0.5877852522924830181 ) ) ;
#27344=AXIS2_PLACEMENT_3D ( 'NONE', #18456, #70316, #849 ) ;
#27347=LINE ( 'NONE', #16830, #40501 ) ;
#27370=VECTOR ( 'NONE', #25014, 1000.000000000000000 ) ;
#27379=ORIENTED_EDGE ( 'NONE', *, *, #73856, .T. ) ;
#27382=CARTESIAN_POINT ( 'NONE',  ( 0.000000000000000000, -44.88180994100421373, 63.18004540533011948 ) ) ;
#27388=DIRECTION ( 'NONE',  ( -1.000000000000000000, 0.000000000000000000, 0.000000000000000000 ) ) ;
#27392=ADVANCED_FACE ( 'NONE', ( #44049 ), #32009, .T. ) ;
#27404=VECTOR ( 'NONE', #56285, 1000.000000000000000 ) ;
#27411=CARTESIAN_POINT ( 'NONE',  ( 0.000000000000000000, 65.64334221924966073, -41.19522573413664190 ) ) ;
#27412=DIRECTION ( 'NONE',  ( -1.000000000000000000, 0.000000000000000000, 0.000000000000000000 ) ) ;
#27414=DIRECTION ( 'NONE',  ( 0.000000000000000000, 0.8526401643540897357, 0.5224985647159531288 ) ) ;
#27418=EDGE_CURVE ( 'NONE', #34394, #53435, #50785, .T. ) ;
#27421=CARTESIAN_POINT ( 'NONE',  ( 0.000000000000000000, -30.41916302227164337, 71.27951684758015460 ) ) ;
#27425=EDGE_CURVE ( 'NONE', #1988, #2136, #51156, .T. ) ;
#27453=AXIS2_PLACEMENT_3D ( 'NONE', #17456, #73848, #62982 ) ;
#27456=VERTEX_POINT ( 'NONE', #46640 ) ;
#27462=ORIENTED_EDGE ( 'NONE', *, *, #40178, .F. ) ;
#27463=EDGE_CURVE ( 'NONE', #33591, #28018, #56820, .T. ) ;
#27465=CARTESIAN_POINT ( 'NONE',  ( 10.00000000000000000, 46.21855187248629449, 62.20884554314036308 ) ) ;
#27473=ORIENTED_EDGE ( 'NONE', *, *, #29887, .F. ) ;
#27475=CARTESIAN_POINT ( 'NONE',  ( 10.00000000000000000, 0.000000000000000000, 0.000000000000000000 ) ) ;
#27498=CARTESIAN_POINT ( 'NONE',  ( 0.000000000000000000, 2.956366410620650420, 75.11725578898469280 ) ) ;
#27504=CARTESIAN_POINT ( 'NONE',  ( 10.00000000000000000, -50.95692526931372157, 58.39081064771733054 ) ) ;
#27505=CARTESIAN_POINT ( 'NONE',  ( 5.000000000000002665, -81.34940948281344220, 10.30890764327356557 ) ) ;
#27515=AXIS2_PLACEMENT_3D ( 'NONE', #6640, #46490, #57781 ) ;
#27528=CIRCLE ( 'NONE', #13091, 82.00000000000000000 ) ;
#27530=CARTESIAN_POINT ( 'NONE',  ( 0.000000000000000000, -68.67312586195022561, 35.91791733033449674 ) ) ;
#27534=CIRCLE ( 'NONE', #21516, 31.99999999999999645 ) ;
#27538=DIRECTION ( 'NONE',  ( 0.000000000000000000, 0.000000000000000000, 1.000000000000000000 ) ) ;
#27555=ORIENTED_EDGE ( 'NONE', *, *, #13428, .F. ) ;
#27572=EDGE_LOOP ( 'NONE', ( #14308, #19409, #59065, #39154 ) ) ;
#27575=VERTEX_POINT ( 'NONE', #35710 ) ;
#27584=CARTESIAN_POINT ( 'NONE',  ( 5.000000000000002665, 15.33399622253600292, -80.55351364060572905 ) ) ;
#27601=AXIS2_PLACEMENT_3D ( 'NONE', #38444, #10603, #3880 ) ;
#27605=CARTESIAN_POINT ( 'NONE',  ( 5.000000000000002665, -34.94270380257693631, 74.18225833017875459 ) ) ;
#27606=FACE_OUTER_BOUND ( 'NONE', #209, .T. ) ;
#27609=ADVANCED_FACE ( 'NONE', ( #48116 ), #42119, .T. ) ;
#27615=ORIENTED_EDGE ( 'NONE', *, *, #23272, .F. ) ;
#27616=DIRECTION ( 'NONE',  ( -1.000000000000000000, -0.000000000000000000, -0.000000000000000000 ) ) ;
#27629=CARTESIAN_POINT ( 'NONE',  ( 10.00000000000000000, -41.76106447765443619, -62.50884508063471401 ) ) ;
#27638=DIRECTION ( 'NONE',  ( 1.000000000000000000, 0.000000000000000000, 0.000000000000000000 ) ) ;
#27648=LINE ( 'NONE', #49466, #23790 ) ;
#27651=CARTESIAN_POINT ( 'NONE',  ( 0.000000000000000000, 0.000000000000000000, 0.000000000000000000 ) ) ;
#27665=ORIENTED_EDGE ( 'NONE', *, *, #23272, .T. ) ;
#27668=CARTESIAN_POINT ( 'NONE',  ( 0.000000000000000000, -75.11764819372149304, 2.946379043146075905 ) ) ;
#27674=ORIENTED_EDGE ( 'NONE', *, *, #41665, .T. ) ;
#27677=CIRCLE ( 'NONE', #22918, 32.00000000000000000 ) ;
#27691=CYLINDRICAL_SURFACE ( 'NONE', #55900, 77.49899999999999523 ) ;
#27695=DIRECTION ( 'NONE',  ( -1.000000000000000000, -0.000000000000000000, 0.000000000000000000 ) ) ;
#27697=LINE ( 'NONE', #50621, #7271 ) ;
#27701=CARTESIAN_POINT ( 'NONE',  ( 10.00000000000000000, -0.8261519478436571973, 77.49459641780886443 ) ) ;
#27702=EDGE_CURVE ( 'NONE', #69267, #40399, #71750, .T. ) ;
#27713=ORIENTED_EDGE ( 'NONE', *, *, #37078, .F. ) ;
#27717=DIRECTION ( 'NONE',  ( -1.000000000000000000, 0.000000000000000000, -0.000000000000000000 ) ) ;
#27724=CIRCLE ( 'NONE', #49346, 77.49900000000000944 ) ;
#27725=ORIENTED_EDGE ( 'NONE', *, *, #793, .T. ) ;
#27726=DIRECTION ( 'NONE',  ( -1.000000000000000000, -0.000000000000000000, 0.000000000000000000 ) ) ;
#27735=CARTESIAN_POINT ( 'NONE',  ( 0.000000000000000000, 0.000000000000000000, 0.000000000000000000 ) ) ;
#27740=FACE_OUTER_BOUND ( 'NONE', #42533, .T. ) ;
#27744=EDGE_CURVE ( 'NONE', #26721, #71482, #48949, .T. ) ;
#27749=CARTESIAN_POINT ( 'NONE',  ( 10.00000000000000000, 8.966570791700695153, 81.50828551894228724 ) ) ;
#27775=CARTESIAN_POINT ( 'NONE',  ( 10.00000000000000000, -29.01471420065617224, 76.69515212746006227 ) ) ;
#27789=DIRECTION ( 'NONE',  ( 1.000000000000000000, 0.000000000000000000, 0.000000000000000000 ) ) ;
#27790=DIRECTION ( 'NONE',  ( 0.000000000000000000, 0.000000000000000000, 1.000000000000000000 ) ) ;
#27804=FACE_OUTER_BOUND ( 'NONE', #19035, .T. ) ;
#27805=CIRCLE ( 'NONE', #67409, 77.49900000000000944 ) ;
#27809=ORIENTED_EDGE ( 'NONE', *, *, #59722, .F. ) ;
#27810=VECTOR ( 'NONE', #66426, 1000.000000000000000 ) ;
#27817=VERTEX_POINT ( 'NONE', #37218 ) ;
#27819=ORIENTED_EDGE ( 'NONE', *, *, #73461, .T. ) ;
#27822=AXIS2_PLACEMENT_3D ( 'NONE', #9631, #66417, #32549 ) ;
#27827=ORIENTED_EDGE ( 'NONE', *, *, #39885, .F. ) ;
#27844=VERTEX_POINT ( 'NONE', #40177 ) ;
#27845=DIRECTION ( 'NONE',  ( 0.000000000000000000, 0.000000000000000000, -1.000000000000000000 ) ) ;
#27864=ADVANCED_FACE ( 'NONE', ( #12605 ), #70112, .T. ) ;
#27867=CARTESIAN_POINT ( 'NONE',  ( 10.00000000000000000, 0.000000000000000000, 0.000000000000000000 ) ) ;
#27875=ORIENTED_EDGE ( 'NONE', *, *, #48656, .F. ) ;
#27877=CIRCLE ( 'NONE', #25471, 82.00000000000000000 ) ;
#27878=LINE ( 'NONE', #67739, #32797 ) ;
#27883=DIRECTION ( 'NONE',  ( -1.000000000000000000, 0.000000000000000000, -0.000000000000000000 ) ) ;
#27889=CARTESIAN_POINT ( 'NONE',  ( 0.000000000000000000, -14.66109333815513160, 73.73191006444567108 ) ) ;
#27890=ORIENTED_EDGE ( 'NONE', *, *, #9668, .T. ) ;
#27894=ORIENTED_EDGE ( 'NONE', *, *, #35801, .T. ) ;
#27905=ORIENTED_EDGE ( 'NONE', *, *, #1560, .F. ) ;
#27910=ORIENTED_EDGE ( 'NONE', *, *, #36804, .F. ) ;
#27916=CIRCLE ( 'NONE', #29096, 82.00000000000000000 ) ;
#27921=DIRECTION ( 'NONE',  ( 0.000000000000000000, 0.000000000000000000, -1.000000000000000000 ) ) ;
#27928=VECTOR ( 'NONE', #27960, 1000.000000000000000 ) ;
#27950=CARTESIAN_POINT ( 'NONE',  ( 5.000000000000002665, -10.30890764327441822, 81.34940948281332851 ) ) ;
#27960=DIRECTION ( 'NONE',  ( -1.000000000000000000, 0.000000000000000000, 0.000000000000000000 ) ) ;
#27970=DIRECTION ( 'NONE',  ( -1.000000000000000000, 0.000000000000000000, 0.000000000000000000 ) ) ;
#27978=VERTEX_POINT ( 'NONE', #64866 ) ;
#27982=AXIS2_PLACEMENT_3D ( 'NONE', #32293, #20280, #26661 ) ;
#27988=EDGE_CURVE ( 'NONE', #26527, #53791, #10527, .T. ) ;
#27993=EDGE_CURVE ( 'NONE', #55165, #39002, #12937, .T. ) ;
#27995=ORIENTED_EDGE ( 'NONE', *, *, #62672, .T. ) ;
#27996=ORIENTED_EDGE ( 'NONE', *, *, #15076, .T. ) ;
#28000=LINE ( 'NONE', #62618, #13584 ) ;
#28007=ORIENTED_EDGE ( 'NONE', *, *, #73152, .F. ) ;
#28009=EDGE_LOOP ( 'NONE', ( #38082, #65924, #24168, #69625 ) ) ;
#28018=VERTEX_POINT ( 'NONE', #36278 ) ;
#28022=FACE_OUTER_BOUND ( 'NONE', #43213, .T. ) ;
#28032=DIRECTION ( 'NONE',  ( -1.000000000000000000, -0.000000000000000000, 0.000000000000000000 ) ) ;
#28037=CARTESIAN_POINT ( 'NONE',  ( 0.000000000000000000, 0.000000000000000000, 0.000000000000000000 ) ) ;
#28046=DIRECTION ( 'NONE',  ( -1.000000000000000000, 0.000000000000000000, 0.000000000000000000 ) ) ;
#28050=CARTESIAN_POINT ( 'NONE',  ( 10.00000000000000000, 62.20884554314020676, 46.21855187248652896 ) ) ;
#28053=CARTESIAN_POINT ( 'NONE',  ( 10.00000000000000000, 0.000000000000000000, 0.000000000000000000 ) ) ;
#28059=DIRECTION ( 'NONE',  ( -1.000000000000000000, -0.000000000000000000, -0.000000000000000000 ) ) ;
#28068=CARTESIAN_POINT ( 'NONE',  ( 0.000000000000000000, 0.000000000000000000, 0.000000000000000000 ) ) ;
#28080=AXIS2_PLACEMENT_3D ( 'NONE', #11074, #22351, #15963 ) ;
#28083=EDGE_CURVE ( 'NONE', #34215, #24836, #978, .T. ) ;
#28084=AXIS2_PLACEMENT_3D ( 'NONE', #23819, #68590, #932 ) ;
#28089=ORIENTED_EDGE ( 'NONE', *, *, #17427, .F. ) ;
#28092=DIRECTION ( 'NONE',  ( 0.000000000000000000, 0.000000000000000000, 1.000000000000000000 ) ) ;
#28095=EDGE_CURVE ( 'NONE', #48030, #42459, #52601, .T. ) ;
#28099=ORIENTED_EDGE ( 'NONE', *, *, #31894, .T. ) ;
#28105=FACE_OUTER_BOUND ( 'NONE', #33383, .T. ) ;
#28115=ADVANCED_FACE ( 'NONE', ( #66351 ), #20090, .T. ) ;
#28129=ORIENTED_EDGE ( 'NONE', *, *, #33617, .T. ) ;
#28143=CARTESIAN_POINT ( 'NONE',  ( 10.00000000000000000, 0.000000000000000000, 0.000000000000000000 ) ) ;
#28144=DIRECTION ( 'NONE',  ( -1.000000000000000000, -0.000000000000000000, -0.000000000000000000 ) ) ;
#28154=DIRECTION ( 'NONE',  ( -1.000000000000000000, 0.000000000000000000, 0.000000000000000000 ) ) ;
#28159=CARTESIAN_POINT ( 'NONE',  ( 0.000000000000000000, -75.11764819372145041, -2.946379043147127064 ) ) ;
#28161=CIRCLE ( 'NONE', #35366, 31.99999999999999289 ) ;
#28168=EDGE_CURVE ( 'NONE', #52333, #59827, #38506, .T. ) ;
#28185=EDGE_CURVE ( 'NONE', #60502, #58170, #57397, .T. ) ;
#28187=VECTOR ( 'NONE', #24882, 1000.000000000000000 ) ;
#28196=LINE ( 'NONE', #67684, #22516 ) ;
#28201=ORIENTED_EDGE ( 'NONE', *, *, #38696, .T. ) ;
#28208=VERTEX_POINT ( 'NONE', #27199 ) ;
#28211=DIRECTION ( 'NONE',  ( -1.000000000000000000, 0.000000000000000000, -0.000000000000000000 ) ) ;
#28214=VECTOR ( 'NONE', #68585, 1000.000000000000000 ) ;
#28220=EDGE_LOOP ( 'NONE', ( #15665, #49270, #56058, #51061 ) ) ;
#28224=DIRECTION ( 'NONE',  ( 0.000000000000000000, 0.000000000000000000, 1.000000000000000000 ) ) ;
#28235=DIRECTION ( 'NONE',  ( 0.000000000000000000, 0.000000000000000000, 1.000000000000000000 ) ) ;
#28241=AXIS2_PLACEMENT_3D ( 'NONE', #62703, #5918, #11168 ) ;
#28245=DIRECTION ( 'NONE',  ( 0.000000000000000000, 0.000000000000000000, -1.000000000000000000 ) ) ;
#28247=VECTOR ( 'NONE', #58953, 1000.000000000000000 ) ;
#28255=DIRECTION ( 'NONE',  ( 0.000000000000000000, 0.7071067811865489050, -0.7071067811865462405 ) ) ;
#28258=MECHANICAL_DESIGN_GEOMETRIC_PRESENTATION_REPRESENTATION('',(#10299),#51128);
#28262=VERTEX_POINT ( 'NONE', #17064 ) ;
#28285=CARTESIAN_POINT ( 'NONE',  ( 10.00000000000000000, 0.8261519478431083030, 77.49459641780886443 ) ) ;
#28298=AXIS2_PLACEMENT_3D ( 'NONE', #8918, #72063, #66441 ) ;
#28308=ORIENTED_EDGE ( 'NONE', *, *, #63262, .T. ) ;
#28309=DIRECTION ( 'NONE',  ( -1.000000000000000000, -0.000000000000000000, 0.000000000000000000 ) ) ;
#28314=CARTESIAN_POINT ( 'NONE',  ( 0.000000000000000000, 59.46389618802034960, -49.70050353004825894 ) ) ;
#28320=EDGE_LOOP ( 'NONE', ( #44866, #48542, #45347, #19599 ) ) ;
#28349=FACE_OUTER_BOUND ( 'NONE', #3367, .T. ) ;
#28351=AXIS2_PLACEMENT_3D ( 'NONE', #57503, #12724, #18367 ) ;
#28352=CIRCLE ( 'NONE', #31946, 31.99999999999999645 ) ;
#28363=CARTESIAN_POINT ( 'NONE',  ( 10.00000000000000000, 0.000000000000000000, 0.000000000000000000 ) ) ;
#28369=VERTEX_POINT ( 'NONE', #7264 ) ;
#28373=ORIENTED_EDGE ( 'NONE', *, *, #49829, .T. ) ;
#28381=ORIENTED_EDGE ( 'NONE', *, *, #36505, .T. ) ;
#28388=ORIENTED_EDGE ( 'NONE', *, *, #38944, .T. ) ;
#28404=ORIENTED_EDGE ( 'NONE', *, *, #5984, .F. ) ;
#28411=EDGE_CURVE ( 'NONE', #61965, #32631, #16601, .T. ) ;
#28418=FACE_OUTER_BOUND ( 'NONE', #62049, .T. ) ;
#28430=DIRECTION ( 'NONE',  ( -1.000000000000000000, -0.000000000000000000, -0.000000000000000000 ) ) ;
#28451=CARTESIAN_POINT ( 'NONE',  ( 10.00000000000000000, 31.46837873494978055, 68.27212725128286763 ) ) ;
#28452=AXIS2_PLACEMENT_3D ( 'NONE', #19588, #9055, #24868 ) ;
#28454=VECTOR ( 'NONE', #20737, 1000.000000000000000 ) ;
#28455=ORIENTED_EDGE ( 'NONE', *, *, #70849, .T. ) ;
#28459=DIRECTION ( 'NONE',  ( 0.000000000000000000, 0.000000000000000000, 1.000000000000000000 ) ) ;
#28461=DIRECTION ( 'NONE',  ( -1.000000000000000000, -0.000000000000000000, 0.000000000000000000 ) ) ;
#28465=ORIENTED_EDGE ( 'NONE', *, *, #16824, .T. ) ;
#28469=CARTESIAN_POINT ( 'NONE',  ( 10.00000000000000000, -65.58780272294048075, -36.73666225445966660 ) ) ;
#28486=CARTESIAN_POINT ( 'NONE',  ( 10.00000000000000000, 0.000000000000000000, 0.000000000000000000 ) ) ;
#28488=DIRECTION ( 'NONE',  ( 0.000000000000000000, -0.8910065241883722287, 0.4539904997395383668 ) ) ;
#28490=DIRECTION ( 'NONE',  ( 0.000000000000000000, 0.5224985647159440250, 0.8526401643540951758 ) ) ;
#28498=DIRECTION ( 'NONE',  ( -1.000000000000000000, 0.000000000000000000, 0.000000000000000000 ) ) ;
#28502=ORIENTED_EDGE ( 'NONE', *, *, #9367, .T. ) ;
#28509=EDGE_CURVE ( 'NONE', #30261, #1192, #19009, .T. ) ;
#28530=AXIS2_PLACEMENT_3D ( 'NONE', #13676, #32073, #59557 ) ;
#28562=EDGE_CURVE ( 'NONE', #29240, #47328, #43700, .T. ) ;
#28563=VERTEX_POINT ( 'NONE', #10572 ) ;
#28569=ORIENTED_EDGE ( 'NONE', *, *, #71042, .F. ) ;
#28572=ORIENTED_EDGE ( 'NONE', *, *, #74296, .F. ) ;
#28574=AXIS2_PLACEMENT_3D ( 'NONE', #52140, #47611, #53619 ) ;
#28580=DIRECTION ( 'NONE',  ( -1.000000000000000000, 0.000000000000000000, 0.000000000000000000 ) ) ;
#28592=DIRECTION ( 'NONE',  ( -1.000000000000000000, -0.000000000000000000, 0.000000000000000000 ) ) ;
#28596=EDGE_CURVE ( 'NONE', #14685, #25432, #14222, .T. ) ;
#28598=DIRECTION ( 'NONE',  ( 0.000000000000000000, 0.000000000000000000, 1.000000000000000000 ) ) ;
#28603=DIRECTION ( 'NONE',  ( 0.000000000000000000, 0.000000000000000000, 1.000000000000000000 ) ) ;
#28605=EDGE_CURVE ( 'NONE', #33095, #15883, #46659, .T. ) ;
#28609=DIRECTION ( 'NONE',  ( 0.000000000000000000, 0.000000000000000000, 1.000000000000000000 ) ) ;
#28623=VERTEX_POINT ( 'NONE', #10208 ) ;
#28627=EDGE_CURVE ( 'NONE', #27456, #7986, #50797, .T. ) ;
#28629=VECTOR ( 'NONE', #48318, 1000.000000000000000 ) ;
#28636=ORIENTED_EDGE ( 'NONE', *, *, #69867, .F. ) ;
#28641=ORIENTED_EDGE ( 'NONE', *, *, #36001, .T. ) ;
#28642=DIRECTION ( 'NONE',  ( 0.000000000000000000, 0.000000000000000000, 1.000000000000000000 ) ) ;
#28646=DIRECTION ( 'NONE',  ( -1.000000000000000000, -0.000000000000000000, 0.000000000000000000 ) ) ;
#28651=ORIENTED_EDGE ( 'NONE', *, *, #44063, .T. ) ;
#28662=ORIENTED_EDGE ( 'NONE', *, *, #28627, .T. ) ;
#28673=ADVANCED_FACE ( 'NONE', ( #6795 ), #23357, .T. ) ;
#28680=VERTEX_POINT ( 'NONE', #68485 ) ;
#28690=CARTESIAN_POINT ( 'NONE',  ( 10.00000000000000000, -68.27212725128298132, 31.46837873494953541 ) ) ;
#28693=AXIS2_PLACEMENT_3D ( 'NONE', #71067, #30841, #42892 ) ;
#28696=CIRCLE ( 'NONE', #67115, 77.49899999999999523 ) ;
#28715=CARTESIAN_POINT ( 'NONE',  ( 10.00000000000000000, -70.52718814184240159, -26.02418014898383802 ) ) ;
#28718=EDGE_CURVE ( 'NONE', #19228, #37462, #58680, .T. ) ;
#28720=AXIS2_PLACEMENT_3D ( 'NONE', #36270, #53943, #71952 ) ;
#28723=ORIENTED_EDGE ( 'NONE', *, *, #18163, .T. ) ;
#28726=VECTOR ( 'NONE', #45063, 1000.000000000000000 ) ;
#28729=AXIS2_PLACEMENT_3D ( 'NONE', #22545, #4906, #45488 ) ;
#28733=CARTESIAN_POINT ( 'NONE',  ( 10.00000000000000000, 33.71516098798738881, 74.74816331893441657 ) ) ;
#28740=AXIS2_PLACEMENT_3D ( 'NONE', #5953, #40145, #5580 ) ;
#28742=ORIENTED_EDGE ( 'NONE', *, *, #9402, .F. ) ;
#28743=CIRCLE ( 'NONE', #45629, 31.99999999999998934 ) ;
#28747=EDGE_LOOP ( 'NONE', ( #60513, #11720, #67904, #41601 ) ) ;
#28765=DIRECTION ( 'NONE',  ( 0.000000000000000000, 0.000000000000000000, 1.000000000000000000 ) ) ;
#28782=DIRECTION ( 'NONE',  ( 0.000000000000000000, 0.000000000000000000, 1.000000000000000000 ) ) ;
#28788=CARTESIAN_POINT ( 'NONE',  ( 0.000000000000000000, 75.11764819372149304, 29.05362095685338986 ) ) ;
#28789=VERTEX_POINT ( 'NONE', #62484 ) ;
#28793=EDGE_CURVE ( 'NONE', #21165, #11119, #41877, .T. ) ;
#28804=AXIS2_PLACEMENT_3D ( 'NONE', #26839, #26472, #49406 ) ;
#28809=CARTESIAN_POINT ( 'NONE',  ( 0.000000000000000000, 0.000000000000000000, 0.000000000000000000 ) ) ;
#28810=CARTESIAN_POINT ( 'NONE',  ( 10.00000000000000000, 35.91791733033570466, -68.67312586194960033 ) ) ;
#28820=DIRECTION ( 'NONE',  ( 0.000000000000000000, 0.000000000000000000, 1.000000000000000000 ) ) ;
#28823=VERTEX_POINT ( 'NONE', #24825 ) ;
#28827=CARTESIAN_POINT ( 'NONE',  ( 0.000000000000000000, -10.30890764327323872, -81.34940948281348483 ) ) ;
#28847=ORIENTED_EDGE ( 'NONE', *, *, #382, .F. ) ;
#28851=CIRCLE ( 'NONE', #30081, 31.99999999999998579 ) ;
#28854=EDGE_CURVE ( 'NONE', #17876, #2885, #25929, .T. ) ;
#28862=ORIENTED_EDGE ( 'NONE', *, *, #61978, .T. ) ;
#28869=ORIENTED_EDGE ( 'NONE', *, *, #11520, .T. ) ;
#28881=EDGE_CURVE ( 'NONE', #10255, #28789, #67040, .T. ) ;
#28882=VERTEX_POINT ( 'NONE', #19909 ) ;
#28889=CYLINDRICAL_SURFACE ( 'NONE', #68667, 31.99999999999999289 ) ;
#28894=CYLINDRICAL_SURFACE ( 'NONE', #5470, 82.00000000000000000 ) ;
#28904=CARTESIAN_POINT ( 'NONE',  ( 5.000000000000002665, -80.55351364060599906, 15.33399622253456585 ) ) ;
#28908=VECTOR ( 'NONE', #22796, 1000.000000000000000 ) ;
#28910=VECTOR ( 'NONE', #4114, 1000.000000000000000 ) ;
#28911=CIRCLE ( 'NONE', #38525, 31.99999999999998934 ) ;
#28913=DIRECTION ( 'NONE',  ( 0.000000000000000000, 0.000000000000000000, -1.000000000000000000 ) ) ;
#28918=CARTESIAN_POINT ( 'NONE',  ( 0.000000000000000000, -68.55367621811174672, 44.99326035066030727 ) ) ;
#28922=VERTEX_POINT ( 'NONE', #8651 ) ;
#28928=ORIENTED_EDGE ( 'NONE', *, *, #50465, .T. ) ;
#28930=EDGE_CURVE ( 'NONE', #7986, #55747, #52719, .T. ) ;
#28938=ORIENTED_EDGE ( 'NONE', *, *, #22344, .F. ) ;
#28945=DIRECTION ( 'NONE',  ( -1.000000000000000000, 0.000000000000000000, -0.000000000000000000 ) ) ;
#28946=ORIENTED_EDGE ( 'NONE', *, *, #67726, .T. ) ;
#28948=ADVANCED_FACE ( 'NONE', ( #42495 ), #71044, .T. ) ;
#28964=ORIENTED_EDGE ( 'NONE', *, *, #39471, .F. ) ;
#28966=AXIS2_PLACEMENT_3D ( 'NONE', #54163, #25577, #43988 ) ;
#28977=CARTESIAN_POINT ( 'NONE',  ( 10.00000000000000000, 0.000000000000000000, 0.000000000000000000 ) ) ;
#28980=DIRECTION ( 'NONE',  ( 0.000000000000000000, 0.5877852522924685852, 0.8090169943749507819 ) ) ;
#28990=CARTESIAN_POINT ( 'NONE',  ( 10.00000000000000000, 35.91791733033570466, -68.67312586194960033 ) ) ;
#28995=DIRECTION ( 'NONE',  ( -1.000000000000000000, -0.000000000000000000, 0.000000000000000000 ) ) ;
#29001=EDGE_CURVE ( 'NONE', #16368, #8743, #55134, .T. ) ;
#29002=AXIS2_PLACEMENT_3D ( 'NONE', #49404, #41921, #7704 ) ;
#29004=VECTOR ( 'NONE', #64893, 1000.000000000000000 ) ;
#29005=EDGE_CURVE ( 'NONE', #3846, #28823, #16140, .T. ) ;
#29010=CARTESIAN_POINT ( 'NONE',  ( 10.00000000000000000, 0.000000000000000000, 0.000000000000000000 ) ) ;
#29016=ORIENTED_EDGE ( 'NONE', *, *, #51088, .F. ) ;
#29020=ORIENTED_EDGE ( 'NONE', *, *, #59741, .F. ) ;
#29024=CARTESIAN_POINT ( 'NONE',  ( 10.00000000000000000, -41.19522573413687638, -65.64334221924953283 ) ) ;
#29031=ADVANCED_FACE ( 'NONE', ( #62013 ), #4508, .T. ) ;
#29034=VERTEX_POINT ( 'NONE', #10492 ) ;
#29040=CARTESIAN_POINT ( 'NONE',  ( -10.00000000000000000, 0.000000000000000000, 0.000000000000000000 ) ) ;
#29041=AXIS2_PLACEMENT_3D ( 'NONE', #27498, #22239, #10960 ) ;
#29049=VECTOR ( 'NONE', #1928, 1000.000000000000000 ) ;
#29061=DIRECTION ( 'NONE',  ( -1.000000000000000000, -0.000000000000000000, 0.000000000000000000 ) ) ;
#29064=CIRCLE ( 'NONE', #12202, 77.49899999999999523 ) ;
#29067=ORIENTED_EDGE ( 'NONE', *, *, #65667, .F. ) ;
#29072=LINE ( 'NONE', #52000, #57827 ) ;
#29074=ORIENTED_EDGE ( 'NONE', *, *, #26287, .F. ) ;
#29077=DIRECTION ( 'NONE',  ( -1.000000000000000000, 0.000000000000000000, 0.000000000000000000 ) ) ;
#29089=EDGE_CURVE ( 'NONE', #961, #16368, #21025, .T. ) ;
#29093=DIRECTION ( 'NONE',  ( 1.000000000000000000, 0.000000000000000000, 0.000000000000000000 ) ) ;
#29096=AXIS2_PLACEMENT_3D ( 'NONE', #28143, #10862, #57106 ) ;
#29097=DIRECTION ( 'NONE',  ( 0.000000000000000000, 0.000000000000000000, 1.000000000000000000 ) ) ;
#29098=VERTEX_POINT ( 'NONE', #37596 ) ;
#29104=AXIS2_PLACEMENT_3D ( 'NONE', #1056, #5564, #58154 ) ;
#29107=VERTEX_POINT ( 'NONE', #46566 ) ;
#29110=DIRECTION ( 'NONE',  ( 0.000000000000000000, 0.000000000000000000, 1.000000000000000000 ) ) ;
#29133=DIRECTION ( 'NONE',  ( -1.000000000000000000, 0.000000000000000000, -0.000000000000000000 ) ) ;
#29144=ORIENTED_EDGE ( 'NONE', *, *, #10580, .T. ) ;
#29148=ORIENTED_EDGE ( 'NONE', *, *, #21301, .F. ) ;
#29150=EDGE_LOOP ( 'NONE', ( #1247, #25969, #15062, #49311 ) ) ;
#29155=AXIS2_PLACEMENT_3D ( 'NONE', #69377, #56637, #63030 ) ;
#29158=CARTESIAN_POINT ( 'NONE',  ( 0.000000000000000000, 27.74655509720669500, 77.16300072079670258 ) ) ;
#29165=DIRECTION ( 'NONE',  ( 0.000000000000000000, 0.000000000000000000, 1.000000000000000000 ) ) ;
#29172=ORIENTED_EDGE ( 'NONE', *, *, #26044, .F. ) ;
#29184=CARTESIAN_POINT ( 'NONE',  ( 10.00000000000000000, 0.8261519478431083030, 77.49459641780886443 ) ) ;
#29188=ORIENTED_EDGE ( 'NONE', *, *, #73427, .F. ) ;
#29207=CIRCLE ( 'NONE', #72457, 31.99999999999998934 ) ;
#29212=CARTESIAN_POINT ( 'NONE',  ( 10.00000000000000000, -59.03342792756297541, 46.54456581323783126 ) ) ;
#29218=CYLINDRICAL_SURFACE ( 'NONE', #5702, 31.99999999999999289 ) ;
#29227=PLANE ( 'NONE',  #3525 ) ;
#29233=ORIENTED_EDGE ( 'NONE', *, *, #46857, .F. ) ;
#29236=DIRECTION ( 'NONE',  ( 0.000000000000000000, 0.000000000000000000, 1.000000000000000000 ) ) ;
#29240=VERTEX_POINT ( 'NONE', #36754 ) ;
#29251=CARTESIAN_POINT ( 'NONE',  ( 0.000000000000000000, 0.000000000000000000, 0.000000000000000000 ) ) ;
#29257=DIRECTION ( 'NONE',  ( 0.000000000000000000, 0.9238795325112851842, 0.3826834323650938341 ) ) ;
#29258=CIRCLE ( 'NONE', #490, 77.49900000000000944 ) ;
#29274=LINE ( 'NONE', #35654, #4717 ) ;
#29285=AXIS2_PLACEMENT_3D ( 'NONE', #67167, #31826, #54776 ) ;
#29300=CYLINDRICAL_SURFACE ( 'NONE', #17795, 77.49899999999999523 ) ;
#29303=CARTESIAN_POINT ( 'NONE',  ( 10.00000000000000000, 21.60688246758585862, 79.10210256391376049 ) ) ;
#29308=SURFACE_SIDE_STYLE ('',( #6408 ) ) ;
#29314=CARTESIAN_POINT ( 'NONE',  ( 0.000000000000000000, -23.16143007188376757, -73.95703589263997912 ) ) ;
#29324=ORIENTED_EDGE ( 'NONE', *, *, #66737, .T. ) ;
#29335=DIRECTION ( 'NONE',  ( 0.000000000000000000, 0.000000000000000000, 1.000000000000000000 ) ) ;
#29338=EDGE_CURVE ( 'NONE', #63936, #10604, #25083, .T. ) ;
#29339=DIRECTION ( 'NONE',  ( 0.000000000000000000, 0.000000000000000000, 1.000000000000000000 ) ) ;
#29340=ADVANCED_FACE ( 'NONE', ( #58963 ), #60085, .T. ) ;
#29350=CARTESIAN_POINT ( 'NONE',  ( 0.000000000000000000, 0.000000000000000000, 12.50000000000000000 ) ) ;
#29351=VECTOR ( 'NONE', #43935, 1000.000000000000000 ) ;
#29354=DIRECTION ( 'NONE',  ( 0.000000000000000000, 0.000000000000000000, -1.000000000000000000 ) ) ;
#29357=ORIENTED_EDGE ( 'NONE', *, *, #9776, .F. ) ;
#29362=DIRECTION ( 'NONE',  ( -1.000000000000000000, -0.000000000000000000, -0.000000000000000000 ) ) ;
#29365=CIRCLE ( 'NONE', #66630, 31.99999999999999645 ) ;
#29387=ORIENTED_EDGE ( 'NONE', *, *, #73652, .F. ) ;
#29393=EDGE_LOOP ( 'NONE', ( #48176, #71817, #21610, #25773 ) ) ;
#29399=CARTESIAN_POINT ( 'NONE',  ( 10.00000000000000000, 46.54456581323888997, -59.03342792756214408 ) ) ;
#29404=VERTEX_POINT ( 'NONE', #2219 ) ;
#29420=ORIENTED_EDGE ( 'NONE', *, *, #2815, .T. ) ;
#29452=AXIS2_PLACEMENT_3D ( 'NONE', #45778, #34465, #50269 ) ;
#29453=DIRECTION ( 'NONE',  ( 1.000000000000000000, 0.000000000000000000, 0.000000000000000000 ) ) ;
#29462=CIRCLE ( 'NONE', #23475, 31.99999999999999289 ) ;
#29468=VECTOR ( 'NONE', #49045, 1000.000000000000000 ) ;
#29471=ORIENTED_EDGE ( 'NONE', *, *, #4703, .F. ) ;
#29474=VERTEX_POINT ( 'NONE', #27314 ) ;
#29483=ORIENTED_EDGE ( 'NONE', *, *, #62697, .T. ) ;
#29485=ORIENTED_EDGE ( 'NONE', *, *, #72893, .F. ) ;
#29489=DIRECTION ( 'NONE',  ( -1.000000000000000000, 0.000000000000000000, 0.000000000000000000 ) ) ;
#29519=CIRCLE ( 'NONE', #35540, 31.99999999999999289 ) ;
#29522=DIRECTION ( 'NONE',  ( 1.000000000000000000, -0.000000000000000000, -0.000000000000000000 ) ) ;
#29523=CIRCLE ( 'NONE', #42585, 82.00000000000000000 ) ;
#29554=ORIENTED_EDGE ( 'NONE', *, *, #57485, .F. ) ;
#29569=DIRECTION ( 'NONE',  ( 0.000000000000000000, 0.000000000000000000, 1.000000000000000000 ) ) ;
#29574=ORIENTED_EDGE ( 'NONE', *, *, #21395, .T. ) ;
#29588=ORIENTED_EDGE ( 'NONE', *, *, #56654, .F. ) ;
#29589=CARTESIAN_POINT ( 'NONE',  ( 5.000000000000002665, -71.87247863392386193, -39.47590169984923136 ) ) ;
#29591=ORIENTED_EDGE ( 'NONE', *, *, #6397, .F. ) ;
#29592=ADVANCED_FACE ( 'NONE', ( #61926 ), #45758, .T. ) ;
#29593=AXIS2_PLACEMENT_3D ( 'NONE', #40211, #44750, #63162 ) ;
#29594=ORIENTED_EDGE ( 'NONE', *, *, #22355, .F. ) ;
#29598=VERTEX_POINT ( 'NONE', #11513 ) ;
#29599=DIRECTION ( 'NONE',  ( -1.000000000000000000, 0.000000000000000000, -0.000000000000000000 ) ) ;
#29604=CARTESIAN_POINT ( 'NONE',  ( 10.00000000000000000, 39.47590169984943742, -71.87247863392373404 ) ) ;
#29609=AXIS2_PLACEMENT_3D ( 'NONE', #44305, #22114, #66501 ) ;
#29617=EDGE_CURVE ( 'NONE', #39587, #10916, #9343, .T. ) ;
#29619=DIRECTION ( 'NONE',  ( 0.000000000000000000, 0.000000000000000000, 1.000000000000000000 ) ) ;
#29628=EDGE_CURVE ( 'NONE', #31772, #26087, #17777, .T. ) ;
#29630=VECTOR ( 'NONE', #24532, 1000.000000000000000 ) ;
#29632=AXIS2_PLACEMENT_3D ( 'NONE', #56372, #28154, #5253 ) ;
#29636=AXIS2_PLACEMENT_3D ( 'NONE', #16520, #28913, #34930 ) ;
#29638=CARTESIAN_POINT ( 'NONE',  ( 10.00000000000000000, 78.73519480814985627, -22.90783923731548910 ) ) ;
#29641=CIRCLE ( 'NONE', #3295, 82.00000000000000000 ) ;
#29644=CIRCLE ( 'NONE', #5649, 31.99999999999999289 ) ;
#29651=ORIENTED_EDGE ( 'NONE', *, *, #7982, .F. ) ;
#29662=FACE_OUTER_BOUND ( 'NONE', #15900, .T. ) ;
#29666=DIRECTION ( 'NONE',  ( 0.000000000000000000, 0.000000000000000000, 1.000000000000000000 ) ) ;
#29671=EDGE_CURVE ( 'NONE', #16822, #63002, #58608, .T. ) ;
#29678=VERTEX_POINT ( 'NONE', #22820 ) ;
#29681=AXIS2_PLACEMENT_3D ( 'NONE', #8838, #31753, #26857 ) ;
#29684=EDGE_CURVE ( 'NONE', #68371, #36612, #10788, .T. ) ;
#29688=CARTESIAN_POINT ( 'NONE',  ( 10.00000000000000000, 36.72794159290241822, 65.59268652807223532 ) ) ;
#29692=EDGE_CURVE ( 'NONE', #40404, #64515, #17530, .T. ) ;
#29705=CARTESIAN_POINT ( 'NONE',  ( 10.00000000000000000, 55.19960302592141232, -51.03279382321027668 ) ) ;
#29709=DIRECTION ( 'NONE',  ( -1.000000000000000000, 0.000000000000000000, 0.000000000000000000 ) ) ;
#29740=ORIENTED_EDGE ( 'NONE', *, *, #30529, .F. ) ;
#29752=VECTOR ( 'NONE', #57205, 1000.000000000000000 ) ;
#29756=EDGE_CURVE ( 'NONE', #17478, #16649, #18944, .T. ) ;
#29757=ORIENTED_EDGE ( 'NONE', *, *, #40380, .T. ) ;
#29763=ORIENTED_EDGE ( 'NONE', *, *, #22956, .T. ) ;
#29771=DIRECTION ( 'NONE',  ( -1.000000000000000000, 0.000000000000000000, 0.000000000000000000 ) ) ;
#29778=CARTESIAN_POINT ( 'NONE',  ( 0.000000000000000000, 0.000000000000000000, 0.000000000000000000 ) ) ;
#29779=DIRECTION ( 'NONE',  ( 0.000000000000000000, 0.000000000000000000, 1.000000000000000000 ) ) ;
#29786=AXIS2_PLACEMENT_3D ( 'NONE', #33986, #50146, #39266 ) ;
#29813=CIRCLE ( 'NONE', #23818, 31.99999999999999289 ) ;
#29823=CARTESIAN_POINT ( 'NONE',  ( 10.00000000000000000, 26.01480285779837232, 70.53064760720326376 ) ) ;
#29833=ORIENTED_EDGE ( 'NONE', *, *, #15027, .F. ) ;
#29834=CIRCLE ( 'NONE', #17826, 31.99999999999999289 ) ;
#29835=CIRCLE ( 'NONE', #63466, 31.99999999999999645 ) ;
#29838=ORIENTED_EDGE ( 'NONE', *, *, #28411, .T. ) ;
#29841=ORIENTED_EDGE ( 'NONE', *, *, #16710, .F. ) ;
#29842=CARTESIAN_POINT ( 'NONE',  ( 10.00000000000000000, 56.15606465355042332, -59.75363087400016582 ) ) ;
#29845=ORIENTED_EDGE ( 'NONE', *, *, #18353, .T. ) ;
#29849=AXIS2_PLACEMENT_3D ( 'NONE', #39619, #62178, #45264 ) ;
#29857=ORIENTED_EDGE ( 'NONE', *, *, #32125, .T. ) ;
#29861=CYLINDRICAL_SURFACE ( 'NONE', #61528, 31.99999999999999289 ) ;
#29869=ORIENTED_EDGE ( 'NONE', *, *, #61211, .T. ) ;
#29870=CARTESIAN_POINT ( 'NONE',  ( 10.00000000000000000, -68.67312586195023982, 35.91791733033450384 ) ) ;
#29874=AXIS2_PLACEMENT_3D ( 'NONE', #69151, #7745, #760 ) ;
#29875=ORIENTED_EDGE ( 'NONE', *, *, #19668, .F. ) ;
#29885=ORIENTED_EDGE ( 'NONE', *, *, #6956, .T. ) ;
#29887=EDGE_CURVE ( 'NONE', #57102, #37315, #1085, .T. ) ;
#29897=DIRECTION ( 'NONE',  ( 0.000000000000000000, -0.6494480483301741103, -0.7604059656000390355 ) ) ;
#29905=CARTESIAN_POINT ( 'NONE',  ( 10.00000000000000000, 62.50329211542435104, 41.76937507738811917 ) ) ;
#29914=ORIENTED_EDGE ( 'NONE', *, *, #67206, .T. ) ;
#29920=AXIS2_PLACEMENT_3D ( 'NONE', #33056, #9390, #66187 ) ;
#29922=ORIENTED_EDGE ( 'NONE', *, *, #59180, .F. ) ;
#29939=DIRECTION ( 'NONE',  ( 0.000000000000000000, -0.4539904997395350916, -0.8910065241883738940 ) ) ;
#29945=CIRCLE ( 'NONE', #61198, 82.00000000000000000 ) ;
#29951=CIRCLE ( 'NONE', #21587, 77.49899999999999523 ) ;
#29952=DIRECTION ( 'NONE',  ( 0.000000000000000000, 0.8910065241883657894, 0.4539904997395510788 ) ) ;
#29955=VERTEX_POINT ( 'NONE', #45190 ) ;
#29959=EDGE_CURVE ( 'NONE', #73572, #32622, #61029, .T. ) ;
#29963=EDGE_CURVE ( 'NONE', #17478, #57845, #52661, .T. ) ;
#29965=EDGE_CURVE ( 'NONE', #32553, #2885, #35799, .T. ) ;
#29968=CIRCLE ( 'NONE', #17958, 31.99999999999999289 ) ;
#29970=DIRECTION ( 'NONE',  ( -1.000000000000000000, -0.000000000000000000, 0.000000000000000000 ) ) ;
#29973=EDGE_CURVE ( 'NONE', #36744, #71285, #11803, .T. ) ;
#29984=CARTESIAN_POINT ( 'NONE',  ( 0.000000000000000000, 50.23322058963442061, -64.81221759200289512 ) ) ;
#29988=VERTEX_POINT ( 'NONE', #33139 ) ;
#29993=FACE_OUTER_BOUND ( 'NONE', #33856, .T. ) ;
#30004=CARTESIAN_POINT ( 'NONE',  ( 10.00000000000000000, 77.19088730480534366, -6.903761155836915187 ) ) ;
#30005=AXIS2_PLACEMENT_3D ( 'NONE', #57450, #55960, #68370 ) ;
#30011=EDGE_CURVE ( 'NONE', #70, #30710, #29835, .T. ) ;
#30012=VECTOR ( 'NONE', #29599, 1000.000000000000000 ) ;
#30019=ADVANCED_FACE ( 'NONE', ( #71610 ), #56085, .T. ) ;
#30025=CARTESIAN_POINT ( 'NONE',  ( 0.000000000000000000, 49.70050353004977239, -59.46389618801908483 ) ) ;
#30033=DIRECTION ( 'NONE',  ( 0.000000000000000000, 1.000000000000000000, 0.000000000000000000 ) ) ;
#30044=CARTESIAN_POINT ( 'NONE',  ( 10.00000000000000000, -36.73666225445845157, -65.58780272294114866 ) ) ;
#30047=EDGE_LOOP ( 'NONE', ( #56241, #23409, #60307, #19105 ) ) ;
#30052=ORIENTED_EDGE ( 'NONE', *, *, #68989, .F. ) ;
#30061=ORIENTED_EDGE ( 'NONE', *, *, #13977, .F. ) ;
#30062=AXIS2_PLACEMENT_3D ( 'NONE', #36722, #26179, #9641 ) ;
#30063=EDGE_LOOP ( 'NONE', ( #13948, #23171, #31603, #8549 ) ) ;
#30071=ORIENTED_EDGE ( 'NONE', *, *, #31292, .T. ) ;
#30076=DIRECTION ( 'NONE',  ( 0.000000000000000000, 0.000000000000000000, 1.000000000000000000 ) ) ;
#30081=AXIS2_PLACEMENT_3D ( 'NONE', #35784, #30152, #65496 ) ;
#30082=AXIS2_PLACEMENT_3D ( 'NONE', #65768, #72135, #60508 ) ;
#30088=CARTESIAN_POINT ( 'NONE',  ( 0.000000000000000000, -76.66974797899828786, -11.30684508768421992 ) ) ;
#30096=DIRECTION ( 'NONE',  ( -1.000000000000000000, -0.000000000000000000, -0.000000000000000000 ) ) ;
#30107=EDGE_CURVE ( 'NONE', #59010, #70889, #74229, .T. ) ;
#30126=AXIS2_PLACEMENT_3D ( 'NONE', #5231, #3743, #26645 ) ;
#30130=VECTOR ( 'NONE', #71141, 1000.000000000000000 ) ;
#30132=DIRECTION ( 'NONE',  ( 0.000000000000000000, -0.9510565162951500895, -0.3090169943749583870 ) ) ;
#30135=EDGE_CURVE ( 'NONE', #73972, #11744, #63226, .T. ) ;
#30142=EDGE_LOOP ( 'NONE', ( #46892, #22744, #41143, #23665 ) ) ;
#30144=DIRECTION ( 'NONE',  ( -1.000000000000000000, 0.000000000000000000, 0.000000000000000000 ) ) ;
#30146=EDGE_CURVE ( 'NONE', #23492, #32553, #39922, .T. ) ;
#30152=DIRECTION ( 'NONE',  ( -1.000000000000000000, 0.000000000000000000, 0.000000000000000000 ) ) ;
#30167=AXIS2_PLACEMENT_3D ( 'NONE', #59864, #18877, #70372 ) ;
#30172=ORIENTED_EDGE ( 'NONE', *, *, #50706, .T. ) ;
#30179=DIRECTION ( 'NONE',  ( 0.000000000000000000, 0.000000000000000000, 1.000000000000000000 ) ) ;
#30182=DIRECTION ( 'NONE',  ( -1.000000000000000000, 0.000000000000000000, -0.000000000000000000 ) ) ;
#30184=CYLINDRICAL_SURFACE ( 'NONE', #64462, 32.00000000000000000 ) ;
#30192=CIRCLE ( 'NONE', #49409, 77.49899999999999523 ) ;
#30195=CIRCLE ( 'NONE', #32552, 77.49899999999999523 ) ;
#30196=CYLINDRICAL_SURFACE ( 'NONE', #15385, 77.49899999999999523 ) ;
#30203=CARTESIAN_POINT ( 'NONE',  ( 5.000000000000002665, -2.543863470247813119, -81.96053171279905314 ) ) ;
#30206=DIRECTION ( 'NONE',  ( 0.000000000000000000, 0.000000000000000000, -1.000000000000000000 ) ) ;
#30208=VERTEX_POINT ( 'NONE', #46658 ) ;
#30211=DIRECTION ( 'NONE',  ( 0.000000000000000000, 0.000000000000000000, 1.000000000000000000 ) ) ;
#30219=VERTEX_POINT ( 'NONE', #58679 ) ;
#30233=ORIENTED_EDGE ( 'NONE', *, *, #33338, .F. ) ;
#30247=DIRECTION ( 'NONE',  ( 0.000000000000000000, 0.000000000000000000, 1.000000000000000000 ) ) ;
#30248=ORIENTED_EDGE ( 'NONE', *, *, #14004, .F. ) ;
#30258=ORIENTED_EDGE ( 'NONE', *, *, #18482, .T. ) ;
#30261=VERTEX_POINT ( 'NONE', #42876 ) ;
#30262=ORIENTED_EDGE ( 'NONE', *, *, #66489, .F. ) ;
#30264=DIRECTION ( 'NONE',  ( 0.000000000000000000, 0.000000000000000000, 1.000000000000000000 ) ) ;
#30293=CIRCLE ( 'NONE', #47112, 82.00000000000000000 ) ;
#30299=ORIENTED_EDGE ( 'NONE', *, *, #17433, .T. ) ;
#30301=DIRECTION ( 'NONE',  ( -1.000000000000000000, 0.000000000000000000, 0.000000000000000000 ) ) ;
#30306=ADVANCED_FACE ( 'NONE', ( #53771 ), #24467, .T. ) ;
#30310=CARTESIAN_POINT ( 'NONE',  ( 0.000000000000000000, 0.000000000000000000, 0.000000000000000000 ) ) ;
#30311=CARTESIAN_POINT ( 'NONE',  ( 10.00000000000000000, -18.89407956138203204, -75.16055320797050854 ) ) ;
#30313=LINE ( 'NONE', #684, #50145 ) ;
#30317=ORIENTED_EDGE ( 'NONE', *, *, #53831, .F. ) ;
#30324=CARTESIAN_POINT ( 'NONE',  ( 10.00000000000000000, 65.58780272294129077, -36.73666225445822420 ) ) ;
#30330=ORIENTED_EDGE ( 'NONE', *, *, #58886, .T. ) ;
#30334=CIRCLE ( 'NONE', #49539, 31.99999999999999289 ) ;
#30343=CIRCLE ( 'NONE', #26742, 31.99999999999999289 ) ;
#30344=CIRCLE ( 'NONE', #72367, 32.00000000000000000 ) ;
#30346=ORIENTED_EDGE ( 'NONE', *, *, #3147, .F. ) ;
#30354=ORIENTED_EDGE ( 'NONE', *, *, #66190, .F. ) ;
#30356=ORIENTED_EDGE ( 'NONE', *, *, #33801, .T. ) ;
#30358=CARTESIAN_POINT ( 'NONE',  ( 0.000000000000000000, 0.000000000000000000, 0.000000000000000000 ) ) ;
#30367=ADVANCED_FACE ( 'NONE', ( #36850 ), #31574, .T. ) ;
#30371=EDGE_CURVE ( 'NONE', #56493, #60043, #33488, .T. ) ;
#30379=AXIS2_PLACEMENT_3D ( 'NONE', #74238, #50940, #50565 ) ;
#30390=EDGE_CURVE ( 'NONE', #63033, #7419, #71909, .T. ) ;
#30409=CYLINDRICAL_SURFACE ( 'NONE', #52678, 32.00000000000000000 ) ;
#30418=DIRECTION ( 'NONE',  ( 0.000000000000000000, -0.8090169943749403458, -0.5877852522924830181 ) ) ;
#30422=ORIENTED_EDGE ( 'NONE', *, *, #21445, .F. ) ;
#30423=AXIS2_PLACEMENT_3D ( 'NONE', #36323, #49086, #7762 ) ;
#30433=EDGE_LOOP ( 'NONE', ( #33081, #8626, #70710, #53712 ) ) ;
#30440=LINE ( 'NONE', #8642, #15856 ) ;
#30449=EDGE_CURVE ( 'NONE', #1351, #41590, #16709, .T. ) ;
#30450=LINE ( 'NONE', #2676, #13494 ) ;
#30457=EDGE_CURVE ( 'NONE', #14882, #53902, #43126, .T. ) ;
#30466=EDGE_CURVE ( 'NONE', #47594, #54289, #8277, .T. ) ;
#30473=EDGE_CURVE ( 'NONE', #27844, #30208, #26302, .T. ) ;
#30476=CYLINDRICAL_SURFACE ( 'NONE', #1948, 82.00000000000000000 ) ;
#30477=ORIENTED_EDGE ( 'NONE', *, *, #58305, .F. ) ;
#30481=ORIENTED_EDGE ( 'NONE', *, *, #28627, .F. ) ;
#30482=AXIS2_PLACEMENT_3D ( 'NONE', #68348, #16089, #62726 ) ;
#30488=ADVANCED_FACE ( 'NONE', ( #66546 ), #62021, .T. ) ;
#30503=CARTESIAN_POINT ( 'NONE',  ( 0.000000000000000000, -51.03279382321048985, -55.19960302592120627 ) ) ;
#30505=CIRCLE ( 'NONE', #24567, 31.99999999999999289 ) ;
#30506=ORIENTED_EDGE ( 'NONE', *, *, #48959, .T. ) ;
#30524=LINE ( 'NONE', #53472, #11917 ) ;
#30526=CYLINDRICAL_SURFACE ( 'NONE', #46333, 31.99999999999999289 ) ;
#30529=EDGE_CURVE ( 'NONE', #31227, #30208, #15024, .T. ) ;
#30534=CIRCLE ( 'NONE', #11327, 31.99999999999998934 ) ;
#30542=DIRECTION ( 'NONE',  ( -1.000000000000000000, -0.000000000000000000, -0.000000000000000000 ) ) ;
#30546=CARTESIAN_POINT ( 'NONE',  ( 0.000000000000000000, 50.95692526931414790, -58.39081064771693974 ) ) ;
#30549=DIRECTION ( 'NONE',  ( -1.000000000000000000, 0.000000000000000000, 0.000000000000000000 ) ) ;
#30550=CIRCLE ( 'NONE', #26953, 32.00000000000000000 ) ;
#30572=DIRECTION ( 'NONE',  ( 0.000000000000000000, 0.000000000000000000, 1.000000000000000000 ) ) ;
#30575=DIRECTION ( 'NONE',  ( 1.000000000000000000, 0.000000000000000000, -0.000000000000000000 ) ) ;
#30578=CYLINDRICAL_SURFACE ( 'NONE', #69973, 82.00000000000000000 ) ;
#30579=VERTEX_POINT ( 'NONE', #51841 ) ;
#30581=AXIS2_PLACEMENT_3D ( 'NONE', #49098, #54744, #70915 ) ;
#30590=AXIS2_PLACEMENT_3D ( 'NONE', #45148, #38390, #4561 ) ;
#30597=VECTOR ( 'NONE', #942, 1000.000000000000000 ) ;
#30599=CARTESIAN_POINT ( 'NONE',  ( 10.00000000000000000, 21.60688246758695641, -79.10210256391344785 ) ) ;
#30600=DIRECTION ( 'NONE',  ( 0.000000000000000000, 0.000000000000000000, 1.000000000000000000 ) ) ;
#30604=DIRECTION ( 'NONE',  ( 0.000000000000000000, -0.9510565162951500895, -0.3090169943749583870 ) ) ;
#30605=DIRECTION ( 'NONE',  ( -1.000000000000000000, 0.000000000000000000, 0.000000000000000000 ) ) ;
#30618=ORIENTED_EDGE ( 'NONE', *, *, #50479, .T. ) ;
#30626=EDGE_CURVE ( 'NONE', #38932, #14488, #64689, .T. ) ;
#30628=CARTESIAN_POINT ( 'NONE',  ( 10.00000000000000000, 0.000000000000000000, 0.000000000000000000 ) ) ;
#30629=DIRECTION ( 'NONE',  ( -1.000000000000000000, 0.000000000000000000, 0.000000000000000000 ) ) ;
#30640=CYLINDRICAL_SURFACE ( 'NONE', #63688, 31.99999999999999289 ) ;
#30643=DIRECTION ( 'NONE',  ( 1.000000000000000000, 0.000000000000000000, 0.000000000000000000 ) ) ;
#30650=FACE_OUTER_BOUND ( 'NONE', #29150, .T. ) ;
#30651=EDGE_LOOP ( 'NONE', ( #72133, #52729, #2074, #25124 ) ) ;
#30660=ORIENTED_EDGE ( 'NONE', *, *, #382, .T. ) ;
#30663=AXIS2_PLACEMENT_3D ( 'NONE', #47470, #24534, #40723 ) ;
#30672=DIRECTION ( 'NONE',  ( 0.000000000000000000, -0.3090169943749349057, -0.9510565162951577500 ) ) ;
#30674=FACE_OUTER_BOUND ( 'NONE', #24394, .T. ) ;
#30680=VERTEX_POINT ( 'NONE', #57123 ) ;
#30681=ORIENTED_EDGE ( 'NONE', *, *, #56282, .T. ) ;
#30686=CARTESIAN_POINT ( 'NONE',  ( 0.000000000000000000, 67.80270845531887858, 46.11716303203210998 ) ) ;
#30697=ORIENTED_EDGE ( 'NONE', *, *, #3257, .F. ) ;
#30705=DIRECTION ( 'NONE',  ( 0.000000000000000000, 0.000000000000000000, -1.000000000000000000 ) ) ;
#30707=CYLINDRICAL_SURFACE ( 'NONE', #49499, 32.00000000000000000 ) ;
#30708=CIRCLE ( 'NONE', #19861, 31.99999999999999645 ) ;
#30710=VERTEX_POINT ( 'NONE', #47319 ) ;
#30722=ORIENTED_EDGE ( 'NONE', *, *, #64614, .F. ) ;
#30738=CARTESIAN_POINT ( 'NONE',  ( 10.00000000000000000, 31.46837873494978055, 68.27212725128286763 ) ) ;
#30742=DIRECTION ( 'NONE',  ( 1.000000000000000000, 0.000000000000000000, 0.000000000000000000 ) ) ;
#30752=ORIENTED_EDGE ( 'NONE', *, *, #32822, .F. ) ;
#30755=CIRCLE ( 'NONE', #34373, 31.99999999999999289 ) ;
#30757=AXIS2_PLACEMENT_3D ( 'NONE', #10198, #33120, #57190 ) ;
#30762=ORIENTED_EDGE ( 'NONE', *, *, #31894, .F. ) ;
#30769=EDGE_CURVE ( 'NONE', #70184, #50464, #74339, .T. ) ;
#30770=VERTEX_POINT ( 'NONE', #12714 ) ;
#30771=DIRECTION ( 'NONE',  ( 0.000000000000000000, -0.6494480483301903195, 0.7604059656000251577 ) ) ;
#30776=DIRECTION ( 'NONE',  ( 0.000000000000000000, 0.000000000000000000, 1.000000000000000000 ) ) ;
#30778=ORIENTED_EDGE ( 'NONE', *, *, #65758, .F. ) ;
#30784=EDGE_CURVE ( 'NONE', #30710, #66307, #35644, .T. ) ;
#30795=VERTEX_POINT ( 'NONE', #30004 ) ;
#30797=LINE ( 'NONE', #35703, #44311 ) ;
#30802=DIRECTION ( 'NONE',  ( 0.000000000000000000, -0.7071067811865389130, -0.7071067811865561215 ) ) ;
#30807=LINE ( 'NONE', #24446, #29049 ) ;
#30808=AXIS2_PLACEMENT_3D ( 'NONE', #63999, #46697, #58343 ) ;
#30841=DIRECTION ( 'NONE',  ( -1.000000000000000000, 0.000000000000000000, 0.000000000000000000 ) ) ;
#30864=DIRECTION ( 'NONE',  ( -1.000000000000000000, 0.000000000000000000, -0.000000000000000000 ) ) ;
#30876=CARTESIAN_POINT ( 'NONE',  ( 10.00000000000000000, -81.96053171279899630, -2.543863470249235981 ) ) ;
#30886=AXIS2_PLACEMENT_3D ( 'NONE', #342, #11559, #51050 ) ;
#30891=ORIENTED_EDGE ( 'NONE', *, *, #69519, .T. ) ;
#30908=ADVANCED_FACE ( 'NONE', ( #26591 ), #21307, .T. ) ;
#30912=CARTESIAN_POINT ( 'NONE',  ( 10.00000000000000000, 0.000000000000000000, 0.000000000000000000 ) ) ;
#30915=EDGE_CURVE ( 'NONE', #67983, #47594, #9506, .T. ) ;
#30920=DIRECTION ( 'NONE',  ( -1.000000000000000000, 0.000000000000000000, 0.000000000000000000 ) ) ;
#30923=DIRECTION ( 'NONE',  ( -1.000000000000000000, 0.000000000000000000, 0.000000000000000000 ) ) ;
#30928=DIRECTION ( 'NONE',  ( -1.000000000000000000, -0.000000000000000000, -0.000000000000000000 ) ) ;
#30930=CARTESIAN_POINT ( 'NONE',  ( 10.00000000000000000, 62.50329211542435104, 41.76937507738811917 ) ) ;
#30940=EDGE_LOOP ( 'NONE', ( #8207, #33871, #39308, #8692 ) ) ;
#30944=ORIENTED_EDGE ( 'NONE', *, *, #34064, .F. ) ;
#30950=EDGE_CURVE ( 'NONE', #47594, #9891, #67567, .T. ) ;
#30952=EDGE_LOOP ( 'NONE', ( #40608, #22200, #64575, #8708 ) ) ;
#30959=CARTESIAN_POINT ( 'NONE',  ( 0.000000000000000000, 59.03342792756263435, 46.54456581323825048 ) ) ;
#30960=AXIS2_PLACEMENT_3D ( 'NONE', #28469, #16839, #16460 ) ;
#30970=DIRECTION ( 'NONE',  ( -1.000000000000000000, 0.000000000000000000, 0.000000000000000000 ) ) ;
#30976=LINE ( 'NONE', #48283, #2448 ) ;
#30977=CARTESIAN_POINT ( 'NONE',  ( -10.00000000000000000, 0.000000000000000000, 0.000000000000000000 ) ) ;
#30985=LINE ( 'NONE', #48663, #72127 ) ;
#30987=DIRECTION ( 'NONE',  ( -1.000000000000000000, 0.000000000000000000, 0.000000000000000000 ) ) ;
#30988=CARTESIAN_POINT ( 'NONE',  ( -10.00000000000000000, 0.000000000000000000, 0.000000000000000000 ) ) ;
#30993=ADVANCED_FACE ( 'NONE', ( #66342 ), #54312, .T. ) ;
#30994=CARTESIAN_POINT ( 'NONE',  ( 5.000000000000000000, 55.16347631943131802, -60.67117009219075641 ) ) ;
#30995=ORIENTED_EDGE ( 'NONE', *, *, #45283, .T. ) ;
#30998=AXIS2_PLACEMENT_3D ( 'NONE', #42619, #36973, #37726 ) ;
#31001=DIRECTION ( 'NONE',  ( -1.000000000000000000, 0.000000000000000000, 0.000000000000000000 ) ) ;
#31018=AXIS2_PLACEMENT_3D ( 'NONE', #48357, #53264, #14888 ) ;
#31033=VERTEX_POINT ( 'NONE', #71580 ) ;
#31037=DIRECTION ( 'NONE',  ( 0.000000000000000000, 0.000000000000000000, 1.000000000000000000 ) ) ;
#31041=VECTOR ( 'NONE', #62048, 1000.000000000000000 ) ;
#31043=CIRCLE ( 'NONE', #73065, 77.49899999999999523 ) ;
#31046=DIRECTION ( 'NONE',  ( -1.000000000000000000, -0.000000000000000000, -0.000000000000000000 ) ) ;
#31047=DIRECTION ( 'NONE',  ( 1.000000000000000000, -0.000000000000000000, 0.000000000000000000 ) ) ;
#31056=ORIENTED_EDGE ( 'NONE', *, *, #20392, .F. ) ;
#31057=DIRECTION ( 'NONE',  ( -1.000000000000000000, 0.000000000000000000, 0.000000000000000000 ) ) ;
#31072=DIRECTION ( 'NONE',  ( 0.000000000000000000, -0.3826834323650969427, 0.9238795325112838519 ) ) ;
#31077=DIRECTION ( 'NONE',  ( 0.000000000000000000, 0.000000000000000000, 1.000000000000000000 ) ) ;
#31085=VERTEX_POINT ( 'NONE', #65594 ) ;
#31107=VECTOR ( 'NONE', #60549, 1000.000000000000000 ) ;
#31112=DIRECTION ( 'NONE',  ( -1.000000000000000000, -0.000000000000000000, -0.000000000000000000 ) ) ;
#31121=ORIENTED_EDGE ( 'NONE', *, *, #27146, .F. ) ;
#31130=AXIS2_PLACEMENT_3D ( 'NONE', #2236, #25129, #72088 ) ;
#31131=VERTEX_POINT ( 'NONE', #50878 ) ;
#31146=DIRECTION ( 'NONE',  ( 0.000000000000000000, 0.000000000000000000, 1.000000000000000000 ) ) ;
#31147=CIRCLE ( 'NONE', #25153, 31.99999999999999645 ) ;
#31148=CARTESIAN_POINT ( 'NONE',  ( 10.00000000000000000, 71.91182617369189245, 28.89263327155772743 ) ) ;
#31157=DIRECTION ( 'NONE',  ( -1.000000000000000000, 0.000000000000000000, 0.000000000000000000 ) ) ;
#31168=CARTESIAN_POINT ( 'NONE',  ( 0.000000000000000000, -18.89407956138203204, -75.16055320797050854 ) ) ;
#31178=ORIENTED_EDGE ( 'NONE', *, *, #19272, .T. ) ;
#31181=ORIENTED_EDGE ( 'NONE', *, *, #5456, .F. ) ;
#31184=CARTESIAN_POINT ( 'NONE',  ( 10.00000000000000000, -34.44570377933649041, 69.42325613327427902 ) ) ;
#31191=DIRECTION ( 'NONE',  ( -1.000000000000000000, -0.000000000000000000, -0.000000000000000000 ) ) ;
#31200=CARTESIAN_POINT ( 'NONE',  ( 10.00000000000000000, 0.000000000000000000, 0.000000000000000000 ) ) ;
#31204=DIRECTION ( 'NONE',  ( -1.000000000000000000, 0.000000000000000000, 0.000000000000000000 ) ) ;
#31208=DIRECTION ( 'NONE',  ( 0.000000000000000000, 0.8526401643540897357, 0.5224985647159531288 ) ) ;
#31213=CIRCLE ( 'NONE', #62478, 82.00000000000000000 ) ;
#31214=VECTOR ( 'NONE', #35027, 1000.000000000000000 ) ;
#31215=EDGE_CURVE ( 'NONE', #45970, #57911, #44398, .T. ) ;
#31225=DIRECTION ( 'NONE',  ( -1.000000000000000000, -0.000000000000000000, -0.000000000000000000 ) ) ;
#31227=VERTEX_POINT ( 'NONE', #49758 ) ;
#31234=ORIENTED_EDGE ( 'NONE', *, *, #42684, .T. ) ;
#31241=VECTOR ( 'NONE', #13535, 1000.000000000000000 ) ;
#31244=CARTESIAN_POINT ( 'NONE',  ( 0.000000000000000000, 10.30890764327382847, 81.34940948281339956 ) ) ;
#31259=ORIENTED_EDGE ( 'NONE', *, *, #51550, .T. ) ;
#31269=ORIENTED_EDGE ( 'NONE', *, *, #62510, .T. ) ;
#31274=CARTESIAN_POINT ( 'NONE',  ( 10.00000000000000000, 66.50666863322000211, 39.78640506895629869 ) ) ;
#31275=CARTESIAN_POINT ( 'NONE',  ( 10.00000000000000000, -14.66109333815410487, -73.73191006444587003 ) ) ;
#31292=EDGE_CURVE ( 'NONE', #60557, #45142, #50390, .T. ) ;
#31294=CIRCLE ( 'NONE', #6159, 82.00000000000000000 ) ;
#31303=DIRECTION ( 'NONE',  ( 0.000000000000000000, 0.000000000000000000, 1.000000000000000000 ) ) ;
#31311=DIRECTION ( 'NONE',  ( -1.000000000000000000, 0.000000000000000000, 0.000000000000000000 ) ) ;
#31313=CIRCLE ( 'NONE', #37347, 77.49899999999999523 ) ;
#31314=AXIS2_PLACEMENT_3D ( 'NONE', #44731, #3134, #38711 ) ;
#31315=CARTESIAN_POINT ( 'NONE',  ( 10.00000000000000000, 0.000000000000000000, 0.000000000000000000 ) ) ;
#31319=CARTESIAN_POINT ( 'NONE',  ( 0.000000000000000000, 16.00000000000000000, 2.500000000000000000 ) ) ;
#31331=EDGE_CURVE ( 'NONE', #28882, #65467, #33605, .T. ) ;
#31336=DIRECTION ( 'NONE',  ( -1.000000000000000000, -0.000000000000000000, -0.000000000000000000 ) ) ;
#31340=CIRCLE ( 'NONE', #32521, 82.00000000000000000 ) ;
#31341=VERTEX_POINT ( 'NONE', #72272 ) ;
#31348=FACE_OUTER_BOUND ( 'NONE', #38576, .T. ) ;
#31361=FACE_OUTER_BOUND ( 'NONE', #38289, .T. ) ;
#31362=CARTESIAN_POINT ( 'NONE',  ( 5.000000000000000000, 60.67117009219135326, 55.16347631943062169 ) ) ;
#31368=CIRCLE ( 'NONE', #6178, 77.49899999999999523 ) ;
#31372=CARTESIAN_POINT ( 'NONE',  ( 0.000000000000000000, 0.000000000000000000, 0.000000000000000000 ) ) ;
#31373=CARTESIAN_POINT ( 'NONE',  ( -10.00000000000000000, 0.000000000000000000, 0.000000000000000000 ) ) ;
#31380=CARTESIAN_POINT ( 'NONE',  ( 0.000000000000000000, -0.8261519478425669583, -77.49459641780886443 ) ) ;
#31387=LINE ( 'NONE', #9204, #10964 ) ;
#31389=LINE ( 'NONE', #54338, #8858 ) ;
#31390=CARTESIAN_POINT ( 'NONE',  ( 10.00000000000000000, -20.40083707022935400, 72.35432306680478121 ) ) ;
#31407=CARTESIAN_POINT ( 'NONE',  ( 10.00000000000000000, -20.40083707022829174, -72.35432306680507963 ) ) ;
#31412=VECTOR ( 'NONE', #33489, 1000.000000000000000 ) ;
#31417=VECTOR ( 'NONE', #938, 1000.000000000000000 ) ;
#31418=EDGE_LOOP ( 'NONE', ( #73230, #66321, #55777, #67952 ) ) ;
#31425=DIRECTION ( 'NONE',  ( -1.000000000000000000, 0.000000000000000000, -0.000000000000000000 ) ) ;
#31426=FACE_OUTER_BOUND ( 'NONE', #57434, .T. ) ;
#31433=DIRECTION ( 'NONE',  ( 1.000000000000000000, -0.000000000000000000, -0.000000000000000000 ) ) ;
#31435=CARTESIAN_POINT ( 'NONE',  ( 0.000000000000000000, 3.894527615419058009, -81.90746397400384637 ) ) ;
#31436=LINE ( 'NONE', #53635, #48626 ) ;
#31439=ORIENTED_EDGE ( 'NONE', *, *, #48718, .T. ) ;
#31442=CYLINDRICAL_SURFACE ( 'NONE', #1476, 82.00000000000000000 ) ;
#31449=CARTESIAN_POINT ( 'NONE',  ( 0.000000000000000000, 0.000000000000000000, 0.000000000000000000 ) ) ;
#31453=ORIENTED_EDGE ( 'NONE', *, *, #5534, .F. ) ;
#31463=AXIS2_PLACEMENT_3D ( 'NONE', #1717, #46811, #36253 ) ;
#31467=ORIENTED_EDGE ( 'NONE', *, *, #28793, .F. ) ;
#31478=DIRECTION ( 'NONE',  ( 0.000000000000000000, -0.7604059656000368150, 0.6494480483301767748 ) ) ;
#31484=CYLINDRICAL_SURFACE ( 'NONE', #58862, 31.99999999999999289 ) ;
#31485=DIRECTION ( 'NONE',  ( 0.000000000000000000, -0.4539904997395541875, 0.8910065241883642351 ) ) ;
#31486=ORIENTED_EDGE ( 'NONE', *, *, #14749, .T. ) ;
#31488=DIRECTION ( 'NONE',  ( -1.000000000000000000, 0.000000000000000000, 0.000000000000000000 ) ) ;
#31492=CARTESIAN_POINT ( 'NONE',  ( 0.000000000000000000, -2.543863470248944214, 81.96053171279901051 ) ) ;
#31504=AXIS2_PLACEMENT_3D ( 'NONE', #47642, #19062, #59671 ) ;
#31510=CARTESIAN_POINT ( 'NONE',  ( 10.00000000000000000, 0.000000000000000000, 0.000000000000000000 ) ) ;
#31515=AXIS2_PLACEMENT_3D ( 'NONE', #63587, #73720, #29339 ) ;
#31519=DIRECTION ( 'NONE',  ( 0.000000000000000000, 0.3090169943749482839, -0.9510565162951533091 ) ) ;
#31525=ORIENTED_EDGE ( 'NONE', *, *, #23762, .T. ) ;
#31526=ORIENTED_EDGE ( 'NONE', *, *, #2992, .T. ) ;
#31537=DIRECTION ( 'NONE',  ( 0.000000000000000000, 0.000000000000000000, 1.000000000000000000 ) ) ;
#31541=CARTESIAN_POINT ( 'NONE',  ( 10.00000000000000000, -26.02418014898359289, 70.52718814184250107 ) ) ;
#31543=VERTEX_POINT ( 'NONE', #34648 ) ;
#31547=CARTESIAN_POINT ( 'NONE',  ( 10.00000000000000000, -55.20638768913724448, -51.02545421589383068 ) ) ;
#31554=AXIS2_PLACEMENT_3D ( 'NONE', #7684, #48649, #8435 ) ;
#31572=DIRECTION ( 'NONE',  ( 0.000000000000000000, 0.000000000000000000, 1.000000000000000000 ) ) ;
#31573=AXIS2_PLACEMENT_3D ( 'NONE', #24371, #69852, #41294 ) ;
#31574=CYLINDRICAL_SURFACE ( 'NONE', #25075, 31.99999999999999289 ) ;
#31581=CYLINDRICAL_SURFACE ( 'NONE', #29920, 31.99999999999999289 ) ;
#31584=LINE ( 'NONE', #59434, #64160 ) ;
#31602=ORIENTED_EDGE ( 'NONE', *, *, #65911, .F. ) ;
#31603=ORIENTED_EDGE ( 'NONE', *, *, #43251, .F. ) ;
#31621=VECTOR ( 'NONE', #49683, 1000.000000000000000 ) ;
#31626=DIRECTION ( 'NONE',  ( -1.000000000000000000, -0.000000000000000000, -0.000000000000000000 ) ) ;
#31628=ADVANCED_FACE ( 'NONE', ( #24480 ), #70320, .T. ) ;
#31647=ORIENTED_EDGE ( 'NONE', *, *, #44257, .F. ) ;
#31655=CARTESIAN_POINT ( 'NONE',  ( 10.00000000000000000, 0.000000000000000000, 0.000000000000000000 ) ) ;
#31657=ADVANCED_FACE ( 'NONE', ( #43552 ), #30476, .T. ) ;
#31658=ORIENTED_EDGE ( 'NONE', *, *, #35712, .T. ) ;
#31665=CARTESIAN_POINT ( 'NONE',  ( 10.00000000000000000, 0.000000000000000000, 0.000000000000000000 ) ) ;
#31668=EDGE_CURVE ( 'NONE', #17876, #50235, #9093, .T. ) ;
#31669=CARTESIAN_POINT ( 'NONE',  ( 0.000000000000000000, 0.000000000000000000, 0.000000000000000000 ) ) ;
#31684=ORIENTED_EDGE ( 'NONE', *, *, #35099, .T. ) ;
#31686=CARTESIAN_POINT ( 'NONE',  ( 10.00000000000000000, 59.46389618801964616, 49.70050353004912580 ) ) ;
#31689=ORIENTED_EDGE ( 'NONE', *, *, #24306, .F. ) ;
#31699=ORIENTED_EDGE ( 'NONE', *, *, #15515, .F. ) ;
#31709=AXIS2_PLACEMENT_3D ( 'NONE', #38373, #21429, #3080 ) ;
#31714=CARTESIAN_POINT ( 'NONE',  ( 0.000000000000000000, 0.000000000000000000, 0.000000000000000000 ) ) ;
#31715=EDGE_CURVE ( 'NONE', #1727, #1450, #60737, .T. ) ;
#31717=DIRECTION ( 'NONE',  ( -1.000000000000000000, 0.000000000000000000, 0.000000000000000000 ) ) ;
#31732=CARTESIAN_POINT ( 'NONE',  ( -10.00000000000000000, 0.000000000000000000, 0.000000000000000000 ) ) ;
#31753=DIRECTION ( 'NONE',  ( -1.000000000000000000, -0.000000000000000000, 0.000000000000000000 ) ) ;
#31758=CARTESIAN_POINT ( 'NONE',  ( 0.000000000000000000, 0.000000000000000000, 0.000000000000000000 ) ) ;
#31760=EDGE_CURVE ( 'NONE', #5511, #58272, #49918, .T. ) ;
#31770=ORIENTED_EDGE ( 'NONE', *, *, #74103, .F. ) ;
#31772=VERTEX_POINT ( 'NONE', #310 ) ;
#31776=VERTEX_POINT ( 'NONE', #5181 ) ;
#31791=ORIENTED_EDGE ( 'NONE', *, *, #15651, .F. ) ;
#31793=ORIENTED_EDGE ( 'NONE', *, *, #43736, .F. ) ;
#31803=ORIENTED_EDGE ( 'NONE', *, *, #69333, .T. ) ;
#31812=CARTESIAN_POINT ( 'NONE',  ( 10.00000000000000000, -55.38113227695743745, -54.21277698773734244 ) ) ;
#31820=AXIS2_PLACEMENT_3D ( 'NONE', #20149, #2908, #43851 ) ;
#31826=DIRECTION ( 'NONE',  ( -1.000000000000000000, 0.000000000000000000, 0.000000000000000000 ) ) ;
#31831=EDGE_CURVE ( 'NONE', #61902, #56093, #17916, .T. ) ;
#31839=DIRECTION ( 'NONE',  ( 0.000000000000000000, 0.000000000000000000, 1.000000000000000000 ) ) ;
#31874=CIRCLE ( 'NONE', #64322, 77.49899999999999523 ) ;
#31879=CARTESIAN_POINT ( 'NONE',  ( 10.00000000000000000, -73.72996012237449293, 14.67089635893687571 ) ) ;
#31894=EDGE_CURVE ( 'NONE', #54114, #23922, #52878, .T. ) ;
#31900=AXIS2_PLACEMENT_3D ( 'NONE', #45919, #27104, #28598 ) ;
#31912=ORIENTED_EDGE ( 'NONE', *, *, #43550, .T. ) ;
#31914=EDGE_CURVE ( 'NONE', #64387, #49393, #56185, .T. ) ;
#31918=ORIENTED_EDGE ( 'NONE', *, *, #45505, .T. ) ;
#31927=ADVANCED_FACE ( 'NONE', ( #1783 ), #7001, .T. ) ;
#31928=ADVANCED_FACE ( 'NONE', ( #58890 ), #19017, .T. ) ;
#31934=CARTESIAN_POINT ( 'NONE',  ( 0.000000000000000000, 0.000000000000000000, 0.000000000000000000 ) ) ;
#31939=CARTESIAN_POINT ( 'NONE',  ( 10.00000000000000000, -75.11764819372145041, 29.05362095685286761 ) ) ;
#31946=AXIS2_PLACEMENT_3D ( 'NONE', #73826, #15205, #38888 ) ;
#31954=FACE_OUTER_BOUND ( 'NONE', #17843, .T. ) ;
#31959=DIRECTION ( 'NONE',  ( 0.000000000000000000, 0.000000000000000000, 1.000000000000000000 ) ) ;
#31973=DIRECTION ( 'NONE',  ( -1.000000000000000000, 0.000000000000000000, -0.000000000000000000 ) ) ;
#31985=EDGE_CURVE ( 'NONE', #19363, #31543, #37143, .T. ) ;
#31986=ORIENTED_EDGE ( 'NONE', *, *, #48740, .F. ) ;
#31993=VERTEX_POINT ( 'NONE', #35943 ) ;
#32007=CARTESIAN_POINT ( 'NONE',  ( 0.000000000000000000, 74.65374052328648702, 8.840884882375350529 ) ) ;
#32008=DIRECTION ( 'NONE',  ( -1.000000000000000000, -0.000000000000000000, 0.000000000000000000 ) ) ;
#32009=CYLINDRICAL_SURFACE ( 'NONE', #48896, 31.99999999999999289 ) ;
#32021=DIRECTION ( 'NONE',  ( -1.000000000000000000, 0.000000000000000000, 0.000000000000000000 ) ) ;
#32024=CARTESIAN_POINT ( 'NONE',  ( 0.000000000000000000, 8.840884882376133902, -74.65374052328640175 ) ) ;
#32030=DIRECTION ( 'NONE',  ( -1.000000000000000000, 0.000000000000000000, 0.000000000000000000 ) ) ;
#32036=CARTESIAN_POINT ( 'NONE',  ( 0.000000000000000000, 0.000000000000000000, 0.000000000000000000 ) ) ;
#32045=CIRCLE ( 'NONE', #68075, 31.99999999999999289 ) ;
#32050=AXIS2_PLACEMENT_3D ( 'NONE', #42774, #64976, #70574 ) ;
#32052=VERTEX_POINT ( 'NONE', #43831 ) ;
#32054=DIRECTION ( 'NONE',  ( -1.000000000000000000, 0.000000000000000000, 0.000000000000000000 ) ) ;
#32060=CIRCLE ( 'NONE', #53656, 82.00000000000000000 ) ;
#32073=DIRECTION ( 'NONE',  ( -1.000000000000000000, -0.000000000000000000, 0.000000000000000000 ) ) ;
#32076=ORIENTED_EDGE ( 'NONE', *, *, #23583, .T. ) ;
#32081=DIRECTION ( 'NONE',  ( 0.000000000000000000, 0.000000000000000000, 1.000000000000000000 ) ) ;
#32084=DIRECTION ( 'NONE',  ( -1.000000000000000000, -0.000000000000000000, -0.000000000000000000 ) ) ;
#32086=FACE_OUTER_BOUND ( 'NONE', #34753, .T. ) ;
#32090=ADVANCED_FACE ( 'NONE', ( #70892 ), #49078, .T. ) ;
#32091=ORIENTED_EDGE ( 'NONE', *, *, #2331, .F. ) ;
#32112=CARTESIAN_POINT ( 'NONE',  ( 0.000000000000000000, 46.53671651294032330, -59.03961581697353012 ) ) ;
#32113=CARTESIAN_POINT ( 'NONE',  ( 0.000000000000000000, 73.72996012237460661, -14.67089635893632504 ) ) ;
#32119=LINE ( 'NONE', #61079, #58512 ) ;
#32123=CARTESIAN_POINT ( 'NONE',  ( 10.00000000000000000, 76.66974797899837313, 11.30684508768368524 ) ) ;
#32124=AXIS2_PLACEMENT_3D ( 'NONE', #4468, #15731, #54462 ) ;
#32125=EDGE_CURVE ( 'NONE', #22556, #64812, #58588, .T. ) ;
#32132=DIRECTION ( 'NONE',  ( -1.000000000000000000, -0.000000000000000000, -0.000000000000000000 ) ) ;
#32140=VERTEX_POINT ( 'NONE', #38548 ) ;
#32165=DIRECTION ( 'NONE',  ( -1.000000000000000000, 0.000000000000000000, -0.000000000000000000 ) ) ;
#32166=CARTESIAN_POINT ( 'NONE',  ( 10.00000000000000000, -49.70050353004933896, 59.46389618801946852 ) ) ;
#32185=CARTESIAN_POINT ( 'NONE',  ( 10.00000000000000000, -65.64334221924882229, -41.19522573413803457 ) ) ;
#32197=DIRECTION ( 'NONE',  ( 0.000000000000000000, 0.000000000000000000, 1.000000000000000000 ) ) ;
#32205=CIRCLE ( 'NONE', #9398, 32.00000000000000000 ) ;
#32208=DIRECTION ( 'NONE',  ( -1.000000000000000000, 0.000000000000000000, -0.000000000000000000 ) ) ;
#32219=AXIS2_PLACEMENT_3D ( 'NONE', #5741, #69970, #28642 ) ;
#32220=VECTOR ( 'NONE', #48140, 1000.000000000000000 ) ;
#32228=DIRECTION ( 'NONE',  ( -1.000000000000000000, -0.000000000000000000, -0.000000000000000000 ) ) ;
#32235=CARTESIAN_POINT ( 'NONE',  ( 0.000000000000000000, -31.46837873494930093, -68.27212725128309501 ) ) ;
#32245=ORIENTED_EDGE ( 'NONE', *, *, #72952, .T. ) ;
#32252=VECTOR ( 'NONE', #25224, 1000.000000000000000 ) ;
#32261=ORIENTED_EDGE ( 'NONE', *, *, #17546, .F. ) ;
#32270=CARTESIAN_POINT ( 'NONE',  ( 0.000000000000000000, 5.256550761633969060, -77.32052557432835727 ) ) ;
#32279=LINE ( 'NONE', #55221, #1212 ) ;
#32293=CARTESIAN_POINT ( 'NONE',  ( 0.000000000000000000, -74.65491531819111515, -8.830959090343204920 ) ) ;
#32317=EDGE_CURVE ( 'NONE', #59483, #26699, #41144, .T. ) ;
#32321=CARTESIAN_POINT ( 'NONE',  ( 10.00000000000000000, 29.01471420065564644, 76.69515212746024702 ) ) ;
#32324=VECTOR ( 'NONE', #49854, 1000.000000000000000 ) ;
#32327=VERTEX_POINT ( 'NONE', #68974 ) ;
#32330=CYLINDRICAL_SURFACE ( 'NONE', #67993, 77.49899999999999523 ) ;
#32338=LINE ( 'NONE', #55283, #31041 ) ;
#32341=EDGE_CURVE ( 'NONE', #5845, #54097, #56234, .T. ) ;
#32358=VERTEX_POINT ( 'NONE', #46786 ) ;
#32364=VERTEX_POINT ( 'NONE', #64081 ) ;
#32368=LINE ( 'NONE', #3460, #11906 ) ;
#32386=ORIENTED_EDGE ( 'NONE', *, *, #42339, .T. ) ;
#32397=LINE ( 'NONE', #9107, #60468 ) ;
#32406=VECTOR ( 'NONE', #43409, 1000.000000000000000 ) ;
#32418=EDGE_CURVE ( 'NONE', #52788, #69505, #18975, .T. ) ;
#32419=VERTEX_POINT ( 'NONE', #46047 ) ;
#32428=AXIS2_PLACEMENT_3D ( 'NONE', #48937, #19264, #2764 ) ;
#32436=ORIENTED_EDGE ( 'NONE', *, *, #64614, .T. ) ;
#32437=ORIENTED_EDGE ( 'NONE', *, *, #7982, .T. ) ;
#32438=AXIS2_PLACEMENT_3D ( 'NONE', #4930, #51136, #74061 ) ;
#32443=VERTEX_POINT ( 'NONE', #43378 ) ;
#32446=CARTESIAN_POINT ( 'NONE',  ( 10.00000000000000000, 0.000000000000000000, 0.000000000000000000 ) ) ;
#32466=CARTESIAN_POINT ( 'NONE',  ( 10.00000000000000000, -68.67312586195023982, 35.91791733033450384 ) ) ;
#32470=DIRECTION ( 'NONE',  ( 0.000000000000000000, 0.000000000000000000, 1.000000000000000000 ) ) ;
#32507=CARTESIAN_POINT ( 'NONE',  ( 10.00000000000000000, 26.01480285779837232, 70.53064760720326376 ) ) ;
#32514=EDGE_CURVE ( 'NONE', #31776, #64448, #3527, .T. ) ;
#32516=EDGE_CURVE ( 'NONE', #9438, #26686, #20205, .T. ) ;
#32520=VECTOR ( 'NONE', #32208, 1000.000000000000000 ) ;
#32521=AXIS2_PLACEMENT_3D ( 'NONE', #62170, #10655, #73433 ) ;
#32524=ORIENTED_EDGE ( 'NONE', *, *, #14749, .F. ) ;
#32529=DIRECTION ( 'NONE',  ( 0.000000000000000000, 0.000000000000000000, 1.000000000000000000 ) ) ;
#32537=ORIENTED_EDGE ( 'NONE', *, *, #38320, .T. ) ;
#32549=DIRECTION ( 'NONE',  ( 0.000000000000000000, 0.000000000000000000, 1.000000000000000000 ) ) ;
#32552=AXIS2_PLACEMENT_3D ( 'NONE', #66184, #49245, #49606 ) ;
#32553=VERTEX_POINT ( 'NONE', #49358 ) ;
#32556=DIRECTION ( 'NONE',  ( -1.000000000000000000, -0.000000000000000000, 0.000000000000000000 ) ) ;
#32566=EDGE_CURVE ( 'NONE', #53902, #20797, #10602, .T. ) ;
#32567=ADVANCED_FACE ( 'NONE', ( #36229 ), #48257, .T. ) ;
#32574=ORIENTED_EDGE ( 'NONE', *, *, #53831, .T. ) ;
#32588=DIRECTION ( 'NONE',  ( 0.000000000000000000, 0.000000000000000000, 1.000000000000000000 ) ) ;
#32599=DIRECTION ( 'NONE',  ( 0.000000000000000000, 0.8090169943749487835, -0.5877852522924712497 ) ) ;
#32613=CARTESIAN_POINT ( 'NONE',  ( 10.00000000000000000, -69.42325613327415113, -34.44570377933673910 ) ) ;
#32615=DIRECTION ( 'NONE',  ( 1.000000000000000000, -0.000000000000000000, 0.000000000000000000 ) ) ;
#32622=VERTEX_POINT ( 'NONE', #56501 ) ;
#32623=CARTESIAN_POINT ( 'NONE',  ( 10.00000000000000000, -2.946379043145784582, -75.11764819372150725 ) ) ;
#32624=AXIS2_PLACEMENT_3D ( 'NONE', #60534, #36109, #7541 ) ;
#32631=VERTEX_POINT ( 'NONE', #10616 ) ;
#32641=DIRECTION ( 'NONE',  ( 0.000000000000000000, 0.5224985647159500202, -0.8526401643540915121 ) ) ;
#32643=CARTESIAN_POINT ( 'NONE',  ( 10.00000000000000000, 0.000000000000000000, 0.000000000000000000 ) ) ;
#32647=AXIS2_PLACEMENT_3D ( 'NONE', #46437, #47548, #30247 ) ;
#32648=ORIENTED_EDGE ( 'NONE', *, *, #25291, .T. ) ;
#32649=ORIENTED_EDGE ( 'NONE', *, *, #54582, .F. ) ;
#32660=CARTESIAN_POINT ( 'NONE',  ( 10.00000000000000000, 0.000000000000000000, 0.000000000000000000 ) ) ;
#32662=CARTESIAN_POINT ( 'NONE',  ( 0.000000000000000000, -26.02418014898359289, 70.52718814184250107 ) ) ;
#32668=DIRECTION ( 'NONE',  ( -1.000000000000000000, 0.000000000000000000, 0.000000000000000000 ) ) ;
#32669=DIRECTION ( 'NONE',  ( 1.000000000000000000, 0.000000000000000000, 0.000000000000000000 ) ) ;
#32675=ADVANCED_FACE ( 'NONE', ( #67016 ), #38080, .T. ) ;
#32676=DIRECTION ( 'NONE',  ( -1.000000000000000000, 0.000000000000000000, 0.000000000000000000 ) ) ;
#32687=DIRECTION ( 'NONE',  ( -1.000000000000000000, 0.000000000000000000, 0.000000000000000000 ) ) ;
#32689=CARTESIAN_POINT ( 'NONE',  ( 10.00000000000000000, 0.000000000000000000, 0.000000000000000000 ) ) ;
#32691=CIRCLE ( 'NONE', #356, 82.00000000000000000 ) ;
#32706=ORIENTED_EDGE ( 'NONE', *, *, #66406, .F. ) ;
#32711=CARTESIAN_POINT ( 'NONE',  ( 10.00000000000000000, 0.000000000000000000, 0.000000000000000000 ) ) ;
#32719=VERTEX_POINT ( 'NONE', #33543 ) ;
#32721=DIRECTION ( 'NONE',  ( -1.000000000000000000, 0.000000000000000000, 0.000000000000000000 ) ) ;
#32726=AXIS2_PLACEMENT_3D ( 'NONE', #27629, #23474, #56203 ) ;
#32729=CARTESIAN_POINT ( 'NONE',  ( 10.00000000000000000, 62.50884508063487033, -41.76106447765422303 ) ) ;
#32741=DIRECTION ( 'NONE',  ( -1.000000000000000000, -0.000000000000000000, 0.000000000000000000 ) ) ;
#32758=CARTESIAN_POINT ( 'NONE',  ( 0.000000000000000000, 0.000000000000000000, 0.000000000000000000 ) ) ;
#32759=EDGE_CURVE ( 'NONE', #59559, #37734, #5855, .T. ) ;
#32763=EDGE_CURVE ( 'NONE', #56683, #32364, #73064, .T. ) ;
#32764=DIRECTION ( 'NONE',  ( -1.000000000000000000, 0.000000000000000000, 0.000000000000000000 ) ) ;
#32779=DIRECTION ( 'NONE',  ( -1.000000000000000000, 0.000000000000000000, -0.000000000000000000 ) ) ;
#32785=FILL_AREA_STYLE ('',( #27142 ) ) ;
#32786=ORIENTED_EDGE ( 'NONE', *, *, #10127, .F. ) ;
#32787=VECTOR ( 'NONE', #36694, 1000.000000000000000 ) ;
#32793=VERTEX_POINT ( 'NONE', #41056 ) ;
#32797=VECTOR ( 'NONE', #33507, 1000.000000000000000 ) ;
#32798=DIRECTION ( 'NONE',  ( -1.000000000000000000, 0.000000000000000000, 0.000000000000000000 ) ) ;
#32806=LINE ( 'NONE', #73404, #44368 ) ;
#32820=DIRECTION ( 'NONE',  ( 0.000000000000000000, 0.000000000000000000, 1.000000000000000000 ) ) ;
#32822=EDGE_CURVE ( 'NONE', #19761, #57988, #12830, .T. ) ;
#32831=ORIENTED_EDGE ( 'NONE', *, *, #39291, .T. ) ;
#32842=AXIS2_PLACEMENT_3D ( 'NONE', #3986, #10726, #32529 ) ;
#32848=DIRECTION ( 'NONE',  ( -1.000000000000000000, -0.000000000000000000, -0.000000000000000000 ) ) ;
#32859=ADVANCED_FACE ( 'NONE', ( #63253 ), #11714, .T. ) ;
#32865=DIRECTION ( 'NONE',  ( 0.000000000000000000, 0.000000000000000000, 1.000000000000000000 ) ) ;
#32868=AXIS2_PLACEMENT_3D ( 'NONE', #42552, #61241, #48556 ) ;
#32877=VECTOR ( 'NONE', #12327, 1000.000000000000000 ) ;
#32886=ORIENTED_EDGE ( 'NONE', *, *, #16519, .T. ) ;
#32888=CARTESIAN_POINT ( 'NONE',  ( 10.00000000000000000, 0.000000000000000000, 2.500000000000000000 ) ) ;
#32893=VECTOR ( 'NONE', #48330, 1000.000000000000000 ) ;
#32904=ADVANCED_FACE ( 'NONE', ( #47787 ), #48530, .T. ) ;
#32908=CARTESIAN_POINT ( 'NONE',  ( 0.000000000000000000, -60.67117009219176538, 55.16347631943019536 ) ) ;
#32914=CIRCLE ( 'NONE', #564, 82.00000000000000000 ) ;
#32923=FACE_OUTER_BOUND ( 'NONE', #131, .T. ) ;
#32951=DIRECTION ( 'NONE',  ( -1.000000000000000000, -0.000000000000000000, 0.000000000000000000 ) ) ;
#32969=LINE ( 'NONE', #50639, #36676 ) ;
#32979=DIRECTION ( 'NONE',  ( 0.000000000000000000, 0.000000000000000000, 1.000000000000000000 ) ) ;
#32981=EDGE_CURVE ( 'NONE', #34710, #21157, #15427, .T. ) ;
#32989=DIRECTION ( 'NONE',  ( -1.000000000000000000, 0.000000000000000000, -0.000000000000000000 ) ) ;
#32993=VECTOR ( 'NONE', #72393, 1000.000000000000000 ) ;
#32996=LINE ( 'NONE', #9708, #68942 ) ;
#33002=DIRECTION ( 'NONE',  ( 0.000000000000000000, 0.000000000000000000, -1.000000000000000000 ) ) ;
#33015=DIRECTION ( 'NONE',  ( -1.000000000000000000, 0.000000000000000000, 0.000000000000000000 ) ) ;
#33017=CARTESIAN_POINT ( 'NONE',  ( 10.00000000000000000, 11.30684508768452545, -76.66974797899825944 ) ) ;
#33023=ADVANCED_FACE ( 'NONE', ( #22188 ), #44009, .T. ) ;
#33026=DIRECTION ( 'NONE',  ( 0.000000000000000000, 0.6494480483301848794, -0.7604059656000299317 ) ) ;
#33037=CIRCLE ( 'NONE', #70219, 31.99999999999999645 ) ;
#33056=CARTESIAN_POINT ( 'NONE',  ( 10.00000000000000000, 62.50329211542494789, -41.76937507738723099 ) ) ;
#33069=DIRECTION ( 'NONE',  ( -1.000000000000000000, -0.000000000000000000, 0.000000000000000000 ) ) ;
#33070=ORIENTED_EDGE ( 'NONE', *, *, #52602, .T. ) ;
#33074=ORIENTED_EDGE ( 'NONE', *, *, #43975, .T. ) ;
#33078=EDGE_CURVE ( 'NONE', #72957, #17127, #49997, .T. ) ;
#33080=DIRECTION ( 'NONE',  ( -1.000000000000000000, 0.000000000000000000, -0.000000000000000000 ) ) ;
#33081=ORIENTED_EDGE ( 'NONE', *, *, #72815, .F. ) ;
#33084=ORIENTED_EDGE ( 'NONE', *, *, #6972, .T. ) ;
#33090=CARTESIAN_POINT ( 'NONE',  ( 10.00000000000000000, -31.46837873494930093, -68.27212725128309501 ) ) ;
#33095=VERTEX_POINT ( 'NONE', #62433 ) ;
#33112=VERTEX_POINT ( 'NONE', #44380 ) ;
#33113=EDGE_CURVE ( 'NONE', #37924, #21174, #32338, .T. ) ;
#33116=DIRECTION ( 'NONE',  ( 0.000000000000000000, 0.000000000000000000, 1.000000000000000000 ) ) ;
#33120=DIRECTION ( 'NONE',  ( -1.000000000000000000, 0.000000000000000000, -0.000000000000000000 ) ) ;
#33121=AXIS2_PLACEMENT_3D ( 'NONE', #41898, #48278, #24601 ) ;
#33134=AXIS2_PLACEMENT_3D ( 'NONE', #28977, #63947, #29335 ) ;
#33139=CARTESIAN_POINT ( 'NONE',  ( 10.00000000000000000, 6.903761155838878061, -77.19088730480517313 ) ) ;
#33142=CARTESIAN_POINT ( 'NONE',  ( 0.000000000000000000, 51.02545421589324803, 55.20638768913779870 ) ) ;
#33145=EDGE_CURVE ( 'NONE', #61936, #16380, #50260, .T. ) ;
#33157=ORIENTED_EDGE ( 'NONE', *, *, #3907, .F. ) ;
#33160=ORIENTED_EDGE ( 'NONE', *, *, #72729, .T. ) ;
#33163=AXIS2_PLACEMENT_3D ( 'NONE', #50032, #67717, #4580 ) ;
#33165=CARTESIAN_POINT ( 'NONE',  ( 10.00000000000000000, 65.64334221924966073, -41.19522573413664190 ) ) ;
#33166=ADVANCED_FACE ( 'NONE', ( #40219 ), #40968, .T. ) ;
#33167=ORIENTED_EDGE ( 'NONE', *, *, #40011, .F. ) ;
#33173=CIRCLE ( 'NONE', #39206, 82.00000000000000000 ) ;
#33182=CARTESIAN_POINT ( 'NONE',  ( 5.000000000000002665, 29.01471420065564644, 76.69515212746026123 ) ) ;
#33187=EDGE_LOOP ( 'NONE', ( #3424, #30477, #48445, #42001 ) ) ;
#33194=DIRECTION ( 'NONE',  ( 0.000000000000000000, 0.5877852522924743583, -0.8090169943749466741 ) ) ;
#33198=FACE_OUTER_BOUND ( 'NONE', #17125, .T. ) ;
#33202=ORIENTED_EDGE ( 'NONE', *, *, #27744, .F. ) ;
#33205=ORIENTED_EDGE ( 'NONE', *, *, #664, .T. ) ;
#33211=LINE ( 'NONE', #34333, #5480 ) ;
#33212=LINE ( 'NONE', #27584, #37406 ) ;
#33213=DIRECTION ( 'NONE',  ( 0.000000000000000000, 0.000000000000000000, 1.000000000000000000 ) ) ;
#33215=CIRCLE ( 'NONE', #71629, 32.00000000000000000 ) ;
#33223=CYLINDRICAL_SURFACE ( 'NONE', #49220, 31.99999999999998579 ) ;
#33225=ORIENTED_EDGE ( 'NONE', *, *, #72806, .T. ) ;
#33230=DIRECTION ( 'NONE',  ( 0.000000000000000000, 0.9510565162951544194, -0.3090169943749446757 ) ) ;
#33235=VECTOR ( 'NONE', #1934, 1000.000000000000000 ) ;
#33252=EDGE_CURVE ( 'NONE', #36430, #21993, #777, .T. ) ;
#33253=DIRECTION ( 'NONE',  ( -1.000000000000000000, 0.000000000000000000, 0.000000000000000000 ) ) ;
#33259=DIRECTION ( 'NONE',  ( -1.000000000000000000, -0.000000000000000000, 0.000000000000000000 ) ) ;
#33260=ORIENTED_EDGE ( 'NONE', *, *, #52344, .T. ) ;
#33270=ORIENTED_EDGE ( 'NONE', *, *, #8818, .F. ) ;
#33282=ORIENTED_EDGE ( 'NONE', *, *, #15871, .T. ) ;
#33290=EDGE_LOOP ( 'NONE', ( #46779, #65233, #43568, #30299 ) ) ;
#33293=DIRECTION ( 'NONE',  ( 0.000000000000000000, 0.000000000000000000, 1.000000000000000000 ) ) ;
#33303=CARTESIAN_POINT ( 'NONE',  ( 0.000000000000000000, 36.72794159290241822, 65.59268652807223532 ) ) ;
#33307=ORIENTED_EDGE ( 'NONE', *, *, #19345, .F. ) ;
#33310=DIRECTION ( 'NONE',  ( -1.000000000000000000, -0.000000000000000000, -0.000000000000000000 ) ) ;
#33315=CARTESIAN_POINT ( 'NONE',  ( 10.00000000000000000, 71.27951684758069462, -30.41916302227035729 ) ) ;
#33320=AXIS2_PLACEMENT_3D ( 'NONE', #32623, #10441, #22477 ) ;
#33321=CARTESIAN_POINT ( 'NONE',  ( 10.00000000000000000, 75.16055320797059380, -18.89407956138177269 ) ) ;
#33325=CARTESIAN_POINT ( 'NONE',  ( 10.00000000000000000, -81.90746397400386059, -3.894527615418773347 ) ) ;
#33326=ORIENTED_EDGE ( 'NONE', *, *, #13419, .F. ) ;
#33338=EDGE_CURVE ( 'NONE', #13514, #57170, #71940, .T. ) ;
#33345=VECTOR ( 'NONE', #69063, 1000.000000000000000 ) ;
#33348=ADVANCED_FACE ( 'NONE', ( #70243 ), #13843, .T. ) ;
#33353=FACE_OUTER_BOUND ( 'NONE', #16155, .T. ) ;
#33354=CARTESIAN_POINT ( 'NONE',  ( 10.00000000000000000, -55.38113227695743745, -54.21277698773734244 ) ) ;
#33362=EDGE_CURVE ( 'NONE', #1463, #7305, #25507, .T. ) ;
#33364=ORIENTED_EDGE ( 'NONE', *, *, #72728, .F. ) ;
#33380=DIRECTION ( 'NONE',  ( 0.000000000000000000, 0.000000000000000000, 1.000000000000000000 ) ) ;
#33383=EDGE_LOOP ( 'NONE', ( #38366, #73615, #33558, #34125 ) ) ;
#33384=CARTESIAN_POINT ( 'NONE',  ( 10.00000000000000000, -18.89407956138310496, 75.16055320797023853 ) ) ;
#33411=EDGE_CURVE ( 'NONE', #73705, #16368, #28696, .T. ) ;
#33412=CARTESIAN_POINT ( 'NONE',  ( 10.00000000000000178, 1.530808498934191521E-15, -12.50000000000000000 ) ) ;
#33424=EDGE_CURVE ( 'NONE', #57988, #40784, #55155, .T. ) ;
#33429=DIRECTION ( 'NONE',  ( -1.000000000000000000, 0.000000000000000000, -0.000000000000000000 ) ) ;
#33436=VECTOR ( 'NONE', #32687, 1000.000000000000000 ) ;
#33437=ORIENTED_EDGE ( 'NONE', *, *, #32125, .F. ) ;
#33442=VERTEX_POINT ( 'NONE', #13489 ) ;
#33460=CARTESIAN_POINT ( 'NONE',  ( -10.00000000000000000, 0.000000000000000000, 0.000000000000000000 ) ) ;
#33463=FACE_OUTER_BOUND ( 'NONE', #65980, .T. ) ;
#33464=VERTEX_POINT ( 'NONE', #48077 ) ;
#33470=ORIENTED_EDGE ( 'NONE', *, *, #1905, .T. ) ;
#33471=ORIENTED_EDGE ( 'NONE', *, *, #875, .T. ) ;
#33474=DIRECTION ( 'NONE',  ( 0.000000000000000000, -0.7071067811865389130, -0.7071067811865561215 ) ) ;
#33485=CARTESIAN_POINT ( 'NONE',  ( -10.00000000000000000, 0.000000000000000000, 0.000000000000000000 ) ) ;
#33487=CIRCLE ( 'NONE', #41935, 31.99999999999999645 ) ;
#33488=CIRCLE ( 'NONE', #9455, 31.99999999999999645 ) ;
#33489=DIRECTION ( 'NONE',  ( 1.000000000000000000, -0.000000000000000000, -0.000000000000000000 ) ) ;
#33505=EDGE_CURVE ( 'NONE', #32793, #41146, #9479, .T. ) ;
#33507=DIRECTION ( 'NONE',  ( -1.000000000000000000, 0.000000000000000000, 0.000000000000000000 ) ) ;
#33510=CIRCLE ( 'NONE', #15542, 31.99999999999999289 ) ;
#33511=DIRECTION ( 'NONE',  ( 0.000000000000000000, 0.07845909572783797692, 0.9969173337331285190 ) ) ;
#33517=VERTEX_POINT ( 'NONE', #61215 ) ;
#33522=EDGE_LOOP ( 'NONE', ( #20910, #59300, #60202, #54208 ) ) ;
#33530=EDGE_CURVE ( 'NONE', #43637, #66703, #61116, .T. ) ;
#33538=AXIS2_PLACEMENT_3D ( 'NONE', #10622, #67397, #33550 ) ;
#33539=VECTOR ( 'NONE', #31488, 1000.000000000000000 ) ;
#33542=ORIENTED_EDGE ( 'NONE', *, *, #20041, .T. ) ;
#33543=CARTESIAN_POINT ( 'NONE',  ( 10.00000000000000000, 27.74655509720778568, -77.16300072079631889 ) ) ;
#33548=AXIS2_PLACEMENT_3D ( 'NONE', #12058, #44528, #5059 ) ;
#33550=DIRECTION ( 'NONE',  ( 0.000000000000000000, 0.000000000000000000, 1.000000000000000000 ) ) ;
#33552=ORIENTED_EDGE ( 'NONE', *, *, #43079, .T. ) ;
#33554=CYLINDRICAL_SURFACE ( 'NONE', #66013, 32.00000000000000000 ) ;
#33558=ORIENTED_EDGE ( 'NONE', *, *, #63614, .T. ) ;
#33561=ORIENTED_EDGE ( 'NONE', *, *, #30371, .F. ) ;
#33564=AXIS2_PLACEMENT_3D ( 'NONE', #23163, #271, #16024 ) ;
#33571=AXIS2_PLACEMENT_3D ( 'NONE', #39957, #62912, #27921 ) ;
#33588=CARTESIAN_POINT ( 'NONE',  ( 10.00000000000000000, 0.000000000000000000, 0.000000000000000000 ) ) ;
#33591=VERTEX_POINT ( 'NONE', #50284 ) ;
#33600=FACE_OUTER_BOUND ( 'NONE', #65943, .T. ) ;
#33605=CIRCLE ( 'NONE', #57608, 31.99999999999999289 ) ;
#33611=CARTESIAN_POINT ( 'NONE',  ( 0.000000000000000000, 0.000000000000000000, 0.000000000000000000 ) ) ;
#33616=EDGE_CURVE ( 'NONE', #3606, #16264, #34711, .T. ) ;
#33617=EDGE_CURVE ( 'NONE', #68833, #68809, #23930, .T. ) ;
#33621=FACE_OUTER_BOUND ( 'NONE', #60494, .T. ) ;
#33627=AXIS2_PLACEMENT_3D ( 'NONE', #17035, #17764, #11024 ) ;
#33634=EDGE_CURVE ( 'NONE', #808, #10842, #53930, .T. ) ;
#33643=ORIENTED_EDGE ( 'NONE', *, *, #41769, .T. ) ;
#33646=VERTEX_POINT ( 'NONE', #58814 ) ;
#33681=ORIENTED_EDGE ( 'NONE', *, *, #22227, .T. ) ;
#33686=ORIENTED_EDGE ( 'NONE', *, *, #55487, .F. ) ;
#33693=DIRECTION ( 'NONE',  ( 0.000000000000000000, 0.000000000000000000, 1.000000000000000000 ) ) ;
#33698=VERTEX_POINT ( 'NONE', #1706 ) ;
#33706=DIRECTION ( 'NONE',  ( 0.000000000000000000, 0.000000000000000000, 1.000000000000000000 ) ) ;
#33707=DIRECTION ( 'NONE',  ( 0.000000000000000000, -0.5877852522924625900, -0.8090169943749551118 ) ) ;
#33708=CYLINDRICAL_SURFACE ( 'NONE', #7625, 82.00000000000000000 ) ;
#33709=DIRECTION ( 'NONE',  ( -1.000000000000000000, 0.000000000000000000, 0.000000000000000000 ) ) ;
#33711=CARTESIAN_POINT ( 'NONE',  ( 10.00000000000000000, -75.54627589209955829, 17.28742895386058009 ) ) ;
#33713=DIRECTION ( 'NONE',  ( -1.000000000000000000, -0.000000000000000000, 0.000000000000000000 ) ) ;
#33721=AXIS2_PLACEMENT_3D ( 'NONE', #32113, #59595, #48307 ) ;
#33737=CIRCLE ( 'NONE', #31314, 31.99999999999999645 ) ;
#33738=ORIENTED_EDGE ( 'NONE', *, *, #9367, .F. ) ;
#33741=CARTESIAN_POINT ( 'NONE',  ( 10.00000000000000000, 58.39081064771823293, -50.95692526931266286 ) ) ;
#33750=DIRECTION ( 'NONE',  ( -1.000000000000000000, -0.000000000000000000, -0.000000000000000000 ) ) ;
#33751=ORIENTED_EDGE ( 'NONE', *, *, #32514, .F. ) ;
#33752=DIRECTION ( 'NONE',  ( 0.000000000000000000, 0.000000000000000000, 1.000000000000000000 ) ) ;
#33756=CARTESIAN_POINT ( 'NONE',  ( 10.00000000000000000, -72.35160999960801576, -20.41045688087902121 ) ) ;
#33757=ORIENTED_EDGE ( 'NONE', *, *, #35070, .T. ) ;
#33760=FACE_OUTER_BOUND ( 'NONE', #30940, .T. ) ;
#33764=DIRECTION ( 'NONE',  ( 0.000000000000000000, 0.9238795325112851842, 0.3826834323650937786 ) ) ;
#33772=AXIS2_PLACEMENT_3D ( 'NONE', #52561, #2591, #65338 ) ;
#33774=VERTEX_POINT ( 'NONE', #7673 ) ;
#33776=AXIS2_PLACEMENT_3D ( 'NONE', #63680, #35455, #30179 ) ;
#33791=LINE ( 'NONE', #16881, #63064 ) ;
#33800=DIRECTION ( 'NONE',  ( 0.000000000000000000, 0.000000000000000000, 1.000000000000000000 ) ) ;
#33801=EDGE_CURVE ( 'NONE', #36080, #47197, #64822, .T. ) ;
#33822=ORIENTED_EDGE ( 'NONE', *, *, #61102, .F. ) ;
#33838=CIRCLE ( 'NONE', #50634, 31.99999999999998934 ) ;
#33841=ORIENTED_EDGE ( 'NONE', *, *, #40556, .F. ) ;
#33848=DIRECTION ( 'NONE',  ( 0.000000000000000000, 0.000000000000000000, 1.000000000000000000 ) ) ;
#33849=ORIENTED_EDGE ( 'NONE', *, *, #67572, .F. ) ;
#33856=EDGE_LOOP ( 'NONE', ( #51227, #54829, #59877, #1881 ) ) ;
#33857=EDGE_CURVE ( 'NONE', #16927, #50966, #28743, .T. ) ;
#33866=ORIENTED_EDGE ( 'NONE', *, *, #21202, .T. ) ;
#33871=ORIENTED_EDGE ( 'NONE', *, *, #44346, .T. ) ;
#33874=CARTESIAN_POINT ( 'NONE',  ( 10.00000000000000000, -23.16143007188481207, 73.95703589263968070 ) ) ;
#33879=AXIS2_PLACEMENT_3D ( 'NONE', #48044, #52945, #64978 ) ;
#33881=DIRECTION ( 'NONE',  ( -1.000000000000000000, 0.000000000000000000, -0.000000000000000000 ) ) ;
#33887=CARTESIAN_POINT ( 'NONE',  ( 10.00000000000000000, 0.000000000000000000, 0.000000000000000000 ) ) ;
#33889=AXIS2_PLACEMENT_3D ( 'NONE', #5226, #63114, #28490 ) ;
#33890=ORIENTED_EDGE ( 'NONE', *, *, #15169, .T. ) ;
#33893=DIRECTION ( 'NONE',  ( -1.000000000000000000, 0.000000000000000000, 0.000000000000000000 ) ) ;
#33915=ORIENTED_EDGE ( 'NONE', *, *, #43804, .F. ) ;
#33917=DIRECTION ( 'NONE',  ( 0.000000000000000000, 0.8910065241883657894, 0.4539904997395510788 ) ) ;
#33919=ORIENTED_EDGE ( 'NONE', *, *, #43804, .T. ) ;
#33929=EDGE_CURVE ( 'NONE', #69505, #57102, #50366, .T. ) ;
#33932=AXIS2_PLACEMENT_3D ( 'NONE', #22091, #45030, #27343 ) ;
#33937=ORIENTED_EDGE ( 'NONE', *, *, #12912, .T. ) ;
#33938=EDGE_CURVE ( 'NONE', #15883, #50966, #32806, .T. ) ;
#33947=CARTESIAN_POINT ( 'NONE',  ( 10.00000000000000000, -76.41127070299280888, 12.93880638057289012 ) ) ;
#33948=CARTESIAN_POINT ( 'NONE',  ( 10.00000000000000000, -8.830959090341869100, -74.65491531819127147 ) ) ;
#33986=CARTESIAN_POINT ( 'NONE',  ( 10.00000000000000000, 0.000000000000000000, 0.000000000000000000 ) ) ;
#33988=DIRECTION ( 'NONE',  ( 0.000000000000000000, 0.000000000000000000, 1.000000000000000000 ) ) ;
#33991=AXIS2_PLACEMENT_3D ( 'NONE', #17927, #18656, #69794 ) ;
#33995=CARTESIAN_POINT ( 'NONE',  ( 10.00000000000000000, 81.96053171279901051, -2.543863470248666658 ) ) ;
#33998=DIRECTION ( 'NONE',  ( 0.000000000000000000, 0.1564344650402311743, -0.9876883405951377704 ) ) ;
#34027=ORIENTED_EDGE ( 'NONE', *, *, #15424, .F. ) ;
#34036=ORIENTED_EDGE ( 'NONE', *, *, #8139, .F. ) ;
#34047=EDGE_CURVE ( 'NONE', #43336, #52788, #5017, .T. ) ;
#34053=VERTEX_POINT ( 'NONE', #67782 ) ;
#34059=ORIENTED_EDGE ( 'NONE', *, *, #26044, .T. ) ;
#34061=ADVANCED_FACE ( 'NONE', ( #17021 ), #33554, .T. ) ;
#34062=EDGE_CURVE ( 'NONE', #39425, #28922, #23989, .T. ) ;
#34063=CYLINDRICAL_SURFACE ( 'NONE', #10819, 82.00000000000000000 ) ;
#34064=EDGE_CURVE ( 'NONE', #39002, #70270, #71997, .T. ) ;
#34065=FACE_OUTER_BOUND ( 'NONE', #20922, .T. ) ;
#34069=ORIENTED_EDGE ( 'NONE', *, *, #64499, .T. ) ;
#34071=FACE_OUTER_BOUND ( 'NONE', #51266, .T. ) ;
#34091=AXIS2_PLACEMENT_3D ( 'NONE', #5915, #50636, #51755 ) ;
#34101=DIRECTION ( 'NONE',  ( -1.000000000000000000, 0.000000000000000000, 0.000000000000000000 ) ) ;
#34103=EDGE_CURVE ( 'NONE', #34053, #28563, #20382, .T. ) ;
#34107=DIRECTION ( 'NONE',  ( 1.000000000000000000, -0.000000000000000000, 0.000000000000000000 ) ) ;
#34111=DIRECTION ( 'NONE',  ( 1.000000000000000000, -0.000000000000000000, -0.000000000000000000 ) ) ;
#34115=EDGE_CURVE ( 'NONE', #60600, #48290, #40695, .T. ) ;
#34119=ORIENTED_EDGE ( 'NONE', *, *, #61867, .F. ) ;
#34125=ORIENTED_EDGE ( 'NONE', *, *, #56753, .T. ) ;
#34139=CARTESIAN_POINT ( 'NONE',  ( 0.000000000000000000, 21.60688246758696707, -79.10210256391346206 ) ) ;
#34145=VECTOR ( 'NONE', #62348, 1000.000000000000000 ) ;
#34147=ORIENTED_EDGE ( 'NONE', *, *, #29887, .T. ) ;
#34154=ORIENTED_EDGE ( 'NONE', *, *, #38786, .T. ) ;
#34163=CYLINDRICAL_SURFACE ( 'NONE', #22252, 82.00000000000000000 ) ;
#34168=CARTESIAN_POINT ( 'NONE',  ( 5.000000000000002665, 81.34940948281337114, 10.30890764327411979 ) ) ;
#34172=DIRECTION ( 'NONE',  ( -1.000000000000000000, -0.000000000000000000, -0.000000000000000000 ) ) ;
#34178=CARTESIAN_POINT ( 'NONE',  ( 0.000000000000000000, 14.66109333815564852, -73.73191006444555740 ) ) ;
#34179=AXIS2_PLACEMENT_3D ( 'NONE', #73240, #21742, #42928 ) ;
#34204=VERTEX_POINT ( 'NONE', #54557 ) ;
#34207=AXIS2_PLACEMENT_3D ( 'NONE', #70791, #41860, #36583 ) ;
#34209=EDGE_CURVE ( 'NONE', #36728, #18118, #31213, .T. ) ;
#34210=DIRECTION ( 'NONE',  ( -1.000000000000000000, -0.000000000000000000, -0.000000000000000000 ) ) ;
#34215=VERTEX_POINT ( 'NONE', #49280 ) ;
#34227=ORIENTED_EDGE ( 'NONE', *, *, #43068, .T. ) ;
#34237=ORIENTED_EDGE ( 'NONE', *, *, #72299, .T. ) ;
#34238=CARTESIAN_POINT ( 'NONE',  ( 10.00000000000000000, 0.000000000000000000, 0.000000000000000000 ) ) ;
#34261=DIRECTION ( 'NONE',  ( -1.000000000000000000, -0.000000000000000000, -0.000000000000000000 ) ) ;
#34265=CARTESIAN_POINT ( 'NONE',  ( 10.00000000000000000, 75.16055320797059380, -18.89407956138177269 ) ) ;
#34273=EDGE_CURVE ( 'NONE', #8568, #37924, #46853, .T. ) ;
#34277=EDGE_CURVE ( 'NONE', #47282, #56810, #15605, .T. ) ;
#34282=ADVANCED_FACE ( 'NONE', ( #25609 ), #42182, .T. ) ;
#34292=DIRECTION ( 'NONE',  ( -1.000000000000000000, 0.000000000000000000, -0.000000000000000000 ) ) ;
#34295=DIRECTION ( 'NONE',  ( -1.000000000000000000, -0.000000000000000000, 0.000000000000000000 ) ) ;
#34304=ORIENTED_EDGE ( 'NONE', *, *, #61916, .T. ) ;
#34309=EDGE_CURVE ( 'NONE', #34480, #30579, #68480, .T. ) ;
#34323=AXIS2_PLACEMENT_3D ( 'NONE', #5794, #49770, #55797 ) ;
#34327=VERTEX_POINT ( 'NONE', #38751 ) ;
#34328=LINE ( 'NONE', #5413, #25126 ) ;
#34333=CARTESIAN_POINT ( 'NONE',  ( 10.00000000000000000, -71.91182617369167929, -28.89263327155822481 ) ) ;
#34337=EDGE_LOOP ( 'NONE', ( #59186, #56480, #33167, #57593 ) ) ;
#34344=CARTESIAN_POINT ( 'NONE',  ( 0.000000000000000000, -75.54627589209955829, 17.28742895386058009 ) ) ;
#34355=ADVANCED_FACE ( 'NONE', ( #33463 ), #50386, .T. ) ;
#34372=ORIENTED_EDGE ( 'NONE', *, *, #5280, .F. ) ;
#34373=AXIS2_PLACEMENT_3D ( 'NONE', #24455, #6078, #28980 ) ;
#34376=EDGE_CURVE ( 'NONE', #32419, #22189, #42065, .T. ) ;
#34381=VERTEX_POINT ( 'NONE', #60938 ) ;
#34383=VERTEX_POINT ( 'NONE', #3816 ) ;
#34386=EDGE_CURVE ( 'NONE', #22507, #73223, #21604, .T. ) ;
#34394=VERTEX_POINT ( 'NONE', #16184 ) ;
#34399=DIRECTION ( 'NONE',  ( 1.000000000000000000, -0.000000000000000000, -0.000000000000000000 ) ) ;
#34403=EDGE_LOOP ( 'NONE', ( #30052, #61869, #73692, #7089 ) ) ;
#34415=AXIS2_PLACEMENT_3D ( 'NONE', #23760, #51957, #34668 ) ;
#34422=CIRCLE ( 'NONE', #54867, 82.00000000000000000 ) ;
#34423=ORIENTED_EDGE ( 'NONE', *, *, #33616, .T. ) ;
#34432=ORIENTED_EDGE ( 'NONE', *, *, #5370, .T. ) ;
#34437=DIRECTION ( 'NONE',  ( -1.000000000000000000, 0.000000000000000000, 0.000000000000000000 ) ) ;
#34447=DIRECTION ( 'NONE',  ( -1.000000000000000000, -0.000000000000000000, 0.000000000000000000 ) ) ;
#34449=EDGE_CURVE ( 'NONE', #16195, #54579, #43266, .T. ) ;
#34454=CARTESIAN_POINT ( 'NONE',  ( 5.000000000000002665, 76.69515212746057387, -29.01471420065480089 ) ) ;
#34456=DIRECTION ( 'NONE',  ( 0.000000000000000000, -0.9876883405951394357, 0.1564344650402205716 ) ) ;
#34463=CARTESIAN_POINT ( 'NONE',  ( 10.00000000000000000, 24.73286445877703699, 73.44644590900070114 ) ) ;
#34465=DIRECTION ( 'NONE',  ( 1.000000000000000000, 0.000000000000000000, 0.000000000000000000 ) ) ;
#34468=ORIENTED_EDGE ( 'NONE', *, *, #25527, .F. ) ;
#34480=VERTEX_POINT ( 'NONE', #10537 ) ;
#34491=VECTOR ( 'NONE', #13856, 1000.000000000000000 ) ;
#34503=DIRECTION ( 'NONE',  ( -1.000000000000000000, -0.000000000000000000, 0.000000000000000000 ) ) ;
#34506=CYLINDRICAL_SURFACE ( 'NONE', #2750, 31.99999999999998579 ) ;
#34508=ORIENTED_EDGE ( 'NONE', *, *, #59873, .T. ) ;
#34519=CIRCLE ( 'NONE', #50116, 31.99999999999999289 ) ;
#34532=CARTESIAN_POINT ( 'NONE',  ( 0.000000000000000000, 28.89263327155746097, 71.91182617369197771 ) ) ;
#34535=EDGE_CURVE ( 'NONE', #57460, #25525, #40886, .T. ) ;
#34542=LINE ( 'NONE', #39834, #67757 ) ;
#34548=VECTOR ( 'NONE', #45946, 1000.000000000000000 ) ;
#34549=CARTESIAN_POINT ( 'NONE',  ( 0.000000000000000000, -50.23322058963393744, 64.81221759200325039 ) ) ;
#34570=CARTESIAN_POINT ( 'NONE',  ( 10.00000000000000000, 0.000000000000000000, 0.000000000000000000 ) ) ;
#34583=VERTEX_POINT ( 'NONE', #29303 ) ;
#34585=EDGE_LOOP ( 'NONE', ( #64864, #543, #72305, #31525 ) ) ;
#34589=CARTESIAN_POINT ( 'NONE',  ( 5.000000000000002665, 76.69515212746016175, 29.01471420065591289 ) ) ;
#34608=FACE_OUTER_BOUND ( 'NONE', #59257, .T. ) ;
#34611=ADVANCED_FACE ( 'NONE', ( #63550 ), #41344, .T. ) ;
#34616=EDGE_CURVE ( 'NONE', #29034, #38013, #12023, .T. ) ;
#34622=DIRECTION ( 'NONE',  ( -1.000000000000000000, 0.000000000000000000, 0.000000000000000000 ) ) ;
#34627=VECTOR ( 'NONE', #66721, 1000.000000000000000 ) ;
#34632=DIRECTION ( 'NONE',  ( -1.000000000000000000, -0.000000000000000000, 0.000000000000000000 ) ) ;
#34644=AXIS2_PLACEMENT_3D ( 'NONE', #40762, #58788, #12174 ) ;
#34645=EDGE_CURVE ( 'NONE', #9362, #32052, #9690, .T. ) ;
#34648=CARTESIAN_POINT ( 'NONE',  ( 10.00000000000000000, -73.95703589263958122, -23.16143007188506431 ) ) ;
#34652=EDGE_CURVE ( 'NONE', #37997, #35415, #50476, .T. ) ;
#34653=FACE_OUTER_BOUND ( 'NONE', #22363, .T. ) ;
#34661=CARTESIAN_POINT ( 'NONE',  ( 10.00000000000000000, -70.53064760720336324, 26.01480285779810231 ) ) ;
#34662=ORIENTED_EDGE ( 'NONE', *, *, #63763, .T. ) ;
#34663=DIRECTION ( 'NONE',  ( -1.000000000000000000, -0.000000000000000000, 0.000000000000000000 ) ) ;
#34668=DIRECTION ( 'NONE',  ( 0.000000000000000000, 0.000000000000000000, 1.000000000000000000 ) ) ;
#34675=AXIS2_PLACEMENT_3D ( 'NONE', #44733, #67657, #3406 ) ;
#34686=DIRECTION ( 'NONE',  ( -1.000000000000000000, -0.000000000000000000, 0.000000000000000000 ) ) ;
#34695=DIRECTION ( 'NONE',  ( -1.000000000000000000, -0.000000000000000000, 0.000000000000000000 ) ) ;
#34696=DIRECTION ( 'NONE',  ( 0.000000000000000000, 0.000000000000000000, -1.000000000000000000 ) ) ;
#34703=CARTESIAN_POINT ( 'NONE',  ( 10.00000000000000000, 0.000000000000000000, 0.000000000000000000 ) ) ;
#34704=DIRECTION ( 'NONE',  ( 0.000000000000000000, 0.000000000000000000, 1.000000000000000000 ) ) ;
#34707=VECTOR ( 'NONE', #19045, 1000.000000000000000 ) ;
#34708=AXIS2_PLACEMENT_3D ( 'NONE', #33460, #56419, #36796 ) ;
#34710=VERTEX_POINT ( 'NONE', #23468 ) ;
#34711=CIRCLE ( 'NONE', #44321, 82.00000000000000000 ) ;
#34713=AXIS2_PLACEMENT_3D ( 'NONE', #4149, #15399, #38342 ) ;
#34736=AXIS2_PLACEMENT_3D ( 'NONE', #60603, #9448, #49662 ) ;
#34741=CARTESIAN_POINT ( 'NONE',  ( 5.000000000000002665, -21.60688246758530440, -79.10210256391390260 ) ) ;
#34748=ADVANCED_FACE ( 'NONE', ( #71155 ), #70793, .T. ) ;
#34753=EDGE_LOOP ( 'NONE', ( #35853, #37725, #54818, #34119 ) ) ;
#34754=CYLINDRICAL_SURFACE ( 'NONE', #25111, 32.00000000000000000 ) ;
#34778=FACE_OUTER_BOUND ( 'NONE', #12414, .T. ) ;
#34779=CARTESIAN_POINT ( 'NONE',  ( 10.00000000000000000, 0.8261519478441983200, -77.49459641780885022 ) ) ;
#34786=ORIENTED_EDGE ( 'NONE', *, *, #59149, .F. ) ;
#34787=CARTESIAN_POINT ( 'NONE',  ( 10.00000000000000000, 0.000000000000000000, 0.000000000000000000 ) ) ;
#34791=VECTOR ( 'NONE', #71631, 1000.000000000000000 ) ;
#34797=EDGE_CURVE ( 'NONE', #45506, #44699, #20028, .T. ) ;
#34807=ORIENTED_EDGE ( 'NONE', *, *, #15694, .T. ) ;
#34810=CYLINDRICAL_SURFACE ( 'NONE', #38454, 31.99999999999999289 ) ;
#34814=EDGE_CURVE ( 'NONE', #30208, #11931, #54083, .T. ) ;
#34815=ORIENTED_EDGE ( 'NONE', *, *, #57470, .T. ) ;
#34824=CARTESIAN_POINT ( 'NONE',  ( -10.00000000000000000, 0.000000000000000000, 0.000000000000000000 ) ) ;
#34826=AXIS2_PLACEMENT_3D ( 'NONE', #44022, #50008, #49640 ) ;
#34839=CARTESIAN_POINT ( 'NONE',  ( 10.00000000000000000, 71.27951684758026829, 30.41916302227139113 ) ) ;
#34841=CARTESIAN_POINT ( 'NONE',  ( 0.000000000000000000, 23.16143007188426850, 73.95703589263983702 ) ) ;
#34848=ORIENTED_EDGE ( 'NONE', *, *, #57057, .F. ) ;
#34849=ORIENTED_EDGE ( 'NONE', *, *, #70875, .F. ) ;
#34855=DIRECTION ( 'NONE',  ( 0.000000000000000000, 0.000000000000000000, 1.000000000000000000 ) ) ;
#34861=ORIENTED_EDGE ( 'NONE', *, *, #16413, .F. ) ;
#34874=CIRCLE ( 'NONE', #49244, 82.00000000000000000 ) ;
#34876=ORIENTED_EDGE ( 'NONE', *, *, #51461, .F. ) ;
#34879=DIRECTION ( 'NONE',  ( 0.000000000000000000, 0.000000000000000000, 1.000000000000000000 ) ) ;
#34887=DIRECTION ( 'NONE',  ( 0.000000000000000000, 0.000000000000000000, 1.000000000000000000 ) ) ;
#34888=DIRECTION ( 'NONE',  ( -1.000000000000000000, -0.000000000000000000, -0.000000000000000000 ) ) ;
#34895=CARTESIAN_POINT ( 'NONE',  ( 10.00000000000000000, -41.76937507738745836, -62.50329211542482710 ) ) ;
#34903=ADVANCED_FACE ( 'NONE', ( #19298 ), #8398, .T. ) ;
#34910=AXIS2_PLACEMENT_3D ( 'NONE', #49038, #71965, #25385 ) ;
#34915=DIRECTION ( 'NONE',  ( -1.000000000000000000, 0.000000000000000000, 0.000000000000000000 ) ) ;
#34923=FACE_OUTER_BOUND ( 'NONE', #62903, .T. ) ;
#34929=AXIS2_PLACEMENT_3D ( 'NONE', #52204, #56757, #51839 ) ;
#34930=DIRECTION ( 'NONE',  ( -1.000000000000000000, 0.000000000000000000, -0.000000000000000000 ) ) ;
#34935=DIRECTION ( 'NONE',  ( -1.000000000000000000, -0.000000000000000000, -0.000000000000000000 ) ) ;
#34939=VERTEX_POINT ( 'NONE', #61642 ) ;
#34946=ADVANCED_FACE ( 'NONE', ( #8004 ), #55992, .T. ) ;
#34949=ORIENTED_EDGE ( 'NONE', *, *, #15644, .T. ) ;
#34953=ORIENTED_EDGE ( 'NONE', *, *, #65043, .F. ) ;
#34956=CARTESIAN_POINT ( 'NONE',  ( 10.00000000000000000, 0.000000000000000000, 0.000000000000000000 ) ) ;
#34957=EDGE_CURVE ( 'NONE', #9632, #60502, #52901, .T. ) ;
#34958=EDGE_LOOP ( 'NONE', ( #33919, #73103, #34227, #60378 ) ) ;
#34962=EDGE_LOOP ( 'NONE', ( #55957, #7823, #5300, #45431 ) ) ;
#34964=ORIENTED_EDGE ( 'NONE', *, *, #35070, .F. ) ;
#34973=CARTESIAN_POINT ( 'NONE',  ( -10.00000000000000000, 0.000000000000000000, 0.000000000000000000 ) ) ;
#34974=ORIENTED_EDGE ( 'NONE', *, *, #66489, .T. ) ;
#34986=DIRECTION ( 'NONE',  ( -1.000000000000000000, -0.000000000000000000, -0.000000000000000000 ) ) ;
#34990=EDGE_CURVE ( 'NONE', #32052, #70437, #71882, .T. ) ;
#34991=FACE_OUTER_BOUND ( 'NONE', #3004, .T. ) ;
#34995=DIRECTION ( 'NONE',  ( 1.000000000000000000, 0.000000000000000000, 0.000000000000000000 ) ) ;
#35004=EDGE_CURVE ( 'NONE', #56502, #65113, #8522, .T. ) ;
#35024=CIRCLE ( 'NONE', #51827, 82.00000000000000000 ) ;
#35027=DIRECTION ( 'NONE',  ( 1.000000000000000000, -0.000000000000000000, 0.000000000000000000 ) ) ;
#35049=DIRECTION ( 'NONE',  ( 0.000000000000000000, -0.4539904997395350361, -0.8910065241883738940 ) ) ;
#35070=EDGE_CURVE ( 'NONE', #14784, #4987, #33737, .T. ) ;
#35073=DIRECTION ( 'NONE',  ( 0.000000000000000000, -0.9723699203976741146, -0.2334453638559159938 ) ) ;
#35075=EDGE_CURVE ( 'NONE', #60043, #1351, #27724, .T. ) ;
#35079=CYLINDRICAL_SURFACE ( 'NONE', #51080, 82.00000000000000000 ) ;
#35082=VECTOR ( 'NONE', #42716, 1000.000000000000000 ) ;
#35097=EDGE_LOOP ( 'NONE', ( #22019, #44056, #51960, #42506 ) ) ;
#35099=EDGE_CURVE ( 'NONE', #2787, #19205, #63507, .T. ) ;
#35101=DIRECTION ( 'NONE',  ( 0.000000000000000000, -0.9723699203976789995, 0.2334453638558956490 ) ) ;
#35104=CARTESIAN_POINT ( 'NONE',  ( 10.00000000000000000, -63.18004540532994184, -44.88180994100446952 ) ) ;
#35109=CYLINDRICAL_SURFACE ( 'NONE', #25420, 82.00000000000000000 ) ;
#35110=ORIENTED_EDGE ( 'NONE', *, *, #33616, .F. ) ;
#35119=ORIENTED_EDGE ( 'NONE', *, *, #35867, .F. ) ;
#35124=AXIS2_PLACEMENT_3D ( 'NONE', #47389, #36103, #19177 ) ;
#35128=ORIENTED_EDGE ( 'NONE', *, *, #72115, .F. ) ;
#35150=ADVANCED_FACE ( 'NONE', ( #22 ), #17995, .T. ) ;
#35171=ORIENTED_EDGE ( 'NONE', *, *, #25041, .T. ) ;
#35176=CARTESIAN_POINT ( 'NONE',  ( 5.000000000000000000, 67.80270845531887858, 46.11716303203210998 ) ) ;
#35177=AXIS2_PLACEMENT_3D ( 'NONE', #39388, #62712, #40125 ) ;
#35180=ORIENTED_EDGE ( 'NONE', *, *, #43330, .T. ) ;
#35190=DIRECTION ( 'NONE',  ( -1.000000000000000000, 0.000000000000000000, 0.000000000000000000 ) ) ;
#35191=FACE_OUTER_BOUND ( 'NONE', #27057, .T. ) ;
#35219=ADVANCED_FACE ( 'NONE', ( #58216 ), #57121, .T. ) ;
#35223=ORIENTED_EDGE ( 'NONE', *, *, #16720, .F. ) ;
#35226=AXIS2_PLACEMENT_3D ( 'NONE', #46561, #52192, #36372 ) ;
#35233=DIRECTION ( 'NONE',  ( 0.000000000000000000, 0.000000000000000000, 1.000000000000000000 ) ) ;
#35240=ORIENTED_EDGE ( 'NONE', *, *, #40605, .F. ) ;
#35242=CARTESIAN_POINT ( 'NONE',  ( 10.00000000000000000, -51.03279382321125723, 55.19960302592048862 ) ) ;
#35256=EDGE_CURVE ( 'NONE', #1142, #27456, #44544, .T. ) ;
#35263=CIRCLE ( 'NONE', #2877, 82.00000000000000000 ) ;
#35268=FACE_OUTER_BOUND ( 'NONE', #26909, .T. ) ;
#35281=CYLINDRICAL_SURFACE ( 'NONE', #31573, 77.49899999999999523 ) ;
#35285=AXIS2_PLACEMENT_3D ( 'NONE', #51129, #39868, #56785 ) ;
#35291=VECTOR ( 'NONE', #10215, 1000.000000000000000 ) ;
#35305=CARTESIAN_POINT ( 'NONE',  ( 0.000000000000000000, -39.78640506895652607, 66.50666863321986000 ) ) ;
#35310=CYLINDRICAL_SURFACE ( 'NONE', #842, 77.49899999999999523 ) ;
#35316=ORIENTED_EDGE ( 'NONE', *, *, #22939, .T. ) ;
#35318=ORIENTED_EDGE ( 'NONE', *, *, #47344, .F. ) ;
#35330=EDGE_CURVE ( 'NONE', #54114, #16652, #56573, .T. ) ;
#35332=CYLINDRICAL_SURFACE ( 'NONE', #70690, 31.99999999999999289 ) ;
#35339=VERTEX_POINT ( 'NONE', #2222 ) ;
#35342=VECTOR ( 'NONE', #19732, 1000.000000000000000 ) ;
#35347=DIRECTION ( 'NONE',  ( 0.000000000000000000, 0.000000000000000000, 1.000000000000000000 ) ) ;
#35351=DIRECTION ( 'NONE',  ( 0.000000000000000000, 0.000000000000000000, 1.000000000000000000 ) ) ;
#35356=CIRCLE ( 'NONE', #46207, 31.99999999999998934 ) ;
#35362=CYLINDRICAL_SURFACE ( 'NONE', #49436, 77.49899999999999523 ) ;
#35366=AXIS2_PLACEMENT_3D ( 'NONE', #39419, #34503, #30418 ) ;
#35370=DIRECTION ( 'NONE',  ( 0.000000000000000000, -0.7604059656000227152, -0.6494480483301933171 ) ) ;
#35372=EDGE_CURVE ( 'NONE', #73771, #63204, #28911, .T. ) ;
#35375=ORIENTED_EDGE ( 'NONE', *, *, #16809, .T. ) ;
#35385=EDGE_CURVE ( 'NONE', #31227, #62260, #21708, .T. ) ;
#35396=ORIENTED_EDGE ( 'NONE', *, *, #58677, .F. ) ;
#35397=CARTESIAN_POINT ( 'NONE',  ( 10.00000000000000000, 18.89407956138256139, 75.16055320797038064 ) ) ;
#35405=VERTEX_POINT ( 'NONE', #33325 ) ;
#35406=DIRECTION ( 'NONE',  ( 0.000000000000000000, 0.000000000000000000, 1.000000000000000000 ) ) ;
#35411=CARTESIAN_POINT ( 'NONE',  ( 10.00000000000000000, -44.88180994100329713, -63.18004540533077318 ) ) ;
#35415=VERTEX_POINT ( 'NONE', #20199 ) ;
#35417=ORIENTED_EDGE ( 'NONE', *, *, #51928, .F. ) ;
#35421=VERTEX_POINT ( 'NONE', #38624 ) ;
#35431=DIRECTION ( 'NONE',  ( -1.000000000000000000, -0.000000000000000000, 0.000000000000000000 ) ) ;
#35434=ORIENTED_EDGE ( 'NONE', *, *, #61045, .T. ) ;
#35438=DIRECTION ( 'NONE',  ( -1.000000000000000000, -0.000000000000000000, 0.000000000000000000 ) ) ;
#35455=DIRECTION ( 'NONE',  ( -1.000000000000000000, -0.000000000000000000, -0.000000000000000000 ) ) ;
#35459=CARTESIAN_POINT ( 'NONE',  ( 10.00000000000000000, 0.000000000000000000, 0.000000000000000000 ) ) ;
#35460=ORIENTED_EDGE ( 'NONE', *, *, #43715, .T. ) ;
#35476=EDGE_CURVE ( 'NONE', #4362, #22507, #10985, .T. ) ;
#35489=AXIS2_PLACEMENT_3D ( 'NONE', #36633, #2480, #72327 ) ;
#35490=ORIENTED_EDGE ( 'NONE', *, *, #57797, .F. ) ;
#35496=AXIS2_PLACEMENT_3D ( 'NONE', #20185, #43527, #65699 ) ;
#35502=CIRCLE ( 'NONE', #9104, 32.00000000000000000 ) ;
#35520=ORIENTED_EDGE ( 'NONE', *, *, #41402, .T. ) ;
#35531=ORIENTED_EDGE ( 'NONE', *, *, #15334, .F. ) ;
#35533=DIRECTION ( 'NONE',  ( -1.000000000000000000, -0.000000000000000000, -0.000000000000000000 ) ) ;
#35540=AXIS2_PLACEMENT_3D ( 'NONE', #56153, #44132, #39241 ) ;
#35548=AXIS2_PLACEMENT_3D ( 'NONE', #20600, #59074, #70692 ) ;
#35553=FACE_OUTER_BOUND ( 'NONE', #20328, .T. ) ;
#35555=EDGE_CURVE ( 'NONE', #70629, #44617, #59028, .T. ) ;
#35569=EDGE_LOOP ( 'NONE', ( #2630, #34953, #61017, #42838 ) ) ;
#35575=CLOSED_SHELL ( 'NONE', ( #71250, #43, #66547, #54071, #51880, #55571, #25812, #22234, #39392, #65363, #71775, #25606, #64496, #67163, #72788, #13745, #25867, #36210, #19329, #9769, #40230, #50913, #9519, #6839, #61098, #21967, #17601, #22842, #44229, #48801, #31657, #24614, #20771, #41276, #58134, #69899, #71710, #35219, #62131, #51506, #13931, #52876, #49294, #27078, #2683, #38736, #27301, #57496, #71040, #70617, #28115, #21027, #49735, #59310, #69085, #66941, #58892, #9236, #32904, #54853, #46585, #67315, #68702, #29340, #23783, #47018, #23499, #23626, #16825, #49883, #53072, #1592, #2673, #59675, #56995, #18927, #55092, #11027, #11138, #45107, #43382, #24800, #59622, #45496, #72962, #21737, #8600, #46006, #34282, #23674, #12784, #12973, #65994, #21363, #34903, #69619, #45414, #14209, #42428, #54506, #20304, #36921, #50230, #37468, #60843, #711, #40100, #17805, #1139, #70225, #62497, #5821, #48869, #23038, #49795, #24382, #34748, #48582, #11478, #44754, #28673, #15782, #30367, #44336, #37610, #59093, #56174, #16813, #62163, #35657, #45019, #31927, #24374, #70933, #6984, #56030, #17062, #52502, #55003, #16654, #27127, #59754, #16977, #6364, #34061, #54177, #48130, #64416, #11784, #46951, #12236, #34355, #23097, #26194, #13139, #32859, #63857, #32090, #4366, #11285, #71429, #10109, #2063, #52189, #38089, #4572, #51964, #53150, #34611, #38182, #8297, #60811, #29592, #54770, #11095, #72416, #14106, #38478, #65960, #60346, #60766, #58737, #62407, #37303, #55251, #48689, #8746, #51327, #70668, #43513, #61108, #13507, #56699, #12792, #27609, #41865, #24051, #63407, #15872, #4500, #148, #33348, #6622, #32675, #66464, #48271, #23370, #27392, #15016, #69830, #54432, #64341, #35830, #50680, #73330, #8656, #30306, #33166, #57038, #8160, #71792, #12308, #9309, #7638, #73472, #13894, #36765, #49044, #52946, #36659, #9671, #61006, #40422, #22262, #57924, #37956, #40314, #14865, #37888, #41483, #64210, #26074, #17835, #33023, #6490, #30908, #29031, #65782, #4943, #15610, #35925, #32567, #15007, #18004, #44737, #61205, #67386, #71092, #50645, #35150, #37892, #24526, #71958, #3772, #24426, #63784, #37958, #36020, #61047, #68896, #18813, #31928, #4858, #40373, #68701, #72060, #30019, #58498, #64676, #39580, #21558, #7028, #6130, #43659, #54728, #19092, #31628, #56617, #34946, #59858, #258, #28948, #56272, #1872, #12222, #5099, #37000, #26751, #54392, #14933, #49048, #38530, #20524, #40667, #43304, #36296, #59787, #51846, #1232, #40051, #52888, #27864, #73118, #48613, #12070, #9356, #74169, #30993, #45086, #62744, #37346, #18659, #26654, #10035, #21523, #47545, #71347, #20475, #30488, #38175, #72332, #2263, #24564 ) ) ;
#35576=ORIENTED_EDGE ( 'NONE', *, *, #34652, .F. ) ;
#35579=DIRECTION ( 'NONE',  ( -1.000000000000000000, -0.000000000000000000, -0.000000000000000000 ) ) ;
#35581=LINE ( 'NONE', #36322, #22024 ) ;
#35583=FACE_OUTER_BOUND ( 'NONE', #28747, .T. ) ;
#35588=ORIENTED_EDGE ( 'NONE', *, *, #42902, .F. ) ;
#35594=CARTESIAN_POINT ( 'NONE',  ( 10.00000000000000000, -41.76106447765443619, -62.50884508063471401 ) ) ;
#35599=ORIENTED_EDGE ( 'NONE', *, *, #24124, .T. ) ;
#35610=FACE_OUTER_BOUND ( 'NONE', #3619, .T. ) ;
#35616=AXIS2_PLACEMENT_3D ( 'NONE', #69517, #41318, #64259 ) ;
#35618=CARTESIAN_POINT ( 'NONE',  ( 0.000000000000000000, -81.50828551894220197, -8.966570791701583332 ) ) ;
#35621=VERTEX_POINT ( 'NONE', #5169 ) ;
#35636=DIRECTION ( 'NONE',  ( -1.000000000000000000, 0.000000000000000000, 0.000000000000000000 ) ) ;
#35641=CIRCLE ( 'NONE', #21201, 31.99999999999999289 ) ;
#35644=LINE ( 'NONE', #8186, #33539 ) ;
#35647=CARTESIAN_POINT ( 'NONE',  ( 0.000000000000000000, -72.35432306680469594, -20.40083707022958848 ) ) ;
#35654=CARTESIAN_POINT ( 'NONE',  ( 5.000000000000000000, 56.15606465354959198, 59.75363087400094741 ) ) ;
#35657=ADVANCED_FACE ( 'NONE', ( #58493 ), #41212, .T. ) ;
#35661=ORIENTED_EDGE ( 'NONE', *, *, #59933, .T. ) ;
#35670=ORIENTED_EDGE ( 'NONE', *, *, #47865, .T. ) ;
#35675=ORIENTED_EDGE ( 'NONE', *, *, #50706, .F. ) ;
#35676=CARTESIAN_POINT ( 'NONE',  ( 10.00000000000000000, 69.42325613327489009, -34.44570377933524696 ) ) ;
#35703=CARTESIAN_POINT ( 'NONE',  ( 10.00000000000000000, -11.30684508768284680, -76.66974797899850103 ) ) ;
#35709=DIRECTION ( 'NONE',  ( -1.000000000000000000, 0.000000000000000000, 0.000000000000000000 ) ) ;
#35710=CARTESIAN_POINT ( 'NONE',  ( 0.000000000000000000, 63.18004540533092239, -44.88180994100307686 ) ) ;
#35712=EDGE_CURVE ( 'NONE', #53902, #15045, #70490, .T. ) ;
#35714=AXIS2_PLACEMENT_3D ( 'NONE', #5194, #5933, #45790 ) ;
#35716=DIRECTION ( 'NONE',  ( -1.000000000000000000, 0.000000000000000000, -0.000000000000000000 ) ) ;
#35717=CARTESIAN_POINT ( 'NONE',  ( 10.00000000000000000, -74.65491531819111515, 23.16904090965678975 ) ) ;
#35719=AXIS2_PLACEMENT_3D ( 'NONE', #43211, #9716, #14611 ) ;
#35720=DIRECTION ( 'NONE',  ( 0.000000000000000000, 0.000000000000000000, 1.000000000000000000 ) ) ;
#35725=EDGE_CURVE ( 'NONE', #42459, #8427, #8100, .T. ) ;
#35742=DIRECTION ( 'NONE',  ( 0.000000000000000000, 0.000000000000000000, 1.000000000000000000 ) ) ;
#35745=DIRECTION ( 'NONE',  ( -1.000000000000000000, -0.000000000000000000, 0.000000000000000000 ) ) ;
#35761=CIRCLE ( 'NONE', #38190, 32.00000000000000000 ) ;
#35781=DIRECTION ( 'NONE',  ( 0.000000000000000000, 0.000000000000000000, 1.000000000000000000 ) ) ;
#35784=CARTESIAN_POINT ( 'NONE',  ( 0.000000000000000000, -65.59268652807237743, 36.72794159290217664 ) ) ;
#35793=LINE ( 'NONE', #18876, #19171 ) ;
#35796=CARTESIAN_POINT ( 'NONE',  ( 10.00000000000000000, -50.95692526931286181, -58.39081064771806240 ) ) ;
#35799=CIRCLE ( 'NONE', #44245, 31.99999999999999645 ) ;
#35800=DIRECTION ( 'NONE',  ( 1.000000000000000000, 0.000000000000000000, 0.000000000000000000 ) ) ;
#35801=EDGE_CURVE ( 'NONE', #47809, #50757, #30192, .T. ) ;
#35803=CARTESIAN_POINT ( 'NONE',  ( 10.00000000000000000, -49.70050353004846500, -59.46389618802017907 ) ) ;
#35807=EDGE_LOOP ( 'NONE', ( #2443, #22040, #37206, #71385 ) ) ;
#35813=FACE_OUTER_BOUND ( 'NONE', #53627, .T. ) ;
#35819=CIRCLE ( 'NONE', #45462, 31.99999999999999645 ) ;
#35821=CARTESIAN_POINT ( 'NONE',  ( 0.000000000000000000, 0.000000000000000000, 0.000000000000000000 ) ) ;
#35823=AXIS2_PLACEMENT_3D ( 'NONE', #2565, #25445, #25813 ) ;
#35827=AXIS2_PLACEMENT_3D ( 'NONE', #69223, #50802, #17710 ) ;
#35830=ADVANCED_FACE ( 'NONE', ( #30650 ), #15961, .T. ) ;
#35831=AXIS2_PLACEMENT_3D ( 'NONE', #43994, #66910, #60551 ) ;
#35843=ORIENTED_EDGE ( 'NONE', *, *, #30473, .F. ) ;
#35844=CARTESIAN_POINT ( 'NONE',  ( 10.00000000000000000, 0.000000000000000000, 0.000000000000000000 ) ) ;
#35846=CIRCLE ( 'NONE', #68292, 32.00000000000000000 ) ;
#35849=CIRCLE ( 'NONE', #69458, 77.49899999999999523 ) ;
#35852=AXIS2_PLACEMENT_3D ( 'NONE', #63590, #18083, #28235 ) ;
#35853=ORIENTED_EDGE ( 'NONE', *, *, #49533, .F. ) ;
#35867=EDGE_CURVE ( 'NONE', #15883, #29404, #56615, .T. ) ;
#35875=CARTESIAN_POINT ( 'NONE',  ( 10.00000000000000000, 80.55351364060589958, 15.33399622253511829 ) ) ;
#35888=VERTEX_POINT ( 'NONE', #14852 ) ;
#35896=VERTEX_POINT ( 'NONE', #66732 ) ;
#35903=CARTESIAN_POINT ( 'NONE',  ( 10.00000000000000000, -26.01480285779885904, 70.53064760720306481 ) ) ;
#35904=EDGE_CURVE ( 'NONE', #58272, #39711, #15221, .T. ) ;
#35923=CARTESIAN_POINT ( 'NONE',  ( 0.000000000000000000, 26.01480285779933510, -70.53064760720289428 ) ) ;
#35925=ADVANCED_FACE ( 'NONE', ( #4332 ), #20501, .T. ) ;
#35931=ORIENTED_EDGE ( 'NONE', *, *, #64439, .F. ) ;
#35936=AXIS2_PLACEMENT_3D ( 'NONE', #33756, #45804, #63099 ) ;
#35938=AXIS2_PLACEMENT_3D ( 'NONE', #5269, #57129, #62030 ) ;
#35943=CARTESIAN_POINT ( 'NONE',  ( 0.000000000000000000, 76.69515212746057387, -29.01471420065480089 ) ) ;
#35949=DIRECTION ( 'NONE',  ( 0.000000000000000000, 0.000000000000000000, 1.000000000000000000 ) ) ;
#35956=AXIS2_PLACEMENT_3D ( 'NONE', #38629, #10043, #32599 ) ;
#35959=ORIENTED_EDGE ( 'NONE', *, *, #40184, .F. ) ;
#35986=DIRECTION ( 'NONE',  ( -1.000000000000000000, -0.000000000000000000, -0.000000000000000000 ) ) ;
#35987=CIRCLE ( 'NONE', #50362, 31.99999999999999289 ) ;
#35993=AXIS2_PLACEMENT_3D ( 'NONE', #70817, #31336, #8041 ) ;
#35999=ORIENTED_EDGE ( 'NONE', *, *, #9495, .T. ) ;
#36001=EDGE_CURVE ( 'NONE', #46606, #37162, #46391, .T. ) ;
#36003=ORIENTED_EDGE ( 'NONE', *, *, #14097, .F. ) ;
#36008=FACE_OUTER_BOUND ( 'NONE', #27572, .T. ) ;
#36016=FACE_OUTER_BOUND ( 'NONE', #21333, .T. ) ;
#36020=ADVANCED_FACE ( 'NONE', ( #33621 ), #38901, .T. ) ;
#36021=DIRECTION ( 'NONE',  ( 0.000000000000000000, 0.000000000000000000, 1.000000000000000000 ) ) ;
#36022=CIRCLE ( 'NONE', #1241, 82.00000000000000000 ) ;
#36027=EDGE_LOOP ( 'NONE', ( #8905, #3833, #9603, #31269 ) ) ;
#36031=CIRCLE ( 'NONE', #45672, 12.50000000000000000 ) ;
#36034=CIRCLE ( 'NONE', #16677, 77.49899999999999523 ) ;
#36049=DIRECTION ( 'NONE',  ( -1.000000000000000000, -0.000000000000000000, -0.000000000000000000 ) ) ;
#36050=ORIENTED_EDGE ( 'NONE', *, *, #73186, .F. ) ;
#36056=ORIENTED_EDGE ( 'NONE', *, *, #40560, .F. ) ;
#36061=EDGE_CURVE ( 'NONE', #11811, #51313, #59073, .T. ) ;
#36070=AXIS2_PLACEMENT_3D ( 'NONE', #36198, #42227, #48592 ) ;
#36071=( NAMED_UNIT ( * ) PLANE_ANGLE_UNIT ( ) SI_UNIT ( $, .RADIAN. ) );
#36072=ORIENTED_EDGE ( 'NONE', *, *, #36515, .F. ) ;
#36079=AXIS2_PLACEMENT_3D ( 'NONE', #20917, #66782, #31077 ) ;
#36080=VERTEX_POINT ( 'NONE', #33995 ) ;
#36092=CARTESIAN_POINT ( 'NONE',  ( 10.00000000000000000, 0.000000000000000000, 0.000000000000000000 ) ) ;
#36101=DIRECTION ( 'NONE',  ( 0.000000000000000000, 0.000000000000000000, 1.000000000000000000 ) ) ;
#36103=DIRECTION ( 'NONE',  ( -1.000000000000000000, 0.000000000000000000, -0.000000000000000000 ) ) ;
#36108=DIRECTION ( 'NONE',  ( 0.000000000000000000, 0.000000000000000000, 1.000000000000000000 ) ) ;
#36109=DIRECTION ( 'NONE',  ( -1.000000000000000000, -0.000000000000000000, -0.000000000000000000 ) ) ;
#36113=DIRECTION ( 'NONE',  ( 0.000000000000000000, 0.000000000000000000, 1.000000000000000000 ) ) ;
#36115=DIRECTION ( 'NONE',  ( 0.000000000000000000, 0.9876883405951383255, -0.1564344650402276216 ) ) ;
#36121=LINE ( 'NONE', #41763, #18574 ) ;
#36122=AXIS2_PLACEMENT_3D ( 'NONE', #37509, #61551, #31478 ) ;
#36124=VECTOR ( 'NONE', #41553, 1000.000000000000000 ) ;
#36127=FACE_OUTER_BOUND ( 'NONE', #27070, .T. ) ;
#36145=DIRECTION ( 'NONE',  ( -1.000000000000000000, -0.000000000000000000, 0.000000000000000000 ) ) ;
#36151=ORIENTED_EDGE ( 'NONE', *, *, #5936, .F. ) ;
#36161=DIRECTION ( 'NONE',  ( -1.000000000000000000, 0.000000000000000000, -0.000000000000000000 ) ) ;
#36164=DIRECTION ( 'NONE',  ( 0.000000000000000000, 0.1564344650402311743, -0.9876883405951377704 ) ) ;
#36168=EDGE_CURVE ( 'NONE', #68917, #36728, #2424, .T. ) ;
#36173=ORIENTED_EDGE ( 'NONE', *, *, #49468, .T. ) ;
#36175=LINE ( 'NONE', #19253, #58789 ) ;
#36186=ORIENTED_EDGE ( 'NONE', *, *, #18105, .T. ) ;
#36198=CARTESIAN_POINT ( 'NONE',  ( 10.00000000000000000, 2.946379043146343246, 75.11764819372150725 ) ) ;
#36201=AXIS2_PLACEMENT_3D ( 'NONE', #5420, #38499, #61438 ) ;
#36204=CARTESIAN_POINT ( 'NONE',  ( 5.000000000000002665, -81.96053171279903893, 2.543863470248101333 ) ) ;
#36210=ADVANCED_FACE ( 'NONE', ( #52775 ), #35109, .T. ) ;
#36213=ORIENTED_EDGE ( 'NONE', *, *, #24208, .T. ) ;
#36217=EDGE_CURVE ( 'NONE', #36312, #39711, #62699, .T. ) ;
#36225=CARTESIAN_POINT ( 'NONE',  ( 0.000000000000000000, 0.000000000000000000, 0.000000000000000000 ) ) ;
#36229=FACE_OUTER_BOUND ( 'NONE', #33522, .T. ) ;
#36233=ORIENTED_EDGE ( 'NONE', *, *, #9151, .F. ) ;
#36235=AXIS2_PLACEMENT_3D ( 'NONE', #4878, #3755, #38694 ) ;
#36248=ORIENTED_EDGE ( 'NONE', *, *, #25484, .T. ) ;
#36253=DIRECTION ( 'NONE',  ( 0.000000000000000000, -0.8910065241883627918, -0.4539904997395567965 ) ) ;
#36254=AXIS2_PLACEMENT_3D ( 'NONE', #53140, #41130, #58039 ) ;
#36270=CARTESIAN_POINT ( 'NONE',  ( 10.00000000000000000, 46.53671651293948486, 59.03961581697416250 ) ) ;
#36278=CARTESIAN_POINT ( 'NONE',  ( 0.000000000000000000, -23.16143007188480496, 73.95703589263965227 ) ) ;
#36285=DIRECTION ( 'NONE',  ( 0.000000000000000000, -0.8526401643540970632, 0.5224985647159409163 ) ) ;
#36286=DIRECTION ( 'NONE',  ( -1.000000000000000000, -0.000000000000000000, 0.000000000000000000 ) ) ;
#36287=AXIS2_PLACEMENT_3D ( 'NONE', #46206, #23635, #12344 ) ;
#36292=DIRECTION ( 'NONE',  ( 0.000000000000000000, -0.8526401643540970632, 0.5224985647159411384 ) ) ;
#36293=FACE_OUTER_BOUND ( 'NONE', #35569, .T. ) ;
#36296=ADVANCED_FACE ( 'NONE', ( #2045 ), #8013, .T. ) ;
#36309=ORIENTED_EDGE ( 'NONE', *, *, #70849, .F. ) ;
#36312=VERTEX_POINT ( 'NONE', #27133 ) ;
#36316=CARTESIAN_POINT ( 'NONE',  ( 10.00000000000000000, -28.89263327155797967, 71.91182617369179297 ) ) ;
#36319=DIRECTION ( 'NONE',  ( -1.000000000000000000, -0.000000000000000000, -0.000000000000000000 ) ) ;
#36321=CARTESIAN_POINT ( 'NONE',  ( 5.000000000000002665, 71.87247863392471459, -39.47590169984770370 ) ) ;
#36322=CARTESIAN_POINT ( 'NONE',  ( 10.00000000000000000, -24.73286445877757345, 73.44644590900053061 ) ) ;
#36323=CARTESIAN_POINT ( 'NONE',  ( 10.00000000000000000, 75.11725578898467859, 2.956366410620910656 ) ) ;
#36326=DIRECTION ( 'NONE',  ( -1.000000000000000000, -0.000000000000000000, -0.000000000000000000 ) ) ;
#36329=ORIENTED_EDGE ( 'NONE', *, *, #46491, .T. ) ;
#36330=ORIENTED_EDGE ( 'NONE', *, *, #30769, .F. ) ;
#36348=CIRCLE ( 'NONE', #73576, 31.99999999999999289 ) ;
#36351=CYLINDRICAL_SURFACE ( 'NONE', #20585, 31.99999999999998579 ) ;
#36372=DIRECTION ( 'NONE',  ( 0.000000000000000000, -0.2334453638558922628, -0.9723699203976798877 ) ) ;
#36374=LINE ( 'NONE', #70953, #2484 ) ;
#36379=EDGE_CURVE ( 'NONE', #52599, #26527, #74213, .T. ) ;
#36380=EDGE_CURVE ( 'NONE', #12010, #975, #51393, .T. ) ;
#36393=LINE ( 'NONE', #64611, #9596 ) ;
#36403=CARTESIAN_POINT ( 'NONE',  ( 0.000000000000000000, 34.94270380257741948, -74.18225833017852722 ) ) ;
#36415=ORIENTED_EDGE ( 'NONE', *, *, #47878, .T. ) ;
#36424=CARTESIAN_POINT ( 'NONE',  ( 0.000000000000000000, -55.16347631943085617, 60.67117009219118273 ) ) ;
#36425=EDGE_CURVE ( 'NONE', #50699, #36763, #23012, .T. ) ;
#36430=VERTEX_POINT ( 'NONE', #50813 ) ;
#36442=ORIENTED_EDGE ( 'NONE', *, *, #44379, .T. ) ;
#36443=CARTESIAN_POINT ( 'NONE',  ( 0.000000000000000000, 65.58780272294076497, 36.73666225445916211 ) ) ;
#36449=DIRECTION ( 'NONE',  ( 0.000000000000000000, 0.000000000000000000, 1.000000000000000000 ) ) ;
#36471=EDGE_CURVE ( 'NONE', #2787, #29107, #46577, .T. ) ;
#36476=DIRECTION ( 'NONE',  ( 0.000000000000000000, 0.8910065241883655673, 0.4539904997395510233 ) ) ;
#36499=VERTEX_POINT ( 'NONE', #4986 ) ;
#36502=ORIENTED_EDGE ( 'NONE', *, *, #56477, .F. ) ;
#36505=EDGE_CURVE ( 'NONE', #64448, #32364, #53767, .T. ) ;
#36511=CYLINDRICAL_SURFACE ( 'NONE', #26880, 82.00000000000000000 ) ;
#36514=CARTESIAN_POINT ( 'NONE',  ( 10.00000000000000000, 68.55367621811204515, -44.99326035065983120 ) ) ;
#36515=EDGE_CURVE ( 'NONE', #34204, #28208, #5356, .T. ) ;
#36518=CARTESIAN_POINT ( 'NONE',  ( -10.00000000000000000, 0.000000000000000000, 0.000000000000000000 ) ) ;
#36537=ORIENTED_EDGE ( 'NONE', *, *, #6539, .T. ) ;
#36539=DIRECTION ( 'NONE',  ( -1.000000000000000000, -0.000000000000000000, -0.000000000000000000 ) ) ;
#36542=DIRECTION ( 'NONE',  ( -1.000000000000000000, -0.000000000000000000, -0.000000000000000000 ) ) ;
#36559=AXIS2_PLACEMENT_3D ( 'NONE', #59157, #42605, #60281 ) ;
#36565=DIRECTION ( 'NONE',  ( -1.000000000000000000, -0.000000000000000000, 0.000000000000000000 ) ) ;
#36568=CARTESIAN_POINT ( 'NONE',  ( 10.00000000000000000, -70.52718814184277107, 26.02418014898285037 ) ) ;
#36583=DIRECTION ( 'NONE',  ( 0.000000000000000000, 0.000000000000000000, 1.000000000000000000 ) ) ;
#36584=EDGE_CURVE ( 'NONE', #15045, #26436, #66958, .T. ) ;
#36585=CARTESIAN_POINT ( 'NONE',  ( 10.00000000000000000, 14.67089635893819377, -73.72996012237423713 ) ) ;
#36594=DIRECTION ( 'NONE',  ( -1.000000000000000000, -0.000000000000000000, -0.000000000000000000 ) ) ;
#36600=ORIENTED_EDGE ( 'NONE', *, *, #56644, .F. ) ;
#36612=VERTEX_POINT ( 'NONE', #41043 ) ;
#36616=ORIENTED_EDGE ( 'NONE', *, *, #59873, .F. ) ;
#36619=CARTESIAN_POINT ( 'NONE',  ( -10.00000000000000000, 0.000000000000000000, 0.000000000000000000 ) ) ;
#36620=CARTESIAN_POINT ( 'NONE',  ( 10.00000000000000000, 0.000000000000000000, 0.000000000000000000 ) ) ;
#36633=CARTESIAN_POINT ( 'NONE',  ( 10.00000000000000000, -74.65374052328644439, -8.840884882375878107 ) ) ;
#36645=EDGE_CURVE ( 'NONE', #47809, #73223, #71782, .T. ) ;
#36651=CARTESIAN_POINT ( 'NONE',  ( 10.00000000000000000, -46.53671651293991118, 59.03961581697383565 ) ) ;
#36659=ADVANCED_FACE ( 'NONE', ( #70686 ), #69602, .T. ) ;
#36660=CARTESIAN_POINT ( 'NONE',  ( 10.00000000000000000, 65.64334221924909230, 41.19522573413756561 ) ) ;
#36662=FACE_OUTER_BOUND ( 'NONE', #30952, .T. ) ;
#36676=VECTOR ( 'NONE', #15696, 1000.000000000000000 ) ;
#36690=ORIENTED_EDGE ( 'NONE', *, *, #2521, .F. ) ;
#36693=DIRECTION ( 'NONE',  ( -1.000000000000000000, -0.000000000000000000, 0.000000000000000000 ) ) ;
#36694=DIRECTION ( 'NONE',  ( 1.000000000000000000, -0.000000000000000000, -0.000000000000000000 ) ) ;
#36696=DIRECTION ( 'NONE',  ( 0.000000000000000000, 0.000000000000000000, 1.000000000000000000 ) ) ;
#36698=FACE_OUTER_BOUND ( 'NONE', #41602, .T. ) ;
#36700=ORIENTED_EDGE ( 'NONE', *, *, #59350, .F. ) ;
#36706=CARTESIAN_POINT ( 'NONE',  ( 10.00000000000000000, 0.000000000000000000, 0.000000000000000000 ) ) ;
#36718=VECTOR ( 'NONE', #7250, 1000.000000000000000 ) ;
#36722=CARTESIAN_POINT ( 'NONE',  ( 0.000000000000000000, -20.41045688087876897, 72.35160999960810102 ) ) ;
#36724=FACE_OUTER_BOUND ( 'NONE', #68988, .T. ) ;
#36725=AXIS2_PLACEMENT_3D ( 'NONE', #3184, #37745, #59947 ) ;
#36726=ORIENTED_EDGE ( 'NONE', *, *, #9402, .T. ) ;
#36728=VERTEX_POINT ( 'NONE', #71062 ) ;
#36730=AXIS2_PLACEMENT_3D ( 'NONE', #18985, #48312, #36285 ) ;
#36731=CARTESIAN_POINT ( 'NONE',  ( 10.00000000000000000, 0.000000000000000000, 0.000000000000000000 ) ) ;
#36744=VERTEX_POINT ( 'NONE', #71797 ) ;
#36746=DIRECTION ( 'NONE',  ( 0.000000000000000000, 0.9969173337331276308, 0.07845909572784864894 ) ) ;
#36752=FACE_OUTER_BOUND ( 'NONE', #74049, .T. ) ;
#36754=CARTESIAN_POINT ( 'NONE',  ( 10.00000000000000000, -77.32052557432837148, -5.256550761633697277 ) ) ;
#36758=VERTEX_POINT ( 'NONE', #54169 ) ;
#36760=DIRECTION ( 'NONE',  ( 0.000000000000000000, 0.6494480483301849905, -0.7604059656000299317 ) ) ;
#36763=VERTEX_POINT ( 'NONE', #25949 ) ;
#36765=ADVANCED_FACE ( 'NONE', ( #31954 ), #54891, .T. ) ;
#36768=CIRCLE ( 'NONE', #38005, 31.99999999999999289 ) ;
#36777=AXIS2_PLACEMENT_3D ( 'NONE', #37319, #8738, #22236 ) ;
#36781=ORIENTED_EDGE ( 'NONE', *, *, #67247, .F. ) ;
#36785=CARTESIAN_POINT ( 'NONE',  ( 0.000000000000000000, 0.000000000000000000, 2.500000000000000000 ) ) ;
#36796=DIRECTION ( 'NONE',  ( 0.000000000000000000, 0.000000000000000000, 1.000000000000000000 ) ) ;
#36804=EDGE_CURVE ( 'NONE', #26168, #3338, #15436, .T. ) ;
#36806=ORIENTED_EDGE ( 'NONE', *, *, #71336, .F. ) ;
#36818=DIRECTION ( 'NONE',  ( 0.000000000000000000, 0.2334453638559058630, -0.9723699203976765570 ) ) ;
#36833=CIRCLE ( 'NONE', #51276, 31.99999999999999645 ) ;
#36834=CARTESIAN_POINT ( 'NONE',  ( 10.00000000000000000, -21.60688246758641995, 79.10210256391358996 ) ) ;
#36837=LINE ( 'NONE', #42862, #16405 ) ;
#36841=AXIS2_PLACEMENT_3D ( 'NONE', #66894, #15386, #38327 ) ;
#36847=AXIS2_PLACEMENT_3D ( 'NONE', #69146, #754, #22166 ) ;
#36849=LINE ( 'NONE', #47757, #64659 ) ;
#36850=FACE_OUTER_BOUND ( 'NONE', #46994, .T. ) ;
#36854=AXIS2_PLACEMENT_3D ( 'NONE', #24489, #47425, #25591 ) ;
#36859=DIRECTION ( 'NONE',  ( 0.000000000000000000, 0.000000000000000000, 1.000000000000000000 ) ) ;
#36869=CIRCLE ( 'NONE', #71697, 31.99999999999999289 ) ;
#36877=VERTEX_POINT ( 'NONE', #31 ) ;
#36881=VERTEX_POINT ( 'NONE', #67664 ) ;
#36884=ORIENTED_EDGE ( 'NONE', *, *, #18987, .T. ) ;
#36919=FACE_OUTER_BOUND ( 'NONE', #20238, .T. ) ;
#36921=ADVANCED_FACE ( 'NONE', ( #13742 ), #23288, .T. ) ;
#36931=DIRECTION ( 'NONE',  ( 0.000000000000000000, 0.000000000000000000, 1.000000000000000000 ) ) ;
#36935=ORIENTED_EDGE ( 'NONE', *, *, #42435, .T. ) ;
#36943=DIRECTION ( 'NONE',  ( 0.000000000000000000, 0.000000000000000000, 1.000000000000000000 ) ) ;
#36953=DIRECTION ( 'NONE',  ( 0.000000000000000000, 0.000000000000000000, -1.000000000000000000 ) ) ;
#36956=ORIENTED_EDGE ( 'NONE', *, *, #4066, .T. ) ;
#36959=FACE_OUTER_BOUND ( 'NONE', #36027, .T. ) ;
#36973=DIRECTION ( 'NONE',  ( -1.000000000000000000, 0.000000000000000000, 0.000000000000000000 ) ) ;
#37000=ADVANCED_FACE ( 'NONE', ( #2878 ), #69508, .T. ) ;
#37009=DIRECTION ( 'NONE',  ( -1.000000000000000000, 0.000000000000000000, 0.000000000000000000 ) ) ;
#37020=CIRCLE ( 'NONE', #35823, 77.49899999999999523 ) ;
#37023=AXIS2_PLACEMENT_3D ( 'NONE', #47036, #18090, #24466 ) ;
#37027=CYLINDRICAL_SURFACE ( 'NONE', #38779, 32.00000000000000000 ) ;
#37028=DIRECTION ( 'NONE',  ( 0.000000000000000000, 0.000000000000000000, 1.000000000000000000 ) ) ;
#37042=( LENGTH_UNIT ( ) NAMED_UNIT ( * ) SI_UNIT ( .MILLI., .METRE. ) );
#37044=DIRECTION ( 'NONE',  ( -1.000000000000000000, 0.000000000000000000, -0.000000000000000000 ) ) ;
#37050=DIRECTION ( 'NONE',  ( -1.000000000000000000, 0.000000000000000000, -0.000000000000000000 ) ) ;
#37051=ORIENTED_EDGE ( 'NONE', *, *, #62259, .T. ) ;
#37054=CARTESIAN_POINT ( 'NONE',  ( 10.00000000000000000, -26.02418014898260878, -70.52718814184285634 ) ) ;
#37055=VECTOR ( 'NONE', #4594, 1000.000000000000000 ) ;
#37064=AXIS2_PLACEMENT_3D ( 'NONE', #42820, #3359, #43210 ) ;
#37068=AXIS2_PLACEMENT_3D ( 'NONE', #18547, #65537, #36953 ) ;
#37078=EDGE_CURVE ( 'NONE', #45162, #63903, #26274, .T. ) ;
#37097=ORIENTED_EDGE ( 'NONE', *, *, #23333, .F. ) ;
#37113=AXIS2_PLACEMENT_3D ( 'NONE', #8270, #3040, #18440 ) ;
#37115=CIRCLE ( 'NONE', #16721, 32.00000000000000000 ) ;
#37128=DIRECTION ( 'NONE',  ( -1.000000000000000000, 0.000000000000000000, 0.000000000000000000 ) ) ;
#37140=AXIS2_PLACEMENT_3D ( 'NONE', #58687, #7188, #47767 ) ;
#37143=CIRCLE ( 'NONE', #56355, 77.49900000000000944 ) ;
#37155=DIRECTION ( 'NONE',  ( -1.000000000000000000, 0.000000000000000000, -0.000000000000000000 ) ) ;
#37157=EDGE_CURVE ( 'NONE', #59272, #68833, #25047, .T. ) ;
#37161=AXIS2_PLACEMENT_3D ( 'NONE', #19301, #65184, #53890 ) ;
#37162=VERTEX_POINT ( 'NONE', #43463 ) ;
#37164=ORIENTED_EDGE ( 'NONE', *, *, #5278, .F. ) ;
#37166=DIRECTION ( 'NONE',  ( -1.000000000000000000, 0.000000000000000000, -0.000000000000000000 ) ) ;
#37172=CIRCLE ( 'NONE', #70751, 77.49900000000000944 ) ;
#37173=ORIENTED_EDGE ( 'NONE', *, *, #37078, .T. ) ;
#37176=ORIENTED_EDGE ( 'NONE', *, *, #12053, .F. ) ;
#37188=DIRECTION ( 'NONE',  ( -1.000000000000000000, -0.000000000000000000, 0.000000000000000000 ) ) ;
#37189=ORIENTED_EDGE ( 'NONE', *, *, #64858, .T. ) ;
#37196=FACE_OUTER_BOUND ( 'NONE', #21471, .T. ) ;
#37206=ORIENTED_EDGE ( 'NONE', *, *, #35075, .T. ) ;
#37214=AXIS2_PLACEMENT_3D ( 'NONE', #34238, #62843, #51528 ) ;
#37218=CARTESIAN_POINT ( 'NONE',  ( 10.00000000000000000, -75.16055320797043748, 18.89407956138229494 ) ) ;
#37223=CARTESIAN_POINT ( 'NONE',  ( 10.00000000000000000, 0.000000000000000000, 0.000000000000000000 ) ) ;
#37224=CARTESIAN_POINT ( 'NONE',  ( -10.00000000000000000, 0.000000000000000000, 0.000000000000000000 ) ) ;
#37229=DIRECTION ( 'NONE',  ( -1.000000000000000000, 0.000000000000000000, 0.000000000000000000 ) ) ;
#37230=CARTESIAN_POINT ( 'NONE',  ( 0.000000000000000000, 2.956366410621684260, -75.11725578898465017 ) ) ;
#37233=CIRCLE ( 'NONE', #56446, 31.99999999999998934 ) ;
#37245=CARTESIAN_POINT ( 'NONE',  ( 0.000000000000000000, 16.00000000000000000, -2.500000000000000000 ) ) ;
#37251=EDGE_CURVE ( 'NONE', #14220, #2716, #40028, .T. ) ;
#37252=EDGE_CURVE ( 'NONE', #57613, #30770, #16696, .T. ) ;
#37263=CIRCLE ( 'NONE', #60089, 82.00000000000000000 ) ;
#37265=ORIENTED_EDGE ( 'NONE', *, *, #12711, .T. ) ;
#37275=CARTESIAN_POINT ( 'NONE',  ( 10.00000000000000000, 62.20884554314020676, 46.21855187248652896 ) ) ;
#37282=ORIENTED_EDGE ( 'NONE', *, *, #66287, .F. ) ;
#37285=ORIENTED_EDGE ( 'NONE', *, *, #6109, .F. ) ;
#37293=DIRECTION ( 'NONE',  ( -1.000000000000000000, -0.000000000000000000, -0.000000000000000000 ) ) ;
#37297=AXIS2_PLACEMENT_3D ( 'NONE', #40025, #29453, #68602 ) ;
#37303=ADVANCED_FACE ( 'NONE', ( #73478 ), #67854, .T. ) ;
#37312=CYLINDRICAL_SURFACE ( 'NONE', #25373, 31.99999999999999289 ) ;
#37315=VERTEX_POINT ( 'NONE', #28733 ) ;
#37319=CARTESIAN_POINT ( 'NONE',  ( 10.00000000000000000, 51.03279382321088065, 55.19960302592086521 ) ) ;
#37326=CIRCLE ( 'NONE', #46929, 31.99999999999999289 ) ;
#37329=LINE ( 'NONE', #72256, #19056 ) ;
#37330=DIRECTION ( 'NONE',  ( 0.000000000000000000, 0.000000000000000000, 1.000000000000000000 ) ) ;
#37332=DIRECTION ( 'NONE',  ( 0.000000000000000000, 0.000000000000000000, 1.000000000000000000 ) ) ;
#37339=DIRECTION ( 'NONE',  ( 0.000000000000000000, -0.7071067811865536790, 0.7071067811865414665 ) ) ;
#37346=ADVANCED_FACE ( 'NONE', ( #63336 ), #34754, .T. ) ;
#37347=AXIS2_PLACEMENT_3D ( 'NONE', #71021, #20643, #14252 ) ;
#37354=DIRECTION ( 'NONE',  ( -1.000000000000000000, 0.000000000000000000, 0.000000000000000000 ) ) ;
#37355=ORIENTED_EDGE ( 'NONE', *, *, #27160, .F. ) ;
#37372=DIRECTION ( 'NONE',  ( 0.000000000000000000, -0.9969173337331270757, -0.07845909572785580988 ) ) ;
#37384=AXIS2_PLACEMENT_3D ( 'NONE', #32024, #49317, #13992 ) ;
#37388=CARTESIAN_POINT ( 'NONE',  ( -10.00000000000000000, 0.000000000000000000, 0.000000000000000000 ) ) ;
#37390=CARTESIAN_POINT ( 'NONE',  ( 10.00000000000000000, 0.000000000000000000, 0.000000000000000000 ) ) ;
#37406=VECTOR ( 'NONE', #61060, 1000.000000000000000 ) ;
#37407=CARTESIAN_POINT ( 'NONE',  ( 0.000000000000000000, -72.35160999960831418, 20.41045688087797672 ) ) ;
#37409=AXIS2_PLACEMENT_3D ( 'NONE', #7434, #60426, #54769 ) ;
#37416=DIRECTION ( 'NONE',  ( -1.000000000000000000, -0.000000000000000000, -0.000000000000000000 ) ) ;
#37417=CARTESIAN_POINT ( 'NONE',  ( 0.000000000000000000, 74.65491531819105830, 8.830959090343693418 ) ) ;
#37418=CIRCLE ( 'NONE', #28966, 31.99999999999999289 ) ;
#37428=CARTESIAN_POINT ( 'NONE',  ( 0.000000000000000000, 0.000000000000000000, 0.000000000000000000 ) ) ;
#37429=CARTESIAN_POINT ( 'NONE',  ( 0.000000000000000000, 0.000000000000000000, 0.000000000000000000 ) ) ;
#37432=CARTESIAN_POINT ( 'NONE',  ( 10.00000000000000000, 0.000000000000000000, 0.000000000000000000 ) ) ;
#37434=FACE_OUTER_BOUND ( 'NONE', #42078, .T. ) ;
#37436=AXIS2_PLACEMENT_3D ( 'NONE', #69924, #63571, #28224 ) ;
#37441=EDGE_CURVE ( 'NONE', #66307, #60509, #5487, .T. ) ;
#37456=DIRECTION ( 'NONE',  ( -1.000000000000000000, 0.000000000000000000, -0.000000000000000000 ) ) ;
#37457=CARTESIAN_POINT ( 'NONE',  ( 10.00000000000000000, 0.000000000000000000, 0.000000000000000000 ) ) ;
#37462=VERTEX_POINT ( 'NONE', #64075 ) ;
#37463=EDGE_LOOP ( 'NONE', ( #56708, #61014, #72541, #28308 ) ) ;
#37468=ADVANCED_FACE ( 'NONE', ( #64438 ), #18558, .T. ) ;
#37480=ORIENTED_EDGE ( 'NONE', *, *, #38718, .T. ) ;
#37486=DIRECTION ( 'NONE',  ( -1.000000000000000000, 0.000000000000000000, 0.000000000000000000 ) ) ;
#37492=ORIENTED_EDGE ( 'NONE', *, *, #27988, .T. ) ;
#37494=CIRCLE ( 'NONE', #36235, 82.00000000000000000 ) ;
#37497=VECTOR ( 'NONE', #40906, 1000.000000000000000 ) ;
#37499=ORIENTED_EDGE ( 'NONE', *, *, #16062, .F. ) ;
#37501=ORIENTED_EDGE ( 'NONE', *, *, #57833, .T. ) ;
#37505=FACE_OUTER_BOUND ( 'NONE', #50436, .T. ) ;
#37508=CARTESIAN_POINT ( 'NONE',  ( 0.000000000000000000, -29.01471420065617224, 76.69515212746007649 ) ) ;
#37509=CARTESIAN_POINT ( 'NONE',  ( 10.00000000000000000, -68.26794271651239399, -31.47745569255214093 ) ) ;
#37516=EDGE_CURVE ( 'NONE', #14919, #41093, #4252, .T. ) ;
#37519=EDGE_CURVE ( 'NONE', #70184, #62512, #72632, .T. ) ;
#37525=MANIFOLD_SOLID_BREP ( 'Cut-Extrude-Thin1', #35575 ) ;
#37535=AXIS2_PLACEMENT_3D ( 'NONE', #4128, #9366, #27020 ) ;
#37555=CARTESIAN_POINT ( 'NONE',  ( 5.000000000000002665, 79.10210256391398786, -21.60688246758503084 ) ) ;
#37562=ORIENTED_EDGE ( 'NONE', *, *, #13419, .T. ) ;
#37576=DIRECTION ( 'NONE',  ( 0.000000000000000000, 0.7071067811865436870, 0.7071067811865512365 ) ) ;
#37578=ORIENTED_EDGE ( 'NONE', *, *, #57967, .F. ) ;
#37583=DIRECTION ( 'NONE',  ( -1.000000000000000000, 0.000000000000000000, 0.000000000000000000 ) ) ;
#37595=DIRECTION ( 'NONE',  ( 0.000000000000000000, 0.000000000000000000, 1.000000000000000000 ) ) ;
#37596=CARTESIAN_POINT ( 'NONE',  ( 10.00000000000000000, -76.66974797899830207, -11.30684508768422170 ) ) ;
#37598=EDGE_CURVE ( 'NONE', #7305, #1988, #55366, .T. ) ;
#37610=ADVANCED_FACE ( 'NONE', ( #34653 ), #40296, .T. ) ;
#37619=ORIENTED_EDGE ( 'NONE', *, *, #19758, .T. ) ;
#37624=FACE_OUTER_BOUND ( 'NONE', #48394, .T. ) ;
#37631=ORIENTED_EDGE ( 'NONE', *, *, #71010, .F. ) ;
#37632=DIRECTION ( 'NONE',  ( 0.000000000000000000, 0.000000000000000000, 1.000000000000000000 ) ) ;
#37633=ORIENTED_EDGE ( 'NONE', *, *, #57980, .F. ) ;
#37635=AXIS2_PLACEMENT_3D ( 'NONE', #30310, #31425, #54731 ) ;
#37637=ORIENTED_EDGE ( 'NONE', *, *, #61371, .F. ) ;
#37638=DIRECTION ( 'NONE',  ( -1.000000000000000000, 0.000000000000000000, -0.000000000000000000 ) ) ;
#37642=EDGE_LOOP ( 'NONE', ( #27995, #32537, #28455, #69435 ) ) ;
#37643=CARTESIAN_POINT ( 'NONE',  ( 0.000000000000000000, 0.000000000000000000, 0.000000000000000000 ) ) ;
#37648=ORIENTED_EDGE ( 'NONE', *, *, #60536, .F. ) ;
#37657=CYLINDRICAL_SURFACE ( 'NONE', #30590, 82.00000000000000000 ) ;
#37661=ORIENTED_EDGE ( 'NONE', *, *, #70796, .T. ) ;
#37663=DIRECTION ( 'NONE',  ( -1.000000000000000000, 0.000000000000000000, 0.000000000000000000 ) ) ;
#37670=DIRECTION ( 'NONE',  ( 0.000000000000000000, -0.7604059656000369261, 0.6494480483301766638 ) ) ;
#37683=CARTESIAN_POINT ( 'NONE',  ( 0.000000000000000000, 59.75363087400153006, -56.15606465354897381 ) ) ;
#37685=DIRECTION ( 'NONE',  ( -1.000000000000000000, -0.000000000000000000, -0.000000000000000000 ) ) ;
#37711=DIRECTION ( 'NONE',  ( -1.000000000000000000, -0.000000000000000000, 0.000000000000000000 ) ) ;
#37712=CARTESIAN_POINT ( 'NONE',  ( 10.00000000000000000, 15.33399622253600292, -80.55351364060572905 ) ) ;
#37714=CIRCLE ( 'NONE', #28084, 77.49899999999999523 ) ;
#37716=DIRECTION ( 'NONE',  ( -1.000000000000000000, 0.000000000000000000, 0.000000000000000000 ) ) ;
#37717=ORIENTED_EDGE ( 'NONE', *, *, #58135, .F. ) ;
#37722=LINE ( 'NONE', #59918, #44831 ) ;
#37725=ORIENTED_EDGE ( 'NONE', *, *, #53060, .T. ) ;
#37726=DIRECTION ( 'NONE',  ( 0.000000000000000000, 0.8526401643540897357, 0.5224985647159527957 ) ) ;
#37732=ORIENTED_EDGE ( 'NONE', *, *, #69096, .T. ) ;
#37734=VERTEX_POINT ( 'NONE', #57224 ) ;
#37742=ORIENTED_EDGE ( 'NONE', *, *, #12053, .T. ) ;
#37745=DIRECTION ( 'NONE',  ( -1.000000000000000000, 0.000000000000000000, 0.000000000000000000 ) ) ;
#37747=CARTESIAN_POINT ( 'NONE',  ( 10.00000000000000000, 22.90783923731629912, 78.73519480814962890 ) ) ;
#37765=CIRCLE ( 'NONE', #1623, 31.99999999999999645 ) ;
#37770=EDGE_CURVE ( 'NONE', #14685, #11557, #46680, .T. ) ;
#37771=VERTEX_POINT ( 'NONE', #23739 ) ;
#37776=DIRECTION ( 'NONE',  ( -1.000000000000000000, -0.000000000000000000, -0.000000000000000000 ) ) ;
#37778=VECTOR ( 'NONE', #8204, 1000.000000000000000 ) ;
#37783=VERTEX_POINT ( 'NONE', #1961 ) ;
#37792=DIRECTION ( 'NONE',  ( 0.000000000000000000, 0.000000000000000000, 1.000000000000000000 ) ) ;
#37793=DIRECTION ( 'NONE',  ( -1.000000000000000000, 0.000000000000000000, 0.000000000000000000 ) ) ;
#37811=AXIS2_PLACEMENT_3D ( 'NONE', #39721, #28046, #20925 ) ;
#37813=AXIS2_PLACEMENT_3D ( 'NONE', #29040, #63649, #12118 ) ;
#37820=CYLINDRICAL_SURFACE ( 'NONE', #49596, 77.49899999999999523 ) ;
#37835=CARTESIAN_POINT ( 'NONE',  ( 0.000000000000000000, -65.59268652807183742, -36.72794159290312166 ) ) ;
#37847=CARTESIAN_POINT ( 'NONE',  ( 0.000000000000000000, -46.21855187248583974, -62.20884554314070414 ) ) ;
#37850=DIRECTION ( 'NONE',  ( -1.000000000000000000, -0.000000000000000000, 0.000000000000000000 ) ) ;
#37852=LINE ( 'NONE', #32185, #51539 ) ;
#37855=CARTESIAN_POINT ( 'NONE',  ( 0.000000000000000000, 77.19088730480524418, 6.903761155838049390 ) ) ;
#37867=VECTOR ( 'NONE', #60591, 1000.000000000000000 ) ;
#37873=DIRECTION ( 'NONE',  ( 1.000000000000000000, 0.000000000000000000, 0.000000000000000000 ) ) ;
#37875=CARTESIAN_POINT ( 'NONE',  ( 10.00000000000000000, -0.8261519478425671803, -77.49459641780887864 ) ) ;
#37876=DIRECTION ( 'NONE',  ( 0.000000000000000000, -0.2334453638558921795, -0.9723699203976797767 ) ) ;
#37888=ADVANCED_FACE ( 'NONE', ( #27056 ), #32330, .T. ) ;
#37892=ADVANCED_FACE ( 'NONE', ( #54178 ), #43640, .T. ) ;
#37901=CARTESIAN_POINT ( 'NONE',  ( 10.00000000000000000, 8.840884882375075193, 74.65374052328651544 ) ) ;
#37904=CIRCLE ( 'NONE', #46288, 82.00000000000000000 ) ;
#37908=DIRECTION ( 'NONE',  ( 0.000000000000000000, 0.000000000000000000, -1.000000000000000000 ) ) ;
#37920=EDGE_LOOP ( 'NONE', ( #62242, #19627, #2715, #18214 ) ) ;
#37923=AXIS2_PLACEMENT_3D ( 'NONE', #72338, #61068, #14076 ) ;
#37924=VERTEX_POINT ( 'NONE', #13925 ) ;
#37925=AXIS2_PLACEMENT_3D ( 'NONE', #539, #51990, #23436 ) ;
#37942=CARTESIAN_POINT ( 'NONE',  ( 0.000000000000000000, 0.000000000000000000, 0.000000000000000000 ) ) ;
#37956=ADVANCED_FACE ( 'NONE', ( #37624 ), #61294, .T. ) ;
#37958=ADVANCED_FACE ( 'NONE', ( #9037 ), #37983, .T. ) ;
#37965=EDGE_CURVE ( 'NONE', #41146, #59272, #72182, .T. ) ;
#37966=CARTESIAN_POINT ( 'NONE',  ( 0.000000000000000000, -20.40083707022829174, -72.35432306680507963 ) ) ;
#37967=CARTESIAN_POINT ( 'NONE',  ( -10.00000000000000000, 0.000000000000000000, 0.000000000000000000 ) ) ;
#37983=CYLINDRICAL_SURFACE ( 'NONE', #41580, 31.99999999999999289 ) ;
#37991=ORIENTED_EDGE ( 'NONE', *, *, #71010, .T. ) ;
#37997=VERTEX_POINT ( 'NONE', #8302 ) ;
#38001=CARTESIAN_POINT ( 'NONE',  ( 5.000000000000000000, 51.29473840253223926, 63.97538442413444670 ) ) ;
#38005=AXIS2_PLACEMENT_3D ( 'NONE', #19255, #42206, #65141 ) ;
#38013=VERTEX_POINT ( 'NONE', #11264 ) ;
#38017=AXIS2_PLACEMENT_3D ( 'NONE', #42868, #14281, #3042 ) ;
#38036=ORIENTED_EDGE ( 'NONE', *, *, #44509, .T. ) ;
#38047=DIRECTION ( 'NONE',  ( -1.000000000000000000, 0.000000000000000000, -0.000000000000000000 ) ) ;
#38060=LINE ( 'NONE', #72265, #56213 ) ;
#38080=CYLINDRICAL_SURFACE ( 'NONE', #47795, 31.99999999999999289 ) ;
#38081=AXIS2_PLACEMENT_3D ( 'NONE', #19764, #36693, #30672 ) ;
#38082=ORIENTED_EDGE ( 'NONE', *, *, #11773, .F. ) ;
#38083=ORIENTED_EDGE ( 'NONE', *, *, #49527, .F. ) ;
#38086=ORIENTED_EDGE ( 'NONE', *, *, #35385, .T. ) ;
#38088=CIRCLE ( 'NONE', #30886, 31.99999999999999289 ) ;
#38089=ADVANCED_FACE ( 'NONE', ( #73291 ), #56013, .T. ) ;
#38090=ORIENTED_EDGE ( 'NONE', *, *, #39408, .T. ) ;
#38095=EDGE_LOOP ( 'NONE', ( #16398, #3420, #7776, #62450 ) ) ;
#38098=ORIENTED_EDGE ( 'NONE', *, *, #10003, .T. ) ;
#38102=DIRECTION ( 'NONE',  ( -1.000000000000000000, 0.000000000000000000, -0.000000000000000000 ) ) ;
#38107=CYLINDRICAL_SURFACE ( 'NONE', #15626, 82.00000000000000000 ) ;
#38109=CYLINDRICAL_SURFACE ( 'NONE', #69889, 77.49899999999999523 ) ;
#38122=LINE ( 'NONE', #16306, #10983 ) ;
#38124=ORIENTED_EDGE ( 'NONE', *, *, #13058, .T. ) ;
#38128=EDGE_CURVE ( 'NONE', #14220, #21993, #51232, .T. ) ;
#38129=CYLINDRICAL_SURFACE ( 'NONE', #37923, 77.49899999999999523 ) ;
#38135=FACE_OUTER_BOUND ( 'NONE', #50005, .T. ) ;
#38138=ORIENTED_EDGE ( 'NONE', *, *, #52515, .T. ) ;
#38162=CIRCLE ( 'NONE', #20124, 31.99999999999999289 ) ;
#38175=ADVANCED_FACE ( 'NONE', ( #59351 ), #41681, .F. ) ;
#38176=CARTESIAN_POINT ( 'NONE',  ( 10.00000000000000000, 71.91182617369230456, -28.89263327155667938 ) ) ;
#38181=ORIENTED_EDGE ( 'NONE', *, *, #48698, .T. ) ;
#38182=ADVANCED_FACE ( 'NONE', ( #58600 ), #35310, .T. ) ;
#38187=AXIS2_PLACEMENT_3D ( 'NONE', #20522, #20137, #42351 ) ;
#38190=AXIS2_PLACEMENT_3D ( 'NONE', #349, #57084, #33764 ) ;
#38196=VERTEX_POINT ( 'NONE', #52223 ) ;
#38208=DIRECTION ( 'NONE',  ( 0.000000000000000000, -0.6494480483301739993, -0.7604059656000390355 ) ) ;
#38209=DIRECTION ( 'NONE',  ( 0.000000000000000000, 0.5877852522924684742, 0.8090169943749506709 ) ) ;
#38210=ORIENTED_EDGE ( 'NONE', *, *, #65536, .T. ) ;
#38211=DIRECTION ( 'NONE',  ( 0.000000000000000000, 0.000000000000000000, 1.000000000000000000 ) ) ;
#38213=VERTEX_POINT ( 'NONE', #30025 ) ;
#38221=ORIENTED_EDGE ( 'NONE', *, *, #56377, .F. ) ;
#38223=CARTESIAN_POINT ( 'NONE',  ( 0.000000000000000000, 0.000000000000000000, 0.000000000000000000 ) ) ;
#38226=VECTOR ( 'NONE', #12802, 1000.000000000000000 ) ;
#38229=AXIS2_PLACEMENT_3D ( 'NONE', #65237, #49034, #13710 ) ;
#38239=DIRECTION ( 'NONE',  ( -1.000000000000000000, -0.000000000000000000, 0.000000000000000000 ) ) ;
#38242=ORIENTED_EDGE ( 'NONE', *, *, #55783, .T. ) ;
#38245=AXIS2_PLACEMENT_3D ( 'NONE', #64734, #48177, #47802 ) ;
#38250=AXIS2_PLACEMENT_3D ( 'NONE', #42149, #41398, #479 ) ;
#38262=AXIS2_PLACEMENT_3D ( 'NONE', #48284, #3922, #21171 ) ;
#38266=CYLINDRICAL_SURFACE ( 'NONE', #26684, 31.99999999999999289 ) ;
#38268=CARTESIAN_POINT ( 'NONE',  ( 10.00000000000000000, -71.87247863392443037, 39.47590169984818687 ) ) ;
#38273=VERTEX_POINT ( 'NONE', #36403 ) ;
#38275=ORIENTED_EDGE ( 'NONE', *, *, #19019, .F. ) ;
#38277=CYLINDRICAL_SURFACE ( 'NONE', #30960, 31.99999999999999289 ) ;
#38279=CARTESIAN_POINT ( 'NONE',  ( 10.00000000000000000, 20.41045688087930898, -72.35160999960793049 ) ) ;
#38287=ORIENTED_EDGE ( 'NONE', *, *, #73845, .T. ) ;
#38289=EDGE_LOOP ( 'NONE', ( #49681, #18286, #19143, #47099 ) ) ;
#38296=CIRCLE ( 'NONE', #9472, 77.49900000000000944 ) ;
#38299=CARTESIAN_POINT ( 'NONE',  ( 10.00000000000000000, 71.87247863392470038, -39.47590169984768238 ) ) ;
#38303=AXIS2_PLACEMENT_3D ( 'NONE', #18763, #48452, #40980 ) ;
#38312=VERTEX_POINT ( 'NONE', #72098 ) ;
#38315=ORIENTED_EDGE ( 'NONE', *, *, #10771, .T. ) ;
#38320=EDGE_CURVE ( 'NONE', #29404, #20435, #56009, .T. ) ;
#38327=DIRECTION ( 'NONE',  ( 0.000000000000000000, 0.1564344650402244852, 0.9876883405951387696 ) ) ;
#38342=DIRECTION ( 'NONE',  ( 0.000000000000000000, -0.9876883405951359940, -0.1564344650402420822 ) ) ;
#38343=CARTESIAN_POINT ( 'NONE',  ( 5.000000000000002665, 71.21200624218852226, -40.65526001592539984 ) ) ;
#38352=AXIS2_PLACEMENT_3D ( 'NONE', #50095, #38838, #57248 ) ;
#38353=EDGE_CURVE ( 'NONE', #975, #30680, #13833, .T. ) ;
#38354=ORIENTED_EDGE ( 'NONE', *, *, #11612, .F. ) ;
#38355=VECTOR ( 'NONE', #54525, 1000.000000000000000 ) ;
#38362=VERTEX_POINT ( 'NONE', #2619 ) ;
#38366=ORIENTED_EDGE ( 'NONE', *, *, #24208, .F. ) ;
#38371=CARTESIAN_POINT ( 'NONE',  ( 10.00000000000000000, 6.903761155837774943, 77.19088730480525840 ) ) ;
#38373=CARTESIAN_POINT ( 'NONE',  ( -10.00000000000000000, 0.000000000000000000, 0.000000000000000000 ) ) ;
#38377=CYLINDRICAL_SURFACE ( 'NONE', #2278, 32.00000000000000000 ) ;
#38381=ORIENTED_EDGE ( 'NONE', *, *, #26203, .F. ) ;
#38390=DIRECTION ( 'NONE',  ( -1.000000000000000000, -0.000000000000000000, -0.000000000000000000 ) ) ;
#38392=VERTEX_POINT ( 'NONE', #49171 ) ;
#38402=DIRECTION ( 'NONE',  ( 0.000000000000000000, 0.000000000000000000, 1.000000000000000000 ) ) ;
#38405=CARTESIAN_POINT ( 'NONE',  ( 10.00000000000000000, 59.03961581697465277, -46.53671651293886669 ) ) ;
#38412=AXIS2_PLACEMENT_3D ( 'NONE', #13962, #25628, #41440 ) ;
#38416=AXIS2_PLACEMENT_3D ( 'NONE', #41429, #12110, #35049 ) ;
#38421=DIRECTION ( 'NONE',  ( -1.000000000000000000, 0.000000000000000000, -0.000000000000000000 ) ) ;
#38428=DIRECTION ( 'NONE',  ( 0.000000000000000000, -0.9723699203976789995, 0.2334453638558956212 ) ) ;
#38439=CIRCLE ( 'NONE', #44399, 77.49900000000000944 ) ;
#38444=CARTESIAN_POINT ( 'NONE',  ( 10.00000000000000000, 55.19960302592141232, -51.03279382321027668 ) ) ;
#38454=AXIS2_PLACEMENT_3D ( 'NONE', #53851, #14370, #63767 ) ;
#38458=CYLINDRICAL_SURFACE ( 'NONE', #57666, 31.99999999999998579 ) ;
#38461=VECTOR ( 'NONE', #48974, 1000.000000000000000 ) ;
#38462=ORIENTED_EDGE ( 'NONE', *, *, #25299, .F. ) ;
#38465=EDGE_CURVE ( 'NONE', #72369, #34053, #4824, .T. ) ;
#38466=VERTEX_POINT ( 'NONE', #26972 ) ;
#38470=DIRECTION ( 'NONE',  ( -1.000000000000000000, 0.000000000000000000, 0.000000000000000000 ) ) ;
#38478=ADVANCED_FACE ( 'NONE', ( #68331 ), #72822, .T. ) ;
#38497=LINE ( 'NONE', #3204, #71508 ) ;
#38498=CIRCLE ( 'NONE', #40863, 82.00000000000000000 ) ;
#38499=DIRECTION ( 'NONE',  ( -1.000000000000000000, 0.000000000000000000, -0.000000000000000000 ) ) ;
#38502=EDGE_LOOP ( 'NONE', ( #63674, #5303, #51820, #49720 ) ) ;
#38503=ORIENTED_EDGE ( 'NONE', *, *, #4932, .T. ) ;
#38506=LINE ( 'NONE', #5428, #20187 ) ;
#38518=AXIS2_PLACEMENT_3D ( 'NONE', #73992, #55219, #9731 ) ;
#38525=AXIS2_PLACEMENT_3D ( 'NONE', #60087, #8567, #31485 ) ;
#38526=DIRECTION ( 'NONE',  ( 0.000000000000000000, 0.000000000000000000, 1.000000000000000000 ) ) ;
#38527=EDGE_CURVE ( 'NONE', #9035, #49393, #32060, .T. ) ;
#38530=ADVANCED_FACE ( 'NONE', ( #4443 ), #16446, .T. ) ;
#38544=CARTESIAN_POINT ( 'NONE',  ( 10.00000000000000000, 71.27951684758026829, 30.41916302227139113 ) ) ;
#38546=AXIS2_PLACEMENT_3D ( 'NONE', #44253, #55533, #10030 ) ;
#38548=CARTESIAN_POINT ( 'NONE',  ( 0.000000000000000000, -80.28980883073747066, -16.65972982745018172 ) ) ;
#38554=CARTESIAN_POINT ( 'NONE',  ( 0.000000000000000000, 0.000000000000000000, 0.000000000000000000 ) ) ;
#38572=AXIS2_PLACEMENT_3D ( 'NONE', #32507, #55447, #8849 ) ;
#38573=CARTESIAN_POINT ( 'NONE',  ( 10.00000000000000000, -75.11764819372145041, -2.946379043147127064 ) ) ;
#38576=EDGE_LOOP ( 'NONE', ( #46324, #46928, #38462, #51857 ) ) ;
#38586=DIRECTION ( 'NONE',  ( 0.000000000000000000, 0.2334453638559058908, -0.9723699203976764460 ) ) ;
#38598=DIRECTION ( 'NONE',  ( 0.000000000000000000, 0.000000000000000000, 1.000000000000000000 ) ) ;
#38603=DIRECTION ( 'NONE',  ( -1.000000000000000000, 0.000000000000000000, 0.000000000000000000 ) ) ;
#38604=VERTEX_POINT ( 'NONE', #18655 ) ;
#38609=AXIS2_PLACEMENT_3D ( 'NONE', #2769, #42959, #60259 ) ;
#38614=EDGE_CURVE ( 'NONE', #59685, #57988, #51289, .T. ) ;
#38624=CARTESIAN_POINT ( 'NONE',  ( 10.00000000000000000, 76.69515212746016175, 29.01471420065591289 ) ) ;
#38625=VERTEX_POINT ( 'NONE', #64535 ) ;
#38629=CARTESIAN_POINT ( 'NONE',  ( 10.00000000000000000, 65.58780272294076497, 36.73666225445916211 ) ) ;
#38641=VERTEX_POINT ( 'NONE', #12647 ) ;
#38647=DIRECTION ( 'NONE',  ( 0.000000000000000000, 0.000000000000000000, 1.000000000000000000 ) ) ;
#38648=EDGE_CURVE ( 'NONE', #3546, #52788, #29641, .T. ) ;
#38651=CIRCLE ( 'NONE', #11075, 31.99999999999999645 ) ;
#38655=VERTEX_POINT ( 'NONE', #1052 ) ;
#38668=CYLINDRICAL_SURFACE ( 'NONE', #29609, 31.99999999999999289 ) ;
#38678=AXIS2_PLACEMENT_3D ( 'NONE', #34787, #29133, #52070 ) ;
#38680=ORIENTED_EDGE ( 'NONE', *, *, #61188, .F. ) ;
#38682=LINE ( 'NONE', #15746, #28910 ) ;
#38683=ORIENTED_EDGE ( 'NONE', *, *, #7456, .F. ) ;
#38691=DIRECTION ( 'NONE',  ( -1.000000000000000000, 0.000000000000000000, -0.000000000000000000 ) ) ;
#38694=DIRECTION ( 'NONE',  ( 0.000000000000000000, 0.000000000000000000, 1.000000000000000000 ) ) ;
#38696=EDGE_CURVE ( 'NONE', #3338, #45145, #74095, .T. ) ;
#38706=CARTESIAN_POINT ( 'NONE',  ( 10.00000000000000000, 12.93880638057426502, -76.41127070299258150 ) ) ;
#38709=EDGE_CURVE ( 'NONE', #961, #5747, #11615, .T. ) ;
#38711=DIRECTION ( 'NONE',  ( 0.000000000000000000, -0.5877852522924625900, -0.8090169943749551118 ) ) ;
#38713=CARTESIAN_POINT ( 'NONE',  ( 10.00000000000000000, -8.840884882375609877, 74.65374052328647281 ) ) ;
#38714=VECTOR ( 'NONE', #45475, 1000.000000000000000 ) ;
#38716=AXIS2_PLACEMENT_3D ( 'NONE', #60341, #61070, #71590 ) ;
#38718=EDGE_CURVE ( 'NONE', #38841, #64894, #3622, .T. ) ;
#38721=FACE_OUTER_BOUND ( 'NONE', #48464, .T. ) ;
#38736=ADVANCED_FACE ( 'NONE', ( #66394 ), #14873, .T. ) ;
#38749=DIRECTION ( 'NONE',  ( 0.000000000000000000, 0.000000000000000000, 1.000000000000000000 ) ) ;
#38751=CARTESIAN_POINT ( 'NONE',  ( 10.00000000000000000, 5.256550761632864166, 77.32052557432842832 ) ) ;
#38754=ORIENTED_EDGE ( 'NONE', *, *, #6887, .F. ) ;
#38765=EDGE_LOOP ( 'NONE', ( #68426, #53750, #5306, #71913 ) ) ;
#38770=CARTESIAN_POINT ( 'NONE',  ( 10.00000000000000000, 0.000000000000000000, 0.000000000000000000 ) ) ;
#38776=EDGE_CURVE ( 'NONE', #71846, #43844, #21223, .T. ) ;
#38779=AXIS2_PLACEMENT_3D ( 'NONE', #14080, #30629, #65986 ) ;
#38782=CIRCLE ( 'NONE', #25571, 31.99999999999998579 ) ;
#38785=DIRECTION ( 'NONE',  ( 0.000000000000000000, 0.000000000000000000, 1.000000000000000000 ) ) ;
#38786=EDGE_CURVE ( 'NONE', #14607, #26543, #66024, .T. ) ;
#38790=DIRECTION ( 'NONE',  ( 0.000000000000000000, 0.9723699203976756689, 0.2334453638559094157 ) ) ;
#38795=CARTESIAN_POINT ( 'NONE',  ( 10.00000000000000000, -68.67312586194971402, -35.91791733033549860 ) ) ;
#38796=DIRECTION ( 'NONE',  ( -1.000000000000000000, 0.000000000000000000, -0.000000000000000000 ) ) ;
#38805=DIRECTION ( 'NONE',  ( -1.000000000000000000, -0.000000000000000000, 0.000000000000000000 ) ) ;
#38806=ORIENTED_EDGE ( 'NONE', *, *, #34990, .T. ) ;
#38830=DIRECTION ( 'NONE',  ( 0.000000000000000000, -0.1564344650402170744, -0.9876883405951399908 ) ) ;
#38838=DIRECTION ( 'NONE',  ( -1.000000000000000000, 0.000000000000000000, -0.000000000000000000 ) ) ;
#38839=FACE_OUTER_BOUND ( 'NONE', #11711, .T. ) ;
#38840=ORIENTED_EDGE ( 'NONE', *, *, #27702, .T. ) ;
#38841=VERTEX_POINT ( 'NONE', #51213 ) ;
#38844=ORIENTED_EDGE ( 'NONE', *, *, #41493, .F. ) ;
#38848=DIRECTION ( 'NONE',  ( -1.000000000000000000, 0.000000000000000000, -0.000000000000000000 ) ) ;
#38851=DIRECTION ( 'NONE',  ( -1.000000000000000000, 0.000000000000000000, 0.000000000000000000 ) ) ;
#38852=CARTESIAN_POINT ( 'NONE',  ( 10.00000000000000000, 41.19522573413826194, -65.64334221924865176 ) ) ;
#38864=DIRECTION ( 'NONE',  ( 0.000000000000000000, 0.3826834323650842862, 0.9238795325112890700 ) ) ;
#38868=EDGE_CURVE ( 'NONE', #44570, #62914, #9310, .T. ) ;
#38869=CARTESIAN_POINT ( 'NONE',  ( 0.000000000000000000, 44.88180994100376608, 63.18004540533043922 ) ) ;
#38872=AXIS2_PLACEMENT_3D ( 'NONE', #39390, #28461, #74333 ) ;
#38873=EDGE_CURVE ( 'NONE', #64448, #33698, #12907, .T. ) ;
#38885=CIRCLE ( 'NONE', #56928, 82.00000000000000000 ) ;
#38888=DIRECTION ( 'NONE',  ( 0.000000000000000000, 0.9723699203976773342, -0.2334453638559023381 ) ) ;
#38889=VECTOR ( 'NONE', #48401, 1000.000000000000000 ) ;
#38901=CYLINDRICAL_SURFACE ( 'NONE', #12210, 31.99999999999999289 ) ;
#38915=DIRECTION ( 'NONE',  ( 0.000000000000000000, 0.000000000000000000, 1.000000000000000000 ) ) ;
#38921=ORIENTED_EDGE ( 'NONE', *, *, #40951, .F. ) ;
#38925=CARTESIAN_POINT ( 'NONE',  ( 10.00000000000000000, 39.47590169984845687, 71.87247863392427405 ) ) ;
#38926=AXIS2_PLACEMENT_3D ( 'NONE', #5205, #40503, #35233 ) ;
#38927=DIRECTION ( 'NONE',  ( -1.000000000000000000, -0.000000000000000000, -0.000000000000000000 ) ) ;
#38932=VERTEX_POINT ( 'NONE', #38176 ) ;
#38933=ORIENTED_EDGE ( 'NONE', *, *, #39338, .T. ) ;
#38944=EDGE_CURVE ( 'NONE', #72748, #33646, #5746, .T. ) ;
#38950=EDGE_CURVE ( 'NONE', #63017, #1988, #504, .T. ) ;
#38951=EDGE_LOOP ( 'NONE', ( #7593, #71559, #20459, #15425 ) ) ;
#38958=AXIS2_PLACEMENT_3D ( 'NONE', #19694, #20063, #20451 ) ;
#38972=DIRECTION ( 'NONE',  ( -1.000000000000000000, -0.000000000000000000, -0.000000000000000000 ) ) ;
#38979=DIRECTION ( 'NONE',  ( 0.000000000000000000, 0.000000000000000000, 1.000000000000000000 ) ) ;
#38987=CARTESIAN_POINT ( 'NONE',  ( 10.00000000000000000, -44.99326035066101781, 68.55367621811129197 ) ) ;
#38999=CIRCLE ( 'NONE', #73808, 31.99999999999999289 ) ;
#39002=VERTEX_POINT ( 'NONE', #38268 ) ;
#39007=AXIS2_PLACEMENT_3D ( 'NONE', #46533, #56723, #11568 ) ;
#39016=FACE_OUTER_BOUND ( 'NONE', #56122, .T. ) ;
#39025=DIRECTION ( 'NONE',  ( -1.000000000000000000, -0.000000000000000000, -0.000000000000000000 ) ) ;
#39027=VERTEX_POINT ( 'NONE', #66843 ) ;
#39035=DIRECTION ( 'NONE',  ( -1.000000000000000000, -0.000000000000000000, -0.000000000000000000 ) ) ;
#39037=CARTESIAN_POINT ( 'NONE',  ( 10.00000000000000000, 10.30890764327382847, 81.34940948281339956 ) ) ;
#39046=CARTESIAN_POINT ( 'NONE',  ( 10.00000000000000000, 0.000000000000000000, 0.000000000000000000 ) ) ;
#39048=ORIENTED_EDGE ( 'NONE', *, *, #73940, .T. ) ;
#39075=DIRECTION ( 'NONE',  ( -1.000000000000000000, 0.000000000000000000, -0.000000000000000000 ) ) ;
#39103=CIRCLE ( 'NONE', #67935, 77.49899999999999523 ) ;
#39106=CIRCLE ( 'NONE', #65525, 77.49899999999999523 ) ;
#39112=CARTESIAN_POINT ( 'NONE',  ( 10.00000000000000000, 14.67089635893713684, 73.72996012237443608 ) ) ;
#39122=FACE_OUTER_BOUND ( 'NONE', #51939, .T. ) ;
#39135=CYLINDRICAL_SURFACE ( 'NONE', #52897, 82.00000000000000000 ) ;
#39154=ORIENTED_EDGE ( 'NONE', *, *, #49246, .T. ) ;
#39164=EDGE_CURVE ( 'NONE', #59815, #26527, #10817, .T. ) ;
#39168=CARTESIAN_POINT ( 'NONE',  ( 0.000000000000000000, -50.23322058963298531, -64.81221759200398935 ) ) ;
#39169=DIRECTION ( 'NONE',  ( -1.000000000000000000, 0.000000000000000000, -0.000000000000000000 ) ) ;
#39177=ORIENTED_EDGE ( 'NONE', *, *, #38776, .T. ) ;
#39178=DIRECTION ( 'NONE',  ( 1.000000000000000000, -0.000000000000000000, -0.000000000000000000 ) ) ;
#39188=DIRECTION ( 'NONE',  ( -1.000000000000000000, 0.000000000000000000, 0.000000000000000000 ) ) ;
#39193=AXIS2_PLACEMENT_3D ( 'NONE', #72959, #15460, #39524 ) ;
#39195=EDGE_CURVE ( 'NONE', #25891, #54604, #24937, .T. ) ;
#39196=CARTESIAN_POINT ( 'NONE',  ( 10.00000000000000000, 34.94270380257741948, -74.18225833017854143 ) ) ;
#39199=ORIENTED_EDGE ( 'NONE', *, *, #10868, .T. ) ;
#39203=CIRCLE ( 'NONE', #65616, 31.99999999999999645 ) ;
#39204=ORIENTED_EDGE ( 'NONE', *, *, #38709, .F. ) ;
#39206=AXIS2_PLACEMENT_3D ( 'NONE', #31200, #49597, #54152 ) ;
#39225=DIRECTION ( 'NONE',  ( -1.000000000000000000, -0.000000000000000000, 0.000000000000000000 ) ) ;
#39230=DIRECTION ( 'NONE',  ( -1.000000000000000000, 0.000000000000000000, 0.000000000000000000 ) ) ;
#39241=DIRECTION ( 'NONE',  ( 0.000000000000000000, -0.9969173337331287410, 0.07845909572783486829 ) ) ;
#39246=DIRECTION ( 'NONE',  ( 0.000000000000000000, -0.8090169943749531134, 0.5877852522924653655 ) ) ;
#39247=EDGE_CURVE ( 'NONE', #20797, #26436, #27347, .T. ) ;
#39248=EDGE_CURVE ( 'NONE', #24726, #70, #39768, .T. ) ;
#39252=ORIENTED_EDGE ( 'NONE', *, *, #18019, .T. ) ;
#39256=DIRECTION ( 'NONE',  ( 1.000000000000000000, -0.000000000000000000, -0.000000000000000000 ) ) ;
#39266=DIRECTION ( 'NONE',  ( 0.000000000000000000, 0.000000000000000000, 1.000000000000000000 ) ) ;
#39289=FACE_OUTER_BOUND ( 'NONE', #54888, .T. ) ;
#39290=VERTEX_POINT ( 'NONE', #64180 ) ;
#39291=EDGE_CURVE ( 'NONE', #44444, #65198, #30313, .T. ) ;
#39308=ORIENTED_EDGE ( 'NONE', *, *, #11612, .T. ) ;
#39309=ORIENTED_EDGE ( 'NONE', *, *, #27425, .T. ) ;
#39318=EDGE_CURVE ( 'NONE', #55565, #52257, #69380, .T. ) ;
#39323=CARTESIAN_POINT ( 'NONE',  ( 10.00000000000000000, 72.35160999960844208, -20.41045688087747223 ) ) ;
#39331=CARTESIAN_POINT ( 'NONE',  ( 10.00000000000000000, 59.75363087400074846, 56.15606465354979804 ) ) ;
#39333=CARTESIAN_POINT ( 'NONE',  ( 5.000000000000002665, -39.47590169984793818, -71.87247863392457248 ) ) ;
#39338=EDGE_CURVE ( 'NONE', #17434, #64362, #20144, .T. ) ;
#39346=CARTESIAN_POINT ( 'NONE',  ( 10.00000000000000000, -81.96053171279902472, 2.543863470248087566 ) ) ;
#39348=VERTEX_POINT ( 'NONE', #12283 ) ;
#39350=ORIENTED_EDGE ( 'NONE', *, *, #4612, .F. ) ;
#39353=LINE ( 'NONE', #39731, #8110 ) ;
#39363=DIRECTION ( 'NONE',  ( 0.000000000000000000, 0.000000000000000000, 1.000000000000000000 ) ) ;
#39368=CARTESIAN_POINT ( 'NONE',  ( 10.00000000000000000, -62.50884508063395373, -41.76106447765554464 ) ) ;
#39374=DIRECTION ( 'NONE',  ( 0.000000000000000000, -0.8090169943749531134, 0.5877852522924653655 ) ) ;
#39375=CARTESIAN_POINT ( 'NONE',  ( 10.00000000000000000, -77.19088730480528682, 6.903761155837488062 ) ) ;
#39383=VERTEX_POINT ( 'NONE', #70519 ) ;
#39387=CARTESIAN_POINT ( 'NONE',  ( 10.00000000000000000, 0.000000000000000000, 0.000000000000000000 ) ) ;
#39388=CARTESIAN_POINT ( 'NONE',  ( 0.000000000000000000, 0.000000000000000000, 0.000000000000000000 ) ) ;
#39390=CARTESIAN_POINT ( 'NONE',  ( 0.000000000000000000, 0.000000000000000000, 0.000000000000000000 ) ) ;
#39391=DIRECTION ( 'NONE',  ( 0.000000000000000000, 0.000000000000000000, 1.000000000000000000 ) ) ;
#39392=ADVANCED_FACE ( 'NONE', ( #23949 ), #18660, .T. ) ;
#39407=ORIENTED_EDGE ( 'NONE', *, *, #61992, .F. ) ;
#39408=EDGE_CURVE ( 'NONE', #11928, #28623, #70584, .T. ) ;
#39409=DIRECTION ( 'NONE',  ( -1.000000000000000000, 0.000000000000000000, -0.000000000000000000 ) ) ;
#39419=CARTESIAN_POINT ( 'NONE',  ( 10.00000000000000000, 14.67089635893819377, -73.72996012237423713 ) ) ;
#39421=EDGE_LOOP ( 'NONE', ( #56607, #57173, #40300, #40529 ) ) ;
#39425=VERTEX_POINT ( 'NONE', #41236 ) ;
#39443=DIRECTION ( 'NONE',  ( 0.000000000000000000, 0.000000000000000000, 1.000000000000000000 ) ) ;
#39449=AXIS2_PLACEMENT_3D ( 'NONE', #51678, #18201, #226 ) ;
#39459=DIRECTION ( 'NONE',  ( -1.000000000000000000, 0.000000000000000000, -0.000000000000000000 ) ) ;
#39471=EDGE_CURVE ( 'NONE', #11405, #21157, #22584, .T. ) ;
#39475=AXIS2_PLACEMENT_3D ( 'NONE', #41397, #29362, #52307 ) ;
#39483=ORIENTED_EDGE ( 'NONE', *, *, #6109, .T. ) ;
#39490=ORIENTED_EDGE ( 'NONE', *, *, #72396, .F. ) ;
#39499=ORIENTED_EDGE ( 'NONE', *, *, #25537, .T. ) ;
#39503=VECTOR ( 'NONE', #39662, 1000.000000000000000 ) ;
#39505=EDGE_CURVE ( 'NONE', #72748, #8336, #1002, .T. ) ;
#39524=DIRECTION ( 'NONE',  ( 0.000000000000000000, 0.1564344650402242631, 0.9876883405951387696 ) ) ;
#39529=DIRECTION ( 'NONE',  ( 1.000000000000000000, -0.000000000000000000, -0.000000000000000000 ) ) ;
#39531=VECTOR ( 'NONE', #13094, 1000.000000000000000 ) ;
#39554=CARTESIAN_POINT ( 'NONE',  ( 10.00000000000000000, -81.90746397400391743, 3.894527615417593847 ) ) ;
#39557=DIRECTION ( 'NONE',  ( 1.000000000000000000, -0.000000000000000000, -0.000000000000000000 ) ) ;
#39563=ORIENTED_EDGE ( 'NONE', *, *, #35904, .F. ) ;
#39580=ADVANCED_FACE ( 'NONE', ( #36698 ), #25428, .T. ) ;
#39587=VERTEX_POINT ( 'NONE', #60025 ) ;
#39612=CARTESIAN_POINT ( 'NONE',  ( 10.00000000000000000, 59.75363087400152295, -56.15606465354897381 ) ) ;
#39618=FACE_OUTER_BOUND ( 'NONE', #20433, .T. ) ;
#39619=CARTESIAN_POINT ( 'NONE',  ( 10.00000000000000000, -8.830959090342926032, 74.65491531819115778 ) ) ;
#39642=AXIS2_PLACEMENT_3D ( 'NONE', #25554, #42857, #12788 ) ;
#39654=DIRECTION ( 'NONE',  ( 0.000000000000000000, 0.9723699203976756689, 0.2334453638559095268 ) ) ;
#39656=AXIS2_PLACEMENT_3D ( 'NONE', #66347, #14820, #15933 ) ;
#39662=DIRECTION ( 'NONE',  ( -1.000000000000000000, -0.000000000000000000, 0.000000000000000000 ) ) ;
#39666=EDGE_CURVE ( 'NONE', #53610, #38273, #68247, .T. ) ;
#39677=CYLINDRICAL_SURFACE ( 'NONE', #5256, 31.99999999999999289 ) ;
#39685=CIRCLE ( 'NONE', #62502, 77.49900000000000944 ) ;
#39689=VECTOR ( 'NONE', #63050, 1000.000000000000000 ) ;
#39693=CIRCLE ( 'NONE', #16717, 77.49900000000000944 ) ;
#39697=EDGE_LOOP ( 'NONE', ( #48066, #60689, #1549, #21986 ) ) ;
#39708=CARTESIAN_POINT ( 'NONE',  ( -10.00000000000000000, 0.000000000000000000, 0.000000000000000000 ) ) ;
#39711=VERTEX_POINT ( 'NONE', #6487 ) ;
#39721=CARTESIAN_POINT ( 'NONE',  ( 0.000000000000000000, 0.000000000000000000, 0.000000000000000000 ) ) ;
#39731=CARTESIAN_POINT ( 'NONE',  ( 5.000000000000002665, 68.55367621811205936, -44.99326035065983120 ) ) ;
#39732=CARTESIAN_POINT ( 'NONE',  ( 10.00000000000000000, -68.27212725128298132, 31.46837873494953541 ) ) ;
#39740=DIRECTION ( 'NONE',  ( 0.000000000000000000, -0.8090169943749532244, 0.5877852522924652545 ) ) ;
#39742=DIRECTION ( 'NONE',  ( -1.000000000000000000, 0.000000000000000000, -0.000000000000000000 ) ) ;
#39746=DIRECTION ( 'NONE',  ( -1.000000000000000000, 0.000000000000000000, 0.000000000000000000 ) ) ;
#39758=EDGE_CURVE ( 'NONE', #53775, #44963, #25252, .T. ) ;
#39760=AXIS2_PLACEMENT_3D ( 'NONE', #47287, #70190, #18696 ) ;
#39763=ORIENTED_EDGE ( 'NONE', *, *, #74325, .F. ) ;
#39768=LINE ( 'NONE', #62715, #58586 ) ;
#39770=ORIENTED_EDGE ( 'NONE', *, *, #4268, .F. ) ;
#39774=ORIENTED_EDGE ( 'NONE', *, *, #33078, .T. ) ;
#39783=VERTEX_POINT ( 'NONE', #7945 ) ;
#39785=EDGE_LOOP ( 'NONE', ( #36884, #18645, #6577, #29914 ) ) ;
#39789=ORIENTED_EDGE ( 'NONE', *, *, #69141, .F. ) ;
#39808=VERTEX_POINT ( 'NONE', #36514 ) ;
#39813=EDGE_CURVE ( 'NONE', #7419, #42721, #24871, .T. ) ;
#39826=EDGE_CURVE ( 'NONE', #65198, #58172, #4619, .T. ) ;
#39831=EDGE_CURVE ( 'NONE', #52760, #60509, #41426, .T. ) ;
#39834=CARTESIAN_POINT ( 'NONE',  ( 5.000000000000000000, -55.16347631942998220, -60.67117009219196433 ) ) ;
#39839=EDGE_CURVE ( 'NONE', #54928, #61657, #5848, .T. ) ;
#39861=ORIENTED_EDGE ( 'NONE', *, *, #58852, .F. ) ;
#39868=DIRECTION ( 'NONE',  ( -1.000000000000000000, -0.000000000000000000, -0.000000000000000000 ) ) ;
#39869=VECTOR ( 'NONE', #74216, 1000.000000000000000 ) ;
#39870=ORIENTED_EDGE ( 'NONE', *, *, #9579, .T. ) ;
#39874=DIRECTION ( 'NONE',  ( 0.000000000000000000, 0.000000000000000000, 1.000000000000000000 ) ) ;
#39875=VERTEX_POINT ( 'NONE', #13583 ) ;
#39877=ORIENTED_EDGE ( 'NONE', *, *, #11530, .T. ) ;
#39879=ORIENTED_EDGE ( 'NONE', *, *, #47117, .F. ) ;
#39881=DIRECTION ( 'NONE',  ( -1.000000000000000000, -0.000000000000000000, -0.000000000000000000 ) ) ;
#39885=EDGE_CURVE ( 'NONE', #37783, #72369, #62247, .T. ) ;
#39886=CARTESIAN_POINT ( 'NONE',  ( 10.00000000000000000, 0.000000000000000000, 0.000000000000000000 ) ) ;
#39890=ORIENTED_EDGE ( 'NONE', *, *, #43330, .F. ) ;
#39894=FACE_OUTER_BOUND ( 'NONE', #50446, .T. ) ;
#39898=CARTESIAN_POINT ( 'NONE',  ( 0.000000000000000000, 0.000000000000000000, 0.000000000000000000 ) ) ;
#39903=CIRCLE ( 'NONE', #59054, 31.99999999999998934 ) ;
#39920=DIRECTION ( 'NONE',  ( 0.000000000000000000, 0.000000000000000000, 1.000000000000000000 ) ) ;
#39922=LINE ( 'NONE', #6803, #50237 ) ;
#39923=CARTESIAN_POINT ( 'NONE',  ( 0.000000000000000000, 73.73191006444551476, 14.66109333815590254 ) ) ;
#39927=DIRECTION ( 'NONE',  ( -1.000000000000000000, 0.000000000000000000, 0.000000000000000000 ) ) ;
#39929=VERTEX_POINT ( 'NONE', #72204 ) ;
#39935=ORIENTED_EDGE ( 'NONE', *, *, #13761, .T. ) ;
#39944=DIRECTION ( 'NONE',  ( -1.000000000000000000, -0.000000000000000000, 0.000000000000000000 ) ) ;
#39957=CARTESIAN_POINT ( 'NONE',  ( 10.00000000000000000, 68.27212725128275395, 31.46837873495001503 ) ) ;
#39976=ORIENTED_EDGE ( 'NONE', *, *, #27993, .T. ) ;
#39986=EDGE_CURVE ( 'NONE', #71349, #46909, #71819, .T. ) ;
#39989=DIRECTION ( 'NONE',  ( -1.000000000000000000, 0.000000000000000000, 0.000000000000000000 ) ) ;
#40005=DIRECTION ( 'NONE',  ( 0.000000000000000000, -0.3090169943749349613, -0.9510565162951576390 ) ) ;
#40011=EDGE_CURVE ( 'NONE', #30579, #54289, #15063, .T. ) ;
#40020=DIRECTION ( 'NONE',  ( 0.000000000000000000, 0.000000000000000000, 1.000000000000000000 ) ) ;
#40025=CARTESIAN_POINT ( 'NONE',  ( 0.000000000000000000, 36.73666225445894185, 65.58780272294090707 ) ) ;
#40028=LINE ( 'NONE', #62218, #39503 ) ;
#40044=ORIENTED_EDGE ( 'NONE', *, *, #48708, .T. ) ;
#40049=LINE ( 'NONE', #67882, #15860 ) ;
#40051=ADVANCED_FACE ( 'NONE', ( #9427 ), #38377, .T. ) ;
#40067=CARTESIAN_POINT ( 'NONE',  ( 0.000000000000000000, 0.000000000000000000, 0.000000000000000000 ) ) ;
#40075=VECTOR ( 'NONE', #70127, 1000.000000000000000 ) ;
#40080=EDGE_CURVE ( 'NONE', #55666, #5845, #55044, .T. ) ;
#40088=CIRCLE ( 'NONE', #55696, 82.00000000000000000 ) ;
#40100=ADVANCED_FACE ( 'NONE', ( #68813 ), #29300, .T. ) ;
#40105=DIRECTION ( 'NONE',  ( 0.000000000000000000, 0.000000000000000000, 1.000000000000000000 ) ) ;
#40125=DIRECTION ( 'NONE',  ( 0.000000000000000000, -0.5224985647159559043, 0.8526401643540879594 ) ) ;
#40135=ORIENTED_EDGE ( 'NONE', *, *, #20211, .T. ) ;
#40144=ORIENTED_EDGE ( 'NONE', *, *, #25902, .F. ) ;
#40145=DIRECTION ( 'NONE',  ( -1.000000000000000000, 0.000000000000000000, 0.000000000000000000 ) ) ;
#40146=ORIENTED_EDGE ( 'NONE', *, *, #33424, .F. ) ;
#40149=ORIENTED_EDGE ( 'NONE', *, *, #47806, .F. ) ;
#40159=CARTESIAN_POINT ( 'NONE',  ( 10.00000000000000000, 30.41916302227216562, -71.27951684757994144 ) ) ;
#40165=ORIENTED_EDGE ( 'NONE', *, *, #36380, .F. ) ;
#40177=CARTESIAN_POINT ( 'NONE',  ( 0.000000000000000000, 11.30684508768452368, -76.66974797899824523 ) ) ;
#40178=EDGE_CURVE ( 'NONE', #52246, #72116, #51498, .T. ) ;
#40182=EDGE_CURVE ( 'NONE', #56093, #5647, #57522, .T. ) ;
#40183=AXIS2_PLACEMENT_3D ( 'NONE', #55453, #8853, #26869 ) ;
#40184=EDGE_CURVE ( 'NONE', #11833, #65189, #67111, .T. ) ;
#40187=DIRECTION ( 'NONE',  ( 1.000000000000000000, 0.000000000000000000, 0.000000000000000000 ) ) ;
#40188=DIRECTION ( 'NONE',  ( -1.000000000000000000, -0.000000000000000000, 0.000000000000000000 ) ) ;
#40190=FACE_OUTER_BOUND ( 'NONE', #66109, .T. ) ;
#40193=DIRECTION ( 'NONE',  ( -1.000000000000000000, 0.000000000000000000, 0.000000000000000000 ) ) ;
#40195=AXIS2_PLACEMENT_3D ( 'NONE', #20218, #66114, #19849 ) ;
#40196=LINE ( 'NONE', #28904, #41246 ) ;
#40197=CIRCLE ( 'NONE', #3030, 82.00000000000000000 ) ;
#40199=CARTESIAN_POINT ( 'NONE',  ( 0.000000000000000000, 58.39081064771823293, -50.95692526931266286 ) ) ;
#40205=CARTESIAN_POINT ( 'NONE',  ( 10.00000000000000000, -65.58780272294100655, 36.73666225445870737 ) ) ;
#40206=CARTESIAN_POINT ( 'NONE',  ( 0.000000000000000000, 0.000000000000000000, 0.000000000000000000 ) ) ;
#40211=CARTESIAN_POINT ( 'NONE',  ( 10.00000000000000000, 0.000000000000000000, 0.000000000000000000 ) ) ;
#40219=FACE_OUTER_BOUND ( 'NONE', #12740, .T. ) ;
#40221=VECTOR ( 'NONE', #41135, 1000.000000000000000 ) ;
#40226=CIRCLE ( 'NONE', #23595, 31.99999999999999645 ) ;
#40227=ORIENTED_EDGE ( 'NONE', *, *, #11930, .T. ) ;
#40230=ADVANCED_FACE ( 'NONE', ( #39122 ), #421, .T. ) ;
#40235=CARTESIAN_POINT ( 'NONE',  ( 10.00000000000000000, -20.41045688087772092, -72.35160999960838524 ) ) ;
#40236=VERTEX_POINT ( 'NONE', #36424 ) ;
#40237=AXIS2_PLACEMENT_3D ( 'NONE', #31449, #37850, #38208 ) ;
#40238=ORIENTED_EDGE ( 'NONE', *, *, #53073, .T. ) ;
#40243=ORIENTED_EDGE ( 'NONE', *, *, #48286, .F. ) ;
#40250=EDGE_CURVE ( 'NONE', #21255, #29678, #61113, .T. ) ;
#40259=CARTESIAN_POINT ( 'NONE',  ( 10.00000000000000000, 16.00000000000000000, 2.500000000000000000 ) ) ;
#40264=EDGE_CURVE ( 'NONE', #74142, #28208, #63539, .T. ) ;
#40268=LINE ( 'NONE', #41018, #66794 ) ;
#40275=CARTESIAN_POINT ( 'NONE',  ( 0.000000000000000000, 66.50666863322000211, 39.78640506895629159 ) ) ;
#40280=DIRECTION ( 'NONE',  ( 0.000000000000000000, 0.000000000000000000, 1.000000000000000000 ) ) ;
#40296=CYLINDRICAL_SURFACE ( 'NONE', #64344, 77.49899999999999523 ) ;
#40297=ORIENTED_EDGE ( 'NONE', *, *, #8897, .T. ) ;
#40300=ORIENTED_EDGE ( 'NONE', *, *, #34047, .F. ) ;
#40302=EDGE_CURVE ( 'NONE', #21993, #38841, #21424, .T. ) ;
#40313=LINE ( 'NONE', #40691, #74065 ) ;
#40314=ADVANCED_FACE ( 'NONE', ( #29662 ), #30409, .T. ) ;
#40317=DIRECTION ( 'NONE',  ( -1.000000000000000000, -0.000000000000000000, 0.000000000000000000 ) ) ;
#40324=CIRCLE ( 'NONE', #33121, 82.00000000000000000 ) ;
#40326=SHAPE_DEFINITION_REPRESENTATION ( #8545, #49787 ) ;
#40350=CARTESIAN_POINT ( 'NONE',  ( 10.00000000000000000, -71.91182617369207719, 28.89263327155721228 ) ) ;
#40351=DIRECTION ( 'NONE',  ( 0.000000000000000000, 0.9969173337331281859, -0.07845909572784168229 ) ) ;
#40354=VECTOR ( 'NONE', #52313, 1000.000000000000000 ) ;
#40363=ORIENTED_EDGE ( 'NONE', *, *, #10467, .F. ) ;
#40366=CARTESIAN_POINT ( 'NONE',  ( 10.00000000000000000, 14.66109333815564852, -73.73191006444555740 ) ) ;
#40373=ADVANCED_FACE ( 'NONE', ( #1895 ), #35332, .T. ) ;
#40379=CIRCLE ( 'NONE', #19972, 82.00000000000000000 ) ;
#40380=EDGE_CURVE ( 'NONE', #28623, #26543, #20254, .T. ) ;
#40388=ORIENTED_EDGE ( 'NONE', *, *, #72538, .T. ) ;
#40389=CIRCLE ( 'NONE', #7973, 31.99999999999999645 ) ;
#40396=EDGE_LOOP ( 'NONE', ( #67330, #58273, #10367, #62996 ) ) ;
#40397=ORIENTED_EDGE ( 'NONE', *, *, #50465, .F. ) ;
#40399=VERTEX_POINT ( 'NONE', #72117 ) ;
#40404=VERTEX_POINT ( 'NONE', #43580 ) ;
#40416=CARTESIAN_POINT ( 'NONE',  ( 0.000000000000000000, -41.19522573413687638, -65.64334221924953283 ) ) ;
#40420=ORIENTED_EDGE ( 'NONE', *, *, #33617, .F. ) ;
#40422=ADVANCED_FACE ( 'NONE', ( #15342 ), #49925, .T. ) ;
#40439=AXIS2_PLACEMENT_3D ( 'NONE', #48205, #36542, #71488 ) ;
#40450=CIRCLE ( 'NONE', #36847, 31.99999999999999289 ) ;
#40451=LINE ( 'NONE', #70118, #63120 ) ;
#40453=VECTOR ( 'NONE', #34107, 1000.000000000000000 ) ;
#40457=DIRECTION ( 'NONE',  ( 0.000000000000000000, 0.000000000000000000, 1.000000000000000000 ) ) ;
#40476=AXIS2_PLACEMENT_3D ( 'NONE', #16126, #72511, #68004 ) ;
#40483=VECTOR ( 'NONE', #6430, 1000.000000000000000 ) ;
#40490=CARTESIAN_POINT ( 'NONE',  ( 0.000000000000000000, 0.000000000000000000, 0.000000000000000000 ) ) ;
#40499=ORIENTED_EDGE ( 'NONE', *, *, #50909, .T. ) ;
#40501=VECTOR ( 'NONE', #16081, 1000.000000000000000 ) ;
#40503=DIRECTION ( 'NONE',  ( -1.000000000000000000, -0.000000000000000000, -0.000000000000000000 ) ) ;
#40507=AXIS2_PLACEMENT_3D ( 'NONE', #66672, #8042, #61778 ) ;
#40529=ORIENTED_EDGE ( 'NONE', *, *, #73303, .F. ) ;
#40556=EDGE_CURVE ( 'NONE', #1655, #65945, #31147, .T. ) ;
#40560=EDGE_CURVE ( 'NONE', #62877, #52333, #33510, .T. ) ;
#40566=VECTOR ( 'NONE', #55713, 1000.000000000000000 ) ;
#40568=AXIS2_PLACEMENT_3D ( 'NONE', #56097, #16243, #28255 ) ;
#40576=ORIENTED_EDGE ( 'NONE', *, *, #72713, .F. ) ;
#40585=ORIENTED_EDGE ( 'NONE', *, *, #61102, .T. ) ;
#40590=ORIENTED_EDGE ( 'NONE', *, *, #25407, .F. ) ;
#40596=DIRECTION ( 'NONE',  ( -1.000000000000000000, -0.000000000000000000, -0.000000000000000000 ) ) ;
#40604=CARTESIAN_POINT ( 'NONE',  ( 0.000000000000000000, 41.76106447765580043, -62.50884508063379741 ) ) ;
#40605=EDGE_CURVE ( 'NONE', #32327, #14220, #51557, .T. ) ;
#40608=ORIENTED_EDGE ( 'NONE', *, *, #67495, .T. ) ;
#40622=AXIS2_PLACEMENT_3D ( 'NONE', #10790, #33713, #39363 ) ;
#40624=ORIENTED_EDGE ( 'NONE', *, *, #61188, .T. ) ;
#40632=FACE_OUTER_BOUND ( 'NONE', #12333, .T. ) ;
#40639=CYLINDRICAL_SURFACE ( 'NONE', #2003, 31.99999999999999289 ) ;
#40644=ORIENTED_EDGE ( 'NONE', *, *, #21695, .F. ) ;
#40660=DIRECTION ( 'NONE',  ( 0.000000000000000000, 0.000000000000000000, -1.000000000000000000 ) ) ;
#40667=ADVANCED_FACE ( 'NONE', ( #10452 ), #57073, .T. ) ;
#40671=ORIENTED_EDGE ( 'NONE', *, *, #1905, .F. ) ;
#40675=ORIENTED_EDGE ( 'NONE', *, *, #54012, .T. ) ;
#40676=AXIS2_PLACEMENT_3D ( 'NONE', #46403, #17819, #29097 ) ;
#40683=DIRECTION ( 'NONE',  ( -1.000000000000000000, -0.000000000000000000, 0.000000000000000000 ) ) ;
#40691=CARTESIAN_POINT ( 'NONE',  ( 5.000000000000000000, -27.74655509720617275, -77.16300072079690153 ) ) ;
#40695=LINE ( 'NONE', #17387, #10829 ) ;
#40711=CARTESIAN_POINT ( 'NONE',  ( 10.00000000000000000, 3.894527615417895383, 81.90746397400390322 ) ) ;
#40714=ORIENTED_EDGE ( 'NONE', *, *, #64795, .T. ) ;
#40723=DIRECTION ( 'NONE',  ( 0.000000000000000000, -0.5224985647159380298, -0.8526401643540988395 ) ) ;
#40727=ORIENTED_EDGE ( 'NONE', *, *, #30915, .T. ) ;
#40746=CARTESIAN_POINT ( 'NONE',  ( 10.00000000000000000, 60.67117009219215618, -55.16347631942976193 ) ) ;
#40762=CARTESIAN_POINT ( 'NONE',  ( -10.00000000000000000, 0.000000000000000000, 0.000000000000000000 ) ) ;
#40763=AXIS2_PLACEMENT_3D ( 'NONE', #27475, #20734, #54581 ) ;
#40773=DIRECTION ( 'NONE',  ( 0.000000000000000000, -0.7604059656000369261, 0.6494480483301766638 ) ) ;
#40775=CIRCLE ( 'NONE', #3542, 82.00000000000000000 ) ;
#40784=VERTEX_POINT ( 'NONE', #23985 ) ;
#40798=CARTESIAN_POINT ( 'NONE',  ( 10.00000000000000000, 0.000000000000000000, 0.000000000000000000 ) ) ;
#40801=CARTESIAN_POINT ( 'NONE',  ( 10.00000000000000000, 0.000000000000000000, 0.000000000000000000 ) ) ;
#40804=ORIENTED_EDGE ( 'NONE', *, *, #65548, .T. ) ;
#40823=ORIENTED_EDGE ( 'NONE', *, *, #49901, .T. ) ;
#40837=CIRCLE ( 'NONE', #49237, 82.00000000000000000 ) ;
#40844=CARTESIAN_POINT ( 'NONE',  ( 10.00000000000000000, -51.02545421589363883, 55.20638768913742922 ) ) ;
#40852=CYLINDRICAL_SURFACE ( 'NONE', #11810, 77.49899999999999523 ) ;
#40855=DIRECTION ( 'NONE',  ( 0.000000000000000000, -0.5877852522924803536, 0.8090169943749422332 ) ) ;
#40863=AXIS2_PLACEMENT_3D ( 'NONE', #31655, #13993, #21773 ) ;
#40864=ADVANCED_BREP_SHAPE_REPRESENTATION ( '', ( #37525, #43395 ), #56652 ) ;
#40886=CIRCLE ( 'NONE', #4903, 31.99999999999999645 ) ;
#40906=DIRECTION ( 'NONE',  ( 1.000000000000000000, 0.000000000000000000, -0.000000000000000000 ) ) ;
#40908=ORIENTED_EDGE ( 'NONE', *, *, #33505, .F. ) ;
#40918=VERTEX_POINT ( 'NONE', #37855 ) ;
#40925=AXIS2_PLACEMENT_3D ( 'NONE', #14931, #43157, #55901 ) ;
#40930=DIRECTION ( 'NONE',  ( -1.000000000000000000, -0.000000000000000000, -0.000000000000000000 ) ) ;
#40951=EDGE_CURVE ( 'NONE', #1255, #45686, #22751, .T. ) ;
#40959=ORIENTED_EDGE ( 'NONE', *, *, #50479, .F. ) ;
#40967=ORIENTED_EDGE ( 'NONE', *, *, #45099, .F. ) ;
#40968=CYLINDRICAL_SURFACE ( 'NONE', #20315, 77.49899999999999523 ) ;
#40971=ORIENTED_EDGE ( 'NONE', *, *, #22571, .T. ) ;
#40980=DIRECTION ( 'NONE',  ( 0.000000000000000000, -0.4539904997395350361, -0.8910065241883738940 ) ) ;
#40981=EDGE_CURVE ( 'NONE', #5747, #8743, #43869, .T. ) ;
#40987=ORIENTED_EDGE ( 'NONE', *, *, #55670, .T. ) ;
#40988=( NAMED_UNIT ( * ) SI_UNIT ( $, .STERADIAN. ) SOLID_ANGLE_UNIT ( ) );
#40990=CARTESIAN_POINT ( 'NONE',  ( 0.000000000000000000, -73.72996012237429397, -14.67089635893794508 ) ) ;
#40995=ORIENTED_EDGE ( 'NONE', *, *, #5456, .T. ) ;
#40996=ORIENTED_EDGE ( 'NONE', *, *, #43136, .T. ) ;
#41009=CARTESIAN_POINT ( 'NONE',  ( 10.00000000000000000, 0.000000000000000000, 0.000000000000000000 ) ) ;
#41015=DIRECTION ( 'NONE',  ( 0.000000000000000000, 0.000000000000000000, -1.000000000000000000 ) ) ;
#41018=CARTESIAN_POINT ( 'NONE',  ( 10.00000000000000000, 58.39081064771751528, 50.95692526931350841 ) ) ;
#41021=CARTESIAN_POINT ( 'NONE',  ( 10.00000000000000000, 74.65491531819118620, 23.16904090965733332 ) ) ;
#41034=VECTOR ( 'NONE', #29709, 1000.000000000000000 ) ;
#41043=CARTESIAN_POINT ( 'NONE',  ( 0.000000000000000000, -0.8261519478436571973, 77.49459641780886443 ) ) ;
#41056=CARTESIAN_POINT ( 'NONE',  ( 0.000000000000000000, -12.93880638057369659, 76.41127070299266677 ) ) ;
#41091=VECTOR ( 'NONE', #24249, 1000.000000000000000 ) ;
#41093=VERTEX_POINT ( 'NONE', #28788 ) ;
#41102=DIRECTION ( 'NONE',  ( -1.000000000000000000, 0.000000000000000000, -0.000000000000000000 ) ) ;
#41117=EDGE_CURVE ( 'NONE', #4950, #73972, #16792, .T. ) ;
#41130=DIRECTION ( 'NONE',  ( -1.000000000000000000, -0.000000000000000000, -0.000000000000000000 ) ) ;
#41134=DIRECTION ( 'NONE',  ( 0.000000000000000000, -0.9238795325112906243, 0.3826834323650804004 ) ) ;
#41135=DIRECTION ( 'NONE',  ( 1.000000000000000000, -0.000000000000000000, -0.000000000000000000 ) ) ;
#41141=CIRCLE ( 'NONE', #68733, 32.00000000000000000 ) ;
#41143=ORIENTED_EDGE ( 'NONE', *, *, #44257, .T. ) ;
#41144=LINE ( 'NONE', #23846, #45404 ) ;
#41146=VERTEX_POINT ( 'NONE', #61900 ) ;
#41149=DIRECTION ( 'NONE',  ( -1.000000000000000000, -0.000000000000000000, -0.000000000000000000 ) ) ;
#41150=ORIENTED_EDGE ( 'NONE', *, *, #54751, .T. ) ;
#41157=ORIENTED_EDGE ( 'NONE', *, *, #63324, .T. ) ;
#41188=CIRCLE ( 'NONE', #31554, 77.49899999999999523 ) ;
#41191=EDGE_CURVE ( 'NONE', #34939, #57170, #58463, .T. ) ;
#41194=AXIS2_PLACEMENT_3D ( 'NONE', #27145, #16254, #4999 ) ;
#41201=CARTESIAN_POINT ( 'NONE',  ( 10.00000000000000000, -81.34940948281328588, -10.30890764327469711 ) ) ;
#41206=CARTESIAN_POINT ( 'NONE',  ( 0.000000000000000000, 77.32052557432841411, 5.256550761633138613 ) ) ;
#41208=DIRECTION ( 'NONE',  ( 1.000000000000000000, 0.000000000000000000, -0.000000000000000000 ) ) ;
#41212=CYLINDRICAL_SURFACE ( 'NONE', #20592, 31.99999999999999289 ) ;
#41213=ORIENTED_EDGE ( 'NONE', *, *, #27463, .F. ) ;
#41220=ORIENTED_EDGE ( 'NONE', *, *, #48239, .F. ) ;
#41221=ORIENTED_EDGE ( 'NONE', *, *, #61385, .F. ) ;
#41236=CARTESIAN_POINT ( 'NONE',  ( 10.00000000000000000, 81.96053171279901051, 2.543863470248666658 ) ) ;
#41243=AXIS2_PLACEMENT_3D ( 'NONE', #70124, #52104, #46470 ) ;
#41244=ORIENTED_EDGE ( 'NONE', *, *, #15339, .F. ) ;
#41246=VECTOR ( 'NONE', #10882, 1000.000000000000000 ) ;
#41247=CIRCLE ( 'NONE', #58046, 31.99999999999998934 ) ;
#41258=FACE_OUTER_BOUND ( 'NONE', #69366, .T. ) ;
#41261=EDGE_CURVE ( 'NONE', #29988, #59210, #2108, .T. ) ;
#41267=LINE ( 'NONE', #54030, #22161 ) ;
#41274=CARTESIAN_POINT ( 'NONE',  ( 10.00000000000000000, -46.53671651293991118, 59.03961581697383565 ) ) ;
#41276=ADVANCED_FACE ( 'NONE', ( #46452 ), #58848, .T. ) ;
#41292=DIRECTION ( 'NONE',  ( 0.000000000000000000, 0.7604059656000277112, 0.6494480483301875440 ) ) ;
#41294=DIRECTION ( 'NONE',  ( 0.000000000000000000, 0.000000000000000000, 1.000000000000000000 ) ) ;
#41309=LINE ( 'NONE', #70595, #39531 ) ;
#41318=DIRECTION ( 'NONE',  ( -1.000000000000000000, 0.000000000000000000, 0.000000000000000000 ) ) ;
#41329=ORIENTED_EDGE ( 'NONE', *, *, #37251, .T. ) ;
#41341=VECTOR ( 'NONE', #1526, 1000.000000000000000 ) ;
#41344=CYLINDRICAL_SURFACE ( 'NONE', #61335, 31.99999999999999289 ) ;
#41345=EDGE_CURVE ( 'NONE', #47069, #51767, #23984, .T. ) ;
#41346=ORIENTED_EDGE ( 'NONE', *, *, #60199, .T. ) ;
#41356=ORIENTED_EDGE ( 'NONE', *, *, #7460, .T. ) ;
#41363=EDGE_CURVE ( 'NONE', #2959, #5973, #66012, .T. ) ;
#41364=CARTESIAN_POINT ( 'NONE',  ( 5.000000000000002665, -15.33399622253423722, -80.55351364060604169 ) ) ;
#41372=DIRECTION ( 'NONE',  ( -1.000000000000000000, -0.000000000000000000, -0.000000000000000000 ) ) ;
#41385=FACE_OUTER_BOUND ( 'NONE', #14329, .T. ) ;
#41386=DIRECTION ( 'NONE',  ( -1.000000000000000000, -0.000000000000000000, -0.000000000000000000 ) ) ;
#41397=CARTESIAN_POINT ( 'NONE',  ( -10.00000000000000000, 0.000000000000000000, 0.000000000000000000 ) ) ;
#41398=DIRECTION ( 'NONE',  ( -1.000000000000000000, 0.000000000000000000, 0.000000000000000000 ) ) ;
#41402=EDGE_CURVE ( 'NONE', #13032, #4950, #1216, .T. ) ;
#41424=CYLINDRICAL_SURFACE ( 'NONE', #4433, 82.00000000000000000 ) ;
#41426=LINE ( 'NONE', #12840, #65832 ) ;
#41428=ORIENTED_EDGE ( 'NONE', *, *, #73767, .T. ) ;
#41429=CARTESIAN_POINT ( 'NONE',  ( 10.00000000000000000, 75.11725578898472122, -2.956366410619845730 ) ) ;
#41432=ORIENTED_EDGE ( 'NONE', *, *, #8133, .T. ) ;
#41435=CIRCLE ( 'NONE', #42620, 32.00000000000000000 ) ;
#41440=DIRECTION ( 'NONE',  ( 0.000000000000000000, 0.000000000000000000, 1.000000000000000000 ) ) ;
#41453=AXIS2_PLACEMENT_3D ( 'NONE', #34973, #39881, #46254 ) ;
#41457=CARTESIAN_POINT ( 'NONE',  ( 0.000000000000000000, 68.55367621811205936, -44.99326035065983120 ) ) ;
#41462=ORIENTED_EDGE ( 'NONE', *, *, #39195, .F. ) ;
#41463=ORIENTED_EDGE ( 'NONE', *, *, #6312, .F. ) ;
#41474=CIRCLE ( 'NONE', #72680, 31.99999999999999289 ) ;
#41476=CYLINDRICAL_SURFACE ( 'NONE', #53843, 77.49899999999999523 ) ;
#41483=ADVANCED_FACE ( 'NONE', ( #61061 ), #65599, .T. ) ;
#41485=DIRECTION ( 'NONE',  ( 0.000000000000000000, 0.000000000000000000, 1.000000000000000000 ) ) ;
#41489=DIRECTION ( 'NONE',  ( -1.000000000000000000, -0.000000000000000000, 0.000000000000000000 ) ) ;
#41493=EDGE_CURVE ( 'NONE', #28922, #52606, #16843, .T. ) ;
#41512=CIRCLE ( 'NONE', #23484, 77.49899999999999523 ) ;
#41545=DIRECTION ( 'NONE',  ( 0.000000000000000000, 0.000000000000000000, 1.000000000000000000 ) ) ;
#41553=DIRECTION ( 'NONE',  ( 1.000000000000000000, -0.000000000000000000, -0.000000000000000000 ) ) ;
#41557=CARTESIAN_POINT ( 'NONE',  ( 10.00000000000000000, 72.35160999960844208, -20.41045688087747223 ) ) ;
#41563=CARTESIAN_POINT ( 'NONE',  ( 0.000000000000000000, 0.000000000000000000, 0.000000000000000000 ) ) ;
#41577=EDGE_CURVE ( 'NONE', #17670, #5506, #26432, .T. ) ;
#41580=AXIS2_PLACEMENT_3D ( 'NONE', #54900, #3793, #3423 ) ;
#41586=ORIENTED_EDGE ( 'NONE', *, *, #12214, .F. ) ;
#41590=VERTEX_POINT ( 'NONE', #61812 ) ;
#41601=ORIENTED_EDGE ( 'NONE', *, *, #56644, .T. ) ;
#41602=EDGE_LOOP ( 'NONE', ( #64108, #4831, #71254, #46256 ) ) ;
#41605=CARTESIAN_POINT ( 'NONE',  ( 10.00000000000000000, -15.33399622253424965, -80.55351364060605590 ) ) ;
#41611=DIRECTION ( 'NONE',  ( 1.000000000000000000, -0.000000000000000000, -0.000000000000000000 ) ) ;
#41620=EDGE_LOOP ( 'NONE', ( #45013, #73017, #47362, #40995 ) ) ;
#41625=FACE_OUTER_BOUND ( 'NONE', #24138, .T. ) ;
#41628=EDGE_LOOP ( 'NONE', ( #19897, #69436, #53906, #26230 ) ) ;
#41631=ORIENTED_EDGE ( 'NONE', *, *, #22151, .T. ) ;
#41643=VECTOR ( 'NONE', #73357, 1000.000000000000000 ) ;
#41644=DIRECTION ( 'NONE',  ( 0.000000000000000000, 0.4539904997395477482, -0.8910065241883674547 ) ) ;
#41645=CYLINDRICAL_SURFACE ( 'NONE', #3756, 32.00000000000000000 ) ;
#41647=CYLINDRICAL_SURFACE ( 'NONE', #56824, 82.00000000000000000 ) ;
#41651=DIRECTION ( 'NONE',  ( -1.000000000000000000, 0.000000000000000000, 0.000000000000000000 ) ) ;
#41662=EDGE_CURVE ( 'NONE', #36881, #26809, #49076, .T. ) ;
#41665=EDGE_CURVE ( 'NONE', #27978, #464, #36034, .T. ) ;
#41671=DIRECTION ( 'NONE',  ( -1.000000000000000000, 0.000000000000000000, -0.000000000000000000 ) ) ;
#41673=DIRECTION ( 'NONE',  ( 0.000000000000000000, 0.000000000000000000, 1.000000000000000000 ) ) ;
#41681=CYLINDRICAL_SURFACE ( 'NONE', #35616, 12.50000000000000000 ) ;
#41689=ORIENTED_EDGE ( 'NONE', *, *, #7295, .T. ) ;
#41690=ORIENTED_EDGE ( 'NONE', *, *, #69548, .F. ) ;
#41707=ORIENTED_EDGE ( 'NONE', *, *, #37252, .F. ) ;
#41734=DIRECTION ( 'NONE',  ( -1.000000000000000000, 0.000000000000000000, 0.000000000000000000 ) ) ;
#41735=CARTESIAN_POINT ( 'NONE',  ( 10.00000000000000000, 5.256550761633969060, -77.32052557432835727 ) ) ;
#41739=AXIS2_PLACEMENT_3D ( 'NONE', #42272, #14789, #37372 ) ;
#41750=DIRECTION ( 'NONE',  ( 0.000000000000000000, -0.8910065241883722287, 0.4539904997395383113 ) ) ;
#41755=EDGE_LOOP ( 'NONE', ( #71353, #30354, #64005, #17648 ) ) ;
#41763=CARTESIAN_POINT ( 'NONE',  ( 5.000000000000000000, 64.81221759200343513, 50.23322058963371006 ) ) ;
#41766=ORIENTED_EDGE ( 'NONE', *, *, #9582, .T. ) ;
#41769=EDGE_CURVE ( 'NONE', #16195, #31341, #24180, .T. ) ;
#41792=CARTESIAN_POINT ( 'NONE',  ( 5.000000000000000000, 50.23322058963442061, -64.81221759200289512 ) ) ;
#41810=ORIENTED_EDGE ( 'NONE', *, *, #52828, .T. ) ;
#41818=DIRECTION ( 'NONE',  ( -1.000000000000000000, 0.000000000000000000, -0.000000000000000000 ) ) ;
#41821=AXIS2_PLACEMENT_3D ( 'NONE', #51558, #34632, #17711 ) ;
#41824=LINE ( 'NONE', #35803, #16297 ) ;
#41838=DIRECTION ( 'NONE',  ( 0.000000000000000000, 0.6494480483301848794, -0.7604059656000299317 ) ) ;
#41852=DIRECTION ( 'NONE',  ( -1.000000000000000000, 0.000000000000000000, 0.000000000000000000 ) ) ;
#41860=DIRECTION ( 'NONE',  ( -1.000000000000000000, -0.000000000000000000, -0.000000000000000000 ) ) ;
#41865=ADVANCED_FACE ( 'NONE', ( #65883 ), #3116, .T. ) ;
#41877=CIRCLE ( 'NONE', #51479, 77.49900000000000944 ) ;
#41898=CARTESIAN_POINT ( 'NONE',  ( 10.00000000000000000, 0.000000000000000000, 0.000000000000000000 ) ) ;
#41919=DIRECTION ( 'NONE',  ( -1.000000000000000000, 0.000000000000000000, 0.000000000000000000 ) ) ;
#41920=VERTEX_POINT ( 'NONE', #59874 ) ;
#41921=DIRECTION ( 'NONE',  ( -1.000000000000000000, -0.000000000000000000, 0.000000000000000000 ) ) ;
#41925=ORIENTED_EDGE ( 'NONE', *, *, #29684, .F. ) ;
#41928=DIRECTION ( 'NONE',  ( -1.000000000000000000, 0.000000000000000000, 0.000000000000000000 ) ) ;
#41933=AXIS2_PLACEMENT_3D ( 'NONE', #18146, #34695, #51244 ) ;
#41934=EDGE_LOOP ( 'NONE', ( #57575, #55407, #9105, #56225 ) ) ;
#41935=AXIS2_PLACEMENT_3D ( 'NONE', #69338, #11452, #52799 ) ;
#41961=EDGE_CURVE ( 'NONE', #28563, #25004, #8290, .T. ) ;
#41973=CARTESIAN_POINT ( 'NONE',  ( 10.00000000000000000, 77.49459641780886443, 0.8261519478433866359 ) ) ;
#41981=CARTESIAN_POINT ( 'NONE',  ( 10.00000000000000000, 0.000000000000000000, 0.000000000000000000 ) ) ;
#41999=ORIENTED_EDGE ( 'NONE', *, *, #74190, .F. ) ;
#42001=ORIENTED_EDGE ( 'NONE', *, *, #39164, .T. ) ;
#42009=CARTESIAN_POINT ( 'NONE',  ( 0.000000000000000000, 73.44644590900061587, 24.73286445877730699 ) ) ;
#42018=EDGE_CURVE ( 'NONE', #73972, #50699, #59937, .T. ) ;
#42019=ORIENTED_EDGE ( 'NONE', *, *, #24682, .T. ) ;
#42052=CIRCLE ( 'NONE', #62455, 82.00000000000000000 ) ;
#42058=DIRECTION ( 'NONE',  ( -1.000000000000000000, 0.000000000000000000, 0.000000000000000000 ) ) ;
#42060=LINE ( 'NONE', #38544, #51212 ) ;
#42065=CIRCLE ( 'NONE', #22861, 82.00000000000000000 ) ;
#42075=DIRECTION ( 'NONE',  ( 0.000000000000000000, -0.9510565162951566398, 0.3090169943749381809 ) ) ;
#42078=EDGE_LOOP ( 'NONE', ( #70979, #44673, #66225, #66586 ) ) ;
#42082=LINE ( 'NONE', #35676, #67790 ) ;
#42089=VERTEX_POINT ( 'NONE', #68095 ) ;
#42094=CIRCLE ( 'NONE', #44458, 31.99999999999998934 ) ;
#42116=ORIENTED_EDGE ( 'NONE', *, *, #25857, .T. ) ;
#42119=CYLINDRICAL_SURFACE ( 'NONE', #59709, 31.99999999999999289 ) ;
#42124=CARTESIAN_POINT ( 'NONE',  ( 0.000000000000000000, -17.28742895386139722, 75.54627589209937355 ) ) ;
#42131=DIRECTION ( 'NONE',  ( 0.000000000000000000, 0.000000000000000000, -1.000000000000000000 ) ) ;
#42149=CARTESIAN_POINT ( 'NONE',  ( 10.00000000000000000, 0.000000000000000000, 0.000000000000000000 ) ) ;
#42153=CIRCLE ( 'NONE', #66144, 31.99999999999999289 ) ;
#42155=ORIENTED_EDGE ( 'NONE', *, *, #56364, .T. ) ;
#42167=CIRCLE ( 'NONE', #66167, 82.00000000000000000 ) ;
#42175=ORIENTED_EDGE ( 'NONE', *, *, #19333, .F. ) ;
#42182=CYLINDRICAL_SURFACE ( 'NONE', #67224, 82.00000000000000000 ) ;
#42184=EDGE_CURVE ( 'NONE', #73572, #43336, #68366, .T. ) ;
#42189=DIRECTION ( 'NONE',  ( 0.000000000000000000, 0.000000000000000000, -1.000000000000000000 ) ) ;
#42203=DIRECTION ( 'NONE',  ( 1.000000000000000000, 0.000000000000000000, 0.000000000000000000 ) ) ;
#42206=DIRECTION ( 'NONE',  ( -1.000000000000000000, 0.000000000000000000, 0.000000000000000000 ) ) ;
#42207=CARTESIAN_POINT ( 'NONE',  ( 10.00000000000000000, -2.946379043145784582, -75.11764819372150725 ) ) ;
#42217=LINE ( 'NONE', #48217, #72089 ) ;
#42219=EDGE_CURVE ( 'NONE', #64362, #63204, #643, .T. ) ;
#42220=LINE ( 'NONE', #9098, #49977 ) ;
#42225=DIRECTION ( 'NONE',  ( 1.000000000000000000, -0.000000000000000000, -0.000000000000000000 ) ) ;
#42227=DIRECTION ( 'NONE',  ( -1.000000000000000000, 0.000000000000000000, 0.000000000000000000 ) ) ;
#42229=ORIENTED_EDGE ( 'NONE', *, *, #48892, .F. ) ;
#42233=LINE ( 'NONE', #36204, #5890 ) ;
#42237=AXIS2_PLACEMENT_3D ( 'NONE', #60451, #43900, #61558 ) ;
#42244=LINE ( 'NONE', #30203, #63487 ) ;
#42246=DIRECTION ( 'NONE',  ( 0.000000000000000000, 0.000000000000000000, 1.000000000000000000 ) ) ;
#42253=ORIENTED_EDGE ( 'NONE', *, *, #41961, .T. ) ;
#42263=VERTEX_POINT ( 'NONE', #41201 ) ;
#42266=CIRCLE ( 'NONE', #6270, 31.99999999999999645 ) ;
#42269=EDGE_LOOP ( 'NONE', ( #36072, #37562, #5151, #49361 ) ) ;
#42272=CARTESIAN_POINT ( 'NONE',  ( 10.00000000000000000, 0.000000000000000000, 0.000000000000000000 ) ) ;
#42273=ORIENTED_EDGE ( 'NONE', *, *, #57833, .F. ) ;
#42277=ORIENTED_EDGE ( 'NONE', *, *, #26585, .T. ) ;
#42280=VERTEX_POINT ( 'NONE', #46846 ) ;
#42303=DIRECTION ( 'NONE',  ( -1.000000000000000000, 0.000000000000000000, -0.000000000000000000 ) ) ;
#42310=DIRECTION ( 'NONE',  ( 0.000000000000000000, 0.000000000000000000, 1.000000000000000000 ) ) ;
#42321=DIRECTION ( 'NONE',  ( -1.000000000000000000, 0.000000000000000000, -0.000000000000000000 ) ) ;
#42328=CARTESIAN_POINT ( 'NONE',  ( 10.00000000000000000, 55.38113227695782115, 54.21277698773695164 ) ) ;
#42336=VERTEX_POINT ( 'NONE', #24281 ) ;
#42339=EDGE_CURVE ( 'NONE', #55666, #58910, #6644, .T. ) ;
#42340=DIRECTION ( 'NONE',  ( -1.000000000000000000, 0.000000000000000000, -0.000000000000000000 ) ) ;
#42351=DIRECTION ( 'NONE',  ( 0.000000000000000000, 0.000000000000000000, -1.000000000000000000 ) ) ;
#42356=ORIENTED_EDGE ( 'NONE', *, *, #71768, .F. ) ;
#42362=DIRECTION ( 'NONE',  ( 0.000000000000000000, -0.9876883405951394357, 0.1564344650402205716 ) ) ;
#42363=DIRECTION ( 'NONE',  ( 0.000000000000000000, 0.000000000000000000, -1.000000000000000000 ) ) ;
#42382=EDGE_CURVE ( 'NONE', #37462, #14784, #25390, .T. ) ;
#42385=ORIENTED_EDGE ( 'NONE', *, *, #73834, .T. ) ;
#42402=DIRECTION ( 'NONE',  ( 0.000000000000000000, 0.000000000000000000, 1.000000000000000000 ) ) ;
#42421=CARTESIAN_POINT ( 'NONE',  ( 10.00000000000000000, 44.88180994100376608, 63.18004540533043922 ) ) ;
#42423=AXIS2_PLACEMENT_3D ( 'NONE', #23267, #57850, #64972 ) ;
#42428=ADVANCED_FACE ( 'NONE', ( #59229 ), #19365, .T. ) ;
#42435=EDGE_CURVE ( 'NONE', #38013, #19224, #18611, .T. ) ;
#42440=ORIENTED_EDGE ( 'NONE', *, *, #60377, .F. ) ;
#42442=VERTEX_POINT ( 'NONE', #31380 ) ;
#42459=VERTEX_POINT ( 'NONE', #73078 ) ;
#42465=EDGE_CURVE ( 'NONE', #3369, #72495, #9198, .T. ) ;
#42476=DIRECTION ( 'NONE',  ( 0.000000000000000000, 0.000000000000000000, 1.000000000000000000 ) ) ;
#42478=DIRECTION ( 'NONE',  ( -1.000000000000000000, -0.000000000000000000, 0.000000000000000000 ) ) ;
#42488=VECTOR ( 'NONE', #61549, 1000.000000000000000 ) ;
#42490=DIRECTION ( 'NONE',  ( 0.000000000000000000, 0.000000000000000000, 1.000000000000000000 ) ) ;
#42495=FACE_OUTER_BOUND ( 'NONE', #39785, .T. ) ;
#42498=DIRECTION ( 'NONE',  ( -1.000000000000000000, -0.000000000000000000, -0.000000000000000000 ) ) ;
#42506=ORIENTED_EDGE ( 'NONE', *, *, #4612, .T. ) ;
#42510=CIRCLE ( 'NONE', #19686, 31.99999999999999289 ) ;
#42513=EDGE_CURVE ( 'NONE', #4178, #71089, #27023, .T. ) ;
#42516=DIRECTION ( 'NONE',  ( -1.000000000000000000, -0.000000000000000000, -0.000000000000000000 ) ) ;
#42525=VECTOR ( 'NONE', #53969, 1000.000000000000000 ) ;
#42528=AXIS2_PLACEMENT_3D ( 'NONE', #20117, #32132, #43078 ) ;
#42531=ORIENTED_EDGE ( 'NONE', *, *, #72952, .F. ) ;
#42533=EDGE_LOOP ( 'NONE', ( #15747, #42916, #49291, #30356 ) ) ;
#42538=CARTESIAN_POINT ( 'NONE',  ( 0.000000000000000000, 0.000000000000000000, 0.000000000000000000 ) ) ;
#42542=ORIENTED_EDGE ( 'NONE', *, *, #48819, .T. ) ;
#42543=CIRCLE ( 'NONE', #53330, 31.99999999999999289 ) ;
#42552=CARTESIAN_POINT ( 'NONE',  ( 0.000000000000000000, 0.000000000000000000, 0.000000000000000000 ) ) ;
#42555=DIRECTION ( 'NONE',  ( -1.000000000000000000, 0.000000000000000000, -0.000000000000000000 ) ) ;
#42563=ORIENTED_EDGE ( 'NONE', *, *, #50517, .T. ) ;
#42565=DIRECTION ( 'NONE',  ( 0.000000000000000000, 0.000000000000000000, -1.000000000000000000 ) ) ;
#42573=ORIENTED_EDGE ( 'NONE', *, *, #16311, .T. ) ;
#42582=CARTESIAN_POINT ( 'NONE',  ( 0.000000000000000000, 0.000000000000000000, 0.000000000000000000 ) ) ;
#42585=AXIS2_PLACEMENT_3D ( 'NONE', #73034, #73416, #4285 ) ;
#42591=DIRECTION ( 'NONE',  ( 0.000000000000000000, 0.5224985647159440250, 0.8526401643540951758 ) ) ;
#42594=( NAMED_UNIT ( * ) SI_UNIT ( $, .STERADIAN. ) SOLID_ANGLE_UNIT ( ) );
#42605=DIRECTION ( 'NONE',  ( -1.000000000000000000, -0.000000000000000000, -0.000000000000000000 ) ) ;
#42612=EDGE_CURVE ( 'NONE', #21124, #42089, #71973, .T. ) ;
#42618=ORIENTED_EDGE ( 'NONE', *, *, #29617, .T. ) ;
#42619=CARTESIAN_POINT ( 'NONE',  ( 0.000000000000000000, 0.000000000000000000, 0.000000000000000000 ) ) ;
#42620=AXIS2_PLACEMENT_3D ( 'NONE', #54018, #71276, #60039 ) ;
#42633=CARTESIAN_POINT ( 'NONE',  ( 10.00000000000000000, 70.53064760720278059, 26.01480285779964774 ) ) ;
#42635=ORIENTED_EDGE ( 'NONE', *, *, #34990, .F. ) ;
#42644=CARTESIAN_POINT ( 'NONE',  ( 10.00000000000000000, 0.000000000000000000, 0.000000000000000000 ) ) ;
#42645=VECTOR ( 'NONE', #37128, 1000.000000000000000 ) ;
#42647=CARTESIAN_POINT ( 'NONE',  ( 10.00000000000000000, 75.54627589209943039, 17.28742895386112721 ) ) ;
#42658=AXIS2_PLACEMENT_3D ( 'NONE', #25815, #71668, #55505 ) ;
#42661=ORIENTED_EDGE ( 'NONE', *, *, #50167, .T. ) ;
#42664=ORIENTED_EDGE ( 'NONE', *, *, #72785, .F. ) ;
#42665=ORIENTED_EDGE ( 'NONE', *, *, #72538, .F. ) ;
#42671=DIRECTION ( 'NONE',  ( 0.000000000000000000, 0.000000000000000000, 1.000000000000000000 ) ) ;
#42679=LINE ( 'NONE', #71977, #19714 ) ;
#42684=EDGE_CURVE ( 'NONE', #52914, #4552, #33037, .T. ) ;
#42685=DIRECTION ( 'NONE',  ( 0.000000000000000000, 0.9238795325112878487, -0.3826834323650874503 ) ) ;
#42699=VERTEX_POINT ( 'NONE', #58028 ) ;
#42703=EDGE_CURVE ( 'NONE', #4987, #27575, #22722, .T. ) ;
#42707=VECTOR ( 'NONE', #20035, 1000.000000000000000 ) ;
#42716=DIRECTION ( 'NONE',  ( -1.000000000000000000, -0.000000000000000000, 0.000000000000000000 ) ) ;
#42721=VERTEX_POINT ( 'NONE', #559 ) ;
#42728=CYLINDRICAL_SURFACE ( 'NONE', #30581, 82.00000000000000000 ) ;
#42735=EDGE_LOOP ( 'NONE', ( #18453, #29838, #43755, #65740 ) ) ;
#42748=VERTEX_POINT ( 'NONE', #40746 ) ;
#42755=AXIS2_PLACEMENT_3D ( 'NONE', #4314, #50133, #10302 ) ;
#42764=DIRECTION ( 'NONE',  ( 1.000000000000000000, 0.000000000000000000, 0.000000000000000000 ) ) ;
#42771=EDGE_CURVE ( 'NONE', #7429, #23521, #55856, .T. ) ;
#42774=CARTESIAN_POINT ( 'NONE',  ( 10.00000000000000000, 0.000000000000000000, 0.000000000000000000 ) ) ;
#42775=EDGE_CURVE ( 'NONE', #38604, #34215, #5068, .T. ) ;
#42777=CARTESIAN_POINT ( 'NONE',  ( 10.00000000000000000, -71.27951684758005513, -30.41916302227188851 ) ) ;
#42789=CIRCLE ( 'NONE', #55989, 82.00000000000000000 ) ;
#42794=CIRCLE ( 'NONE', #55998, 77.49900000000000944 ) ;
#42798=VERTEX_POINT ( 'NONE', #68204 ) ;
#42803=DIRECTION ( 'NONE',  ( 0.000000000000000000, -1.000000000000000000, -1.040834085586084730E-14 ) ) ;
#42804=ORIENTED_EDGE ( 'NONE', *, *, #662, .F. ) ;
#42820=CARTESIAN_POINT ( 'NONE',  ( 10.00000000000000000, 0.000000000000000000, 0.000000000000000000 ) ) ;
#42828=CARTESIAN_POINT ( 'NONE',  ( 10.00000000000000000, 69.42325613327439271, 34.44570377933623462 ) ) ;
#42838=ORIENTED_EDGE ( 'NONE', *, *, #4625, .T. ) ;
#42848=DIRECTION ( 'NONE',  ( 0.000000000000000000, 0.4539904997395413644, 0.8910065241883706744 ) ) ;
#42856=FACE_OUTER_BOUND ( 'NONE', #4835, .T. ) ;
#42857=DIRECTION ( 'NONE',  ( -1.000000000000000000, 0.000000000000000000, 0.000000000000000000 ) ) ;
#42859=CARTESIAN_POINT ( 'NONE',  ( 10.00000000000000000, 0.000000000000000000, 0.000000000000000000 ) ) ;
#42862=CARTESIAN_POINT ( 'NONE',  ( 10.00000000000000000, -75.54627589209955829, 17.28742895386058009 ) ) ;
#42865=DIRECTION ( 'NONE',  ( -1.000000000000000000, -0.000000000000000000, 0.000000000000000000 ) ) ;
#42868=CARTESIAN_POINT ( 'NONE',  ( 10.00000000000000000, 68.26794271651262136, 31.47745569255165066 ) ) ;
#42875=CARTESIAN_POINT ( 'NONE',  ( 10.00000000000000000, 0.000000000000000000, 0.000000000000000000 ) ) ;
#42876=CARTESIAN_POINT ( 'NONE',  ( 10.00000000000000000, -64.81221759200380461, 50.23322058963325532 ) ) ;
#42877=CARTESIAN_POINT ( 'NONE',  ( 0.000000000000000000, 31.47745569255237896, -68.26794271651228030 ) ) ;
#42879=DIRECTION ( 'NONE',  ( -1.000000000000000000, 0.000000000000000000, -0.000000000000000000 ) ) ;
#42883=EDGE_CURVE ( 'NONE', #26087, #503, #59890, .T. ) ;
#42885=CYLINDRICAL_SURFACE ( 'NONE', #67184, 82.00000000000000000 ) ;
#42887=CYLINDRICAL_SURFACE ( 'NONE', #64697, 31.99999999999999289 ) ;
#42892=DIRECTION ( 'NONE',  ( 0.000000000000000000, -0.5877852522924802425, 0.8090169943749422332 ) ) ;
#42894=CARTESIAN_POINT ( 'NONE',  ( 10.00000000000000000, 0.000000000000000000, 0.000000000000000000 ) ) ;
#42898=VECTOR ( 'NONE', #64222, 1000.000000000000000 ) ;
#42901=CIRCLE ( 'NONE', #65713, 31.99999999999999289 ) ;
#42902=EDGE_CURVE ( 'NONE', #3846, #45970, #1006, .T. ) ;
#42904=DIRECTION ( 'NONE',  ( 0.000000000000000000, 0.000000000000000000, 1.000000000000000000 ) ) ;
#42912=DIRECTION ( 'NONE',  ( -1.000000000000000000, 0.000000000000000000, -0.000000000000000000 ) ) ;
#42916=ORIENTED_EDGE ( 'NONE', *, *, #25125, .F. ) ;
#42927=ORIENTED_EDGE ( 'NONE', *, *, #58817, .F. ) ;
#42928=DIRECTION ( 'NONE',  ( 0.000000000000000000, 0.000000000000000000, 1.000000000000000000 ) ) ;
#42947=LINE ( 'NONE', #54230, #13858 ) ;
#42959=DIRECTION ( 'NONE',  ( -1.000000000000000000, -0.000000000000000000, 0.000000000000000000 ) ) ;
#42961=AXIS2_PLACEMENT_3D ( 'NONE', #71357, #26616, #66487 ) ;
#42965=LINE ( 'NONE', #61365, #18976 ) ;
#42970=CYLINDRICAL_SURFACE ( 'NONE', #47205, 82.00000000000000000 ) ;
#42972=AXIS2_PLACEMENT_3D ( 'NONE', #72257, #54970, #37330 ) ;
#42974=CARTESIAN_POINT ( 'NONE',  ( 0.000000000000000000, 75.54627589209943039, 17.28742895386112721 ) ) ;
#42987=AXIS2_PLACEMENT_3D ( 'NONE', #23560, #52127, #52489 ) ;
#43010=ORIENTED_EDGE ( 'NONE', *, *, #25612, .T. ) ;
#43034=CARTESIAN_POINT ( 'NONE',  ( 0.000000000000000000, 46.54456581323805153, 59.03342792756280488 ) ) ;
#43041=VECTOR ( 'NONE', #47078, 1000.000000000000000 ) ;
#43046=CIRCLE ( 'NONE', #10605, 82.00000000000000000 ) ;
#43056=ORIENTED_EDGE ( 'NONE', *, *, #32317, .F. ) ;
#43059=CARTESIAN_POINT ( 'NONE',  ( 10.00000000000000000, 49.70050353004977239, -59.46389618801908483 ) ) ;
#43064=DIRECTION ( 'NONE',  ( 0.000000000000000000, -0.8090169943749532244, 0.5877852522924652545 ) ) ;
#43065=DIRECTION ( 'NONE',  ( -1.000000000000000000, -0.000000000000000000, -0.000000000000000000 ) ) ;
#43068=EDGE_CURVE ( 'NONE', #16005, #43091, #44447, .T. ) ;
#43071=AXIS2_PLACEMENT_3D ( 'NONE', #199, #68952, #33230 ) ;
#43078=DIRECTION ( 'NONE',  ( 0.000000000000000000, 0.000000000000000000, 1.000000000000000000 ) ) ;
#43079=EDGE_CURVE ( 'NONE', #42336, #38466, #42965, .T. ) ;
#43085=DIRECTION ( 'NONE',  ( -1.000000000000000000, -0.000000000000000000, -0.000000000000000000 ) ) ;
#43091=VERTEX_POINT ( 'NONE', #72611 ) ;
#43105=ORIENTED_EDGE ( 'NONE', *, *, #59350, .T. ) ;
#43107=DIRECTION ( 'NONE',  ( -1.000000000000000000, 0.000000000000000000, 0.000000000000000000 ) ) ;
#43120=ORIENTED_EDGE ( 'NONE', *, *, #24786, .F. ) ;
#43126=CIRCLE ( 'NONE', #62336, 77.49900000000000944 ) ;
#43128=CARTESIAN_POINT ( 'NONE',  ( 10.00000000000000000, 64.81221759200417409, -50.23322058963275794 ) ) ;
#43136=EDGE_CURVE ( 'NONE', #22755, #52246, #65901, .T. ) ;
#43153=DIRECTION ( 'NONE',  ( 0.000000000000000000, 0.000000000000000000, -1.000000000000000000 ) ) ;
#43157=DIRECTION ( 'NONE',  ( 1.000000000000000000, 0.000000000000000000, 0.000000000000000000 ) ) ;
#43158=AXIS2_PLACEMENT_3D ( 'NONE', #10068, #32989, #9703 ) ;
#43161=EDGE_CURVE ( 'NONE', #42263, #54097, #44067, .T. ) ;
#43169=ORIENTED_EDGE ( 'NONE', *, *, #52705, .F. ) ;
#43177=DIRECTION ( 'NONE',  ( -1.000000000000000000, 0.000000000000000000, 0.000000000000000000 ) ) ;
#43181=CIRCLE ( 'NONE', #7162, 82.00000000000000000 ) ;
#43188=DIRECTION ( 'NONE',  ( -1.000000000000000000, -0.000000000000000000, 0.000000000000000000 ) ) ;
#43201=CARTESIAN_POINT ( 'NONE',  ( 0.000000000000000000, 73.95703589263973754, 23.16143007188453851 ) ) ;
#43205=CARTESIAN_POINT ( 'NONE',  ( 0.000000000000000000, 74.65491531819118620, -8.830959090342659579 ) ) ;
#43210=DIRECTION ( 'NONE',  ( 0.000000000000000000, 0.000000000000000000, 1.000000000000000000 ) ) ;
#43211=CARTESIAN_POINT ( 'NONE',  ( 10.00000000000000000, 0.000000000000000000, 0.000000000000000000 ) ) ;
#43213=EDGE_LOOP ( 'NONE', ( #11190, #61611, #31684, #30681 ) ) ;
#43220=CARTESIAN_POINT ( 'NONE',  ( 0.000000000000000000, -65.58780272294048075, -36.73666225445966660 ) ) ;
#43224=ORIENTED_EDGE ( 'NONE', *, *, #41961, .F. ) ;
#43225=ORIENTED_EDGE ( 'NONE', *, *, #55184, .F. ) ;
#43229=ORIENTED_EDGE ( 'NONE', *, *, #73273, .F. ) ;
#43232=ORIENTED_EDGE ( 'NONE', *, *, #722, .F. ) ;
#43235=ORIENTED_EDGE ( 'NONE', *, *, #72396, .T. ) ;
#43241=DIRECTION ( 'NONE',  ( -1.000000000000000000, 0.000000000000000000, 0.000000000000000000 ) ) ;
#43251=EDGE_CURVE ( 'NONE', #24836, #8405, #10968, .T. ) ;
#43259=CARTESIAN_POINT ( 'NONE',  ( 10.00000000000000000, 2.543863470249530856, -81.96053171279901051 ) ) ;
#43266=CIRCLE ( 'NONE', #32438, 32.00000000000000000 ) ;
#43273=CIRCLE ( 'NONE', #58883, 82.00000000000000000 ) ;
#43275=ORIENTED_EDGE ( 'NONE', *, *, #37441, .F. ) ;
#43277=DIRECTION ( 'NONE',  ( 0.000000000000000000, 0.000000000000000000, 1.000000000000000000 ) ) ;
#43285=CARTESIAN_POINT ( 'NONE',  ( -10.00000000000000000, 0.000000000000000000, 0.000000000000000000 ) ) ;
#43304=ADVANCED_FACE ( 'NONE', ( #45935 ), #22621, .T. ) ;
#43313=DIRECTION ( 'NONE',  ( 0.000000000000000000, 0.000000000000000000, 1.000000000000000000 ) ) ;
#43316=VECTOR ( 'NONE', #12758, 1000.000000000000000 ) ;
#43328=DIRECTION ( 'NONE',  ( 0.000000000000000000, -0.9969173337331271867, -0.07845909572785571273 ) ) ;
#43330=EDGE_CURVE ( 'NONE', #29098, #42263, #14199, .T. ) ;
#43332=CARTESIAN_POINT ( 'NONE',  ( 0.000000000000000000, 71.91182617369187824, 28.89263327155772387 ) ) ;
#43336=VERTEX_POINT ( 'NONE', #53041 ) ;
#43338=DIRECTION ( 'NONE',  ( -1.000000000000000000, 0.000000000000000000, 0.000000000000000000 ) ) ;
#43340=EDGE_CURVE ( 'NONE', #73769, #34394, #57414, .T. ) ;
#43365=AXIS2_PLACEMENT_3D ( 'NONE', #61525, #62273, #31537 ) ;
#43374=ORIENTED_EDGE ( 'NONE', *, *, #73991, .T. ) ;
#43376=EDGE_CURVE ( 'NONE', #33774, #17478, #36849, .T. ) ;
#43378=CARTESIAN_POINT ( 'NONE',  ( 0.000000000000000000, 71.21200624218852226, -40.65526001592539984 ) ) ;
#43381=ORIENTED_EDGE ( 'NONE', *, *, #18248, .F. ) ;
#43382=ADVANCED_FACE ( 'NONE', ( #25211 ), #6445, .T. ) ;
#43395=AXIS2_PLACEMENT_3D ( 'NONE', #48320, #71232, #19735 ) ;
#43407=DIRECTION ( 'NONE',  ( 0.000000000000000000, 0.000000000000000000, 1.000000000000000000 ) ) ;
#43409=DIRECTION ( 'NONE',  ( -1.000000000000000000, 0.000000000000000000, 0.000000000000000000 ) ) ;
#43429=CIRCLE ( 'NONE', #58971, 32.00000000000000711 ) ;
#43445=LINE ( 'NONE', #14091, #35342 ) ;
#43459=VECTOR ( 'NONE', #55335, 1000.000000000000000 ) ;
#43463=CARTESIAN_POINT ( 'NONE',  ( 0.000000000000000000, -21.60688246758530440, -79.10210256391390260 ) ) ;
#43466=CARTESIAN_POINT ( 'NONE',  ( 10.00000000000000000, 64.81221759200342092, 50.23322058963369585 ) ) ;
#43471=EDGE_CURVE ( 'NONE', #21162, #45686, #13904, .T. ) ;
#43484=ORIENTED_EDGE ( 'NONE', *, *, #59497, .F. ) ;
#43489=CARTESIAN_POINT ( 'NONE',  ( 0.000000000000000000, -62.20884554314051940, 46.21855187248608132 ) ) ;
#43494=VERTEX_POINT ( 'NONE', #29350 ) ;
#43498=DIRECTION ( 'NONE',  ( 0.000000000000000000, 0.000000000000000000, 1.000000000000000000 ) ) ;
#43505=DIRECTION ( 'NONE',  ( -1.000000000000000000, 0.000000000000000000, 0.000000000000000000 ) ) ;
#43507=CARTESIAN_POINT ( 'NONE',  ( 5.000000000000002665, -80.55351364060578589, -15.33399622253568673 ) ) ;
#43513=ADVANCED_FACE ( 'NONE', ( #25936 ), #54157, .T. ) ;
#43516=CIRCLE ( 'NONE', #69873, 31.99999999999999645 ) ;
#43521=CARTESIAN_POINT ( 'NONE',  ( 0.000000000000000000, -77.49459641780886443, 0.8261519478428377417 ) ) ;
#43522=VECTOR ( 'NONE', #51062, 1000.000000000000000 ) ;
#43527=DIRECTION ( 'NONE',  ( -1.000000000000000000, -0.000000000000000000, -0.000000000000000000 ) ) ;
#43535=DIRECTION ( 'NONE',  ( -1.000000000000000000, 0.000000000000000000, 0.000000000000000000 ) ) ;
#43540=ORIENTED_EDGE ( 'NONE', *, *, #49968, .F. ) ;
#43544=EDGE_CURVE ( 'NONE', #10016, #8802, #48867, .T. ) ;
#43545=EDGE_LOOP ( 'NONE', ( #64248, #27996, #44108, #49080 ) ) ;
#43550=EDGE_CURVE ( 'NONE', #21162, #10732, #43046, .T. ) ;
#43552=FACE_OUTER_BOUND ( 'NONE', #30063, .T. ) ;
#43556=ORIENTED_EDGE ( 'NONE', *, *, #45943, .F. ) ;
#43566=VERTEX_POINT ( 'NONE', #19916 ) ;
#43568=ORIENTED_EDGE ( 'NONE', *, *, #3257, .T. ) ;
#43575=DIRECTION ( 'NONE',  ( 0.000000000000000000, 0.000000000000000000, -1.000000000000000000 ) ) ;
#43580=CARTESIAN_POINT ( 'NONE',  ( 0.000000000000000000, 74.74816331893430288, 33.71516098798768013 ) ) ;
#43589=VERTEX_POINT ( 'NONE', #22065 ) ;
#43591=EDGE_LOOP ( 'NONE', ( #6999, #24866, #44645, #37619 ) ) ;
#43604=DIRECTION ( 'NONE',  ( -1.000000000000000000, -0.000000000000000000, 0.000000000000000000 ) ) ;
#43608=DIRECTION ( 'NONE',  ( -1.000000000000000000, 0.000000000000000000, 0.000000000000000000 ) ) ;
#43615=DIRECTION ( 'NONE',  ( -1.000000000000000000, 0.000000000000000000, 0.000000000000000000 ) ) ;
#43618=CIRCLE ( 'NONE', #9997, 77.49899999999999523 ) ;
#43620=CIRCLE ( 'NONE', #7589, 31.99999999999999645 ) ;
#43632=DIRECTION ( 'NONE',  ( 0.000000000000000000, 0.000000000000000000, 1.000000000000000000 ) ) ;
#43633=CARTESIAN_POINT ( 'NONE',  ( 10.00000000000000000, -59.03342792756231461, -46.54456581323868392 ) ) ;
#43637=VERTEX_POINT ( 'NONE', #59525 ) ;
#43640=CYLINDRICAL_SURFACE ( 'NONE', #48766, 32.00000000000000000 ) ;
#43652=AXIS2_PLACEMENT_3D ( 'NONE', #26147, #53615, #71637 ) ;
#43656=ORIENTED_EDGE ( 'NONE', *, *, #61209, .T. ) ;
#43659=ADVANCED_FACE ( 'NONE', ( #8385 ), #30196, .T. ) ;
#43670=CIRCLE ( 'NONE', #59333, 31.99999999999999289 ) ;
#43690=VECTOR ( 'NONE', #74163, 1000.000000000000000 ) ;
#43691=DIRECTION ( 'NONE',  ( -1.000000000000000000, -0.000000000000000000, 0.000000000000000000 ) ) ;
#43698=CARTESIAN_POINT ( 'NONE',  ( 10.00000000000000000, 23.16143007188426850, 73.95703589263983702 ) ) ;
#43700=LINE ( 'NONE', #73354, #37055 ) ;
#43705=AXIS2_PLACEMENT_3D ( 'NONE', #50445, #73367, #21876 ) ;
#43709=AXIS2_PLACEMENT_3D ( 'NONE', #53442, #6837, #30132 ) ;
#43710=CARTESIAN_POINT ( 'NONE',  ( 10.00000000000000000, 40.65526001592713357, -71.21200624218752750 ) ) ;
#43715=EDGE_CURVE ( 'NONE', #15962, #73126, #44215, .T. ) ;
#43717=CIRCLE ( 'NONE', #55719, 82.00000000000000000 ) ;
#43720=DIRECTION ( 'NONE',  ( 0.000000000000000000, 0.000000000000000000, 1.000000000000000000 ) ) ;
#43728=CARTESIAN_POINT ( 'NONE',  ( 0.000000000000000000, 8.840884882375075193, 74.65374052328651544 ) ) ;
#43736=EDGE_CURVE ( 'NONE', #278, #4935, #50261, .T. ) ;
#43755=ORIENTED_EDGE ( 'NONE', *, *, #71390, .F. ) ;
#43759=ORIENTED_EDGE ( 'NONE', *, *, #49828, .T. ) ;
#43775=ORIENTED_EDGE ( 'NONE', *, *, #66241, .F. ) ;
#43783=AXIS2_PLACEMENT_3D ( 'NONE', #58398, #63316, #58778 ) ;
#43785=CIRCLE ( 'NONE', #49764, 31.99999999999999289 ) ;
#43793=CARTESIAN_POINT ( 'NONE',  ( 10.00000000000000000, -34.44570377933649041, 69.42325613327427902 ) ) ;
#43796=CARTESIAN_POINT ( 'NONE',  ( 0.000000000000000000, 0.000000000000000000, 0.000000000000000000 ) ) ;
#43798=ORIENTED_EDGE ( 'NONE', *, *, #56477, .T. ) ;
#43803=DIRECTION ( 'NONE',  ( 1.000000000000000000, -0.000000000000000000, 0.000000000000000000 ) ) ;
#43804=EDGE_CURVE ( 'NONE', #60565, #22189, #4239, .T. ) ;
#43806=DIRECTION ( 'NONE',  ( 0.000000000000000000, -0.2334453638558921240, -0.9723699203976797767 ) ) ;
#43817=CARTESIAN_POINT ( 'NONE',  ( 0.000000000000000000, -63.97538442413463855, 51.29473840253199768 ) ) ;
#43831=CARTESIAN_POINT ( 'NONE',  ( 0.000000000000000000, -81.90746397400393164, 3.894527615417586741 ) ) ;
#43842=EDGE_LOOP ( 'NONE', ( #50097, #16739, #44142, #31181 ) ) ;
#43844=VERTEX_POINT ( 'NONE', #15496 ) ;
#43846=ORIENTED_EDGE ( 'NONE', *, *, #1774, .F. ) ;
#43851=DIRECTION ( 'NONE',  ( 0.000000000000000000, 0.000000000000000000, 1.000000000000000000 ) ) ;
#43860=ORIENTED_EDGE ( 'NONE', *, *, #62822, .F. ) ;
#43864=CARTESIAN_POINT ( 'NONE',  ( 5.000000000000000000, 60.67117009219216328, -55.16347631942977614 ) ) ;
#43869=LINE ( 'NONE', #26926, #32324 ) ;
#43871=ORIENTED_EDGE ( 'NONE', *, *, #25041, .F. ) ;
#43872=ORIENTED_EDGE ( 'NONE', *, *, #67206, .F. ) ;
#43873=CARTESIAN_POINT ( 'NONE',  ( 10.00000000000000000, -5.256550761633413060, 77.32052557432841411 ) ) ;
#43874=CARTESIAN_POINT ( 'NONE',  ( 10.00000000000000000, -75.11764819372149304, 2.946379043146075905 ) ) ;
#43892=CARTESIAN_POINT ( 'NONE',  ( 0.000000000000000000, 71.21200624218795383, 40.65526001592638039 ) ) ;
#43896=EDGE_CURVE ( 'NONE', #40236, #10267, #50447, .T. ) ;
#43899=AXIS2_PLACEMENT_3D ( 'NONE', #5046, #68562, #67809 ) ;
#43900=DIRECTION ( 'NONE',  ( -1.000000000000000000, 0.000000000000000000, -0.000000000000000000 ) ) ;
#43903=DIRECTION ( 'NONE',  ( -1.000000000000000000, 0.000000000000000000, 0.000000000000000000 ) ) ;
#43910=FACE_OUTER_BOUND ( 'NONE', #62658, .T. ) ;
#43927=ORIENTED_EDGE ( 'NONE', *, *, #72158, .T. ) ;
#43932=CARTESIAN_POINT ( 'NONE',  ( 10.00000000000000000, 2.543863470248371783, 81.96053171279901051 ) ) ;
#43935=DIRECTION ( 'NONE',  ( 1.000000000000000000, -0.000000000000000000, -0.000000000000000000 ) ) ;
#43961=ORIENTED_EDGE ( 'NONE', *, *, #49968, .T. ) ;
#43973=DIRECTION ( 'NONE',  ( 0.000000000000000000, 0.000000000000000000, 1.000000000000000000 ) ) ;
#43974=DIRECTION ( 'NONE',  ( -1.000000000000000000, 0.000000000000000000, -0.000000000000000000 ) ) ;
#43975=EDGE_CURVE ( 'NONE', #45509, #60565, #70694, .T. ) ;
#43988=DIRECTION ( 'NONE',  ( 0.000000000000000000, -0.07845909572785221553, 0.9969173337331274087 ) ) ;
#43991=AXIS2_PLACEMENT_3D ( 'NONE', #72964, #22986, #68845 ) ;
#43994=CARTESIAN_POINT ( 'NONE',  ( 10.00000000000000000, 0.000000000000000000, 0.000000000000000000 ) ) ;
#44002=CARTESIAN_POINT ( 'NONE',  ( 5.000000000000002665, -15.33399622253540961, 80.55351364060584274 ) ) ;
#44009=CYLINDRICAL_SURFACE ( 'NONE', #68316, 31.99999999999999289 ) ;
#44015=DIRECTION ( 'NONE',  ( 1.000000000000000000, 0.000000000000000000, 0.000000000000000000 ) ) ;
#44022=CARTESIAN_POINT ( 'NONE',  ( 10.00000000000000000, 0.000000000000000000, 0.000000000000000000 ) ) ;
#44031=ORIENTED_EDGE ( 'NONE', *, *, #18761, .T. ) ;
#44049=FACE_OUTER_BOUND ( 'NONE', #45748, .T. ) ;
#44052=DIRECTION ( 'NONE',  ( -1.000000000000000000, 0.000000000000000000, 0.000000000000000000 ) ) ;
#44056=ORIENTED_EDGE ( 'NONE', *, *, #49157, .F. ) ;
#44062=CARTESIAN_POINT ( 'NONE',  ( 5.000000000000002665, -8.966570791701281351, 81.50828551894224461 ) ) ;
#44063=EDGE_CURVE ( 'NONE', #991, #1255, #31043, .T. ) ;
#44067=LINE ( 'NONE', #9850, #40566 ) ;
#44069=DIRECTION ( 'NONE',  ( -1.000000000000000000, 0.000000000000000000, 0.000000000000000000 ) ) ;
#44084=AXIS2_PLACEMENT_3D ( 'NONE', #21092, #48930, #56448 ) ;
#44086=ORIENTED_EDGE ( 'NONE', *, *, #1893, .T. ) ;
#44088=( LENGTH_UNIT ( ) NAMED_UNIT ( * ) SI_UNIT ( .MILLI., .METRE. ) );
#44108=ORIENTED_EDGE ( 'NONE', *, *, #15788, .F. ) ;
#44130=AXIS2_PLACEMENT_3D ( 'NONE', #38223, #27299, #32197 ) ;
#44132=DIRECTION ( 'NONE',  ( -1.000000000000000000, 0.000000000000000000, 0.000000000000000000 ) ) ;
#44136=EDGE_CURVE ( 'NONE', #49408, #16264, #59954, .T. ) ;
#44139=DIRECTION ( 'NONE',  ( -1.000000000000000000, -0.000000000000000000, -0.000000000000000000 ) ) ;
#44142=ORIENTED_EDGE ( 'NONE', *, *, #55670, .F. ) ;
#44143=CIRCLE ( 'NONE', #64531, 31.99999999999999289 ) ;
#44149=DIRECTION ( 'NONE',  ( -1.000000000000000000, -0.000000000000000000, 0.000000000000000000 ) ) ;
#44156=DIRECTION ( 'NONE',  ( -1.000000000000000000, 0.000000000000000000, -0.000000000000000000 ) ) ;
#44179=ORIENTED_EDGE ( 'NONE', *, *, #9151, .T. ) ;
#44190=AXIS2_PLACEMENT_3D ( 'NONE', #931, #23817, #12530 ) ;
#44199=EDGE_CURVE ( 'NONE', #17390, #53342, #4733, .T. ) ;
#44207=DIRECTION ( 'NONE',  ( -1.000000000000000000, -0.000000000000000000, 0.000000000000000000 ) ) ;
#44215=CIRCLE ( 'NONE', #53809, 82.00000000000000000 ) ;
#44216=ORIENTED_EDGE ( 'NONE', *, *, #36168, .T. ) ;
#44229=ADVANCED_FACE ( 'NONE', ( #60906 ), #42885, .T. ) ;
#44245=AXIS2_PLACEMENT_3D ( 'NONE', #14096, #37044, #54339 ) ;
#44248=VECTOR ( 'NONE', #26753, 1000.000000000000000 ) ;
#44253=CARTESIAN_POINT ( 'NONE',  ( 0.000000000000000000, -62.50329211542407393, -41.76937507738853839 ) ) ;
#44257=EDGE_CURVE ( 'NONE', #22755, #15522, #71942, .T. ) ;
#44262=AXIS2_PLACEMENT_3D ( 'NONE', #29823, #1322, #64067 ) ;
#44266=AXIS2_PLACEMENT_3D ( 'NONE', #37643, #9057, #4928 ) ;
#44270=EDGE_LOOP ( 'NONE', ( #3629, #41432, #52988, #28742 ) ) ;
#44280=CARTESIAN_POINT ( 'NONE',  ( 10.00000000000000000, -31.47745569255092235, -68.26794271651296242 ) ) ;
#44303=CYLINDRICAL_SURFACE ( 'NONE', #2131, 31.99999999999999289 ) ;
#44305=CARTESIAN_POINT ( 'NONE',  ( 10.00000000000000000, -51.02545421589285723, -55.20638768913812555 ) ) ;
#44308=ORIENTED_EDGE ( 'NONE', *, *, #59887, .T. ) ;
#44311=VECTOR ( 'NONE', #24085, 1000.000000000000000 ) ;
#44321=AXIS2_PLACEMENT_3D ( 'NONE', #27735, #60481, #73585 ) ;
#44327=ORIENTED_EDGE ( 'NONE', *, *, #36217, .F. ) ;
#44330=CARTESIAN_POINT ( 'NONE',  ( 10.00000000000000000, -2.956366410620109519, -75.11725578898472122 ) ) ;
#44331=CARTESIAN_POINT ( 'NONE',  ( 10.00000000000000000, 0.000000000000000000, 0.000000000000000000 ) ) ;
#44336=ADVANCED_FACE ( 'NONE', ( #26680 ), #31581, .T. ) ;
#44337=CARTESIAN_POINT ( 'NONE',  ( 0.000000000000000000, -75.11764819372145041, 29.05362095685286761 ) ) ;
#44346=EDGE_CURVE ( 'NONE', #57622, #43494, #9768, .T. ) ;
#44364=AXIS2_PLACEMENT_3D ( 'NONE', #24606, #65213, #30604 ) ;
#44368=VECTOR ( 'NONE', #38470, 1000.000000000000000 ) ;
#44379=EDGE_CURVE ( 'NONE', #55291, #54928, #25947, .T. ) ;
#44380=CARTESIAN_POINT ( 'NONE',  ( 10.00000000000000000, 34.94270380257639630, 74.18225833017902460 ) ) ;
#44394=DIRECTION ( 'NONE',  ( -1.000000000000000000, -0.000000000000000000, -0.000000000000000000 ) ) ;
#44398=CIRCLE ( 'NONE', #21, 82.00000000000000000 ) ;
#44399=AXIS2_PLACEMENT_3D ( 'NONE', #35459, #46751, #41838 ) ;
#44401=ORIENTED_EDGE ( 'NONE', *, *, #63332, .T. ) ;
#44402=ORIENTED_EDGE ( 'NONE', *, *, #31914, .F. ) ;
#44415=ORIENTED_EDGE ( 'NONE', *, *, #19660, .T. ) ;
#44426=CARTESIAN_POINT ( 'NONE',  ( 10.00000000000000000, -11.30684508768395524, 76.66974797899831628 ) ) ;
#44427=CARTESIAN_POINT ( 'NONE',  ( 5.000000000000002665, 34.94270380257639630, 74.18225833017899618 ) ) ;
#44443=DIRECTION ( 'NONE',  ( -1.000000000000000000, 0.000000000000000000, 0.000000000000000000 ) ) ;
#44444=VERTEX_POINT ( 'NONE', #34549 ) ;
#44446=DIRECTION ( 'NONE',  ( 0.000000000000000000, 0.000000000000000000, 1.000000000000000000 ) ) ;
#44447=LINE ( 'NONE', #50055, #11725 ) ;
#44452=ORIENTED_EDGE ( 'NONE', *, *, #17994, .F. ) ;
#44458=AXIS2_PLACEMENT_3D ( 'NONE', #58960, #64974, #63869 ) ;
#44460=AXIS2_PLACEMENT_3D ( 'NONE', #1019, #25010, #47951 ) ;
#44462=AXIS2_PLACEMENT_3D ( 'NONE', #14618, #20250, #27002 ) ;
#44465=EDGE_CURVE ( 'NONE', #21230, #73771, #26327, .T. ) ;
#44484=AXIS2_PLACEMENT_3D ( 'NONE', #36585, #2053, #30572 ) ;
#44485=CIRCLE ( 'NONE', #6076, 31.99999999999999289 ) ;
#44486=ORIENTED_EDGE ( 'NONE', *, *, #34273, .T. ) ;
#44500=LINE ( 'NONE', #56138, #57135 ) ;
#44503=CARTESIAN_POINT ( 'NONE',  ( 10.00000000000000000, 70.53064760720278059, 26.01480285779964774 ) ) ;
#44509=EDGE_CURVE ( 'NONE', #34480, #32553, #71998, .T. ) ;
#44510=ORIENTED_EDGE ( 'NONE', *, *, #12415, .T. ) ;
#44514=DIRECTION ( 'NONE',  ( -1.000000000000000000, 0.000000000000000000, 0.000000000000000000 ) ) ;
#44520=AXIS2_PLACEMENT_3D ( 'NONE', #63051, #51362, #51742 ) ;
#44524=EDGE_LOOP ( 'NONE', ( #2452, #4071, #29554, #71726 ) ) ;
#44528=DIRECTION ( 'NONE',  ( 1.000000000000000000, 0.000000000000000000, 0.000000000000000000 ) ) ;
#44530=DIRECTION ( 'NONE',  ( -1.000000000000000000, 0.000000000000000000, -0.000000000000000000 ) ) ;
#44532=DIRECTION ( 'NONE',  ( 0.000000000000000000, 0.000000000000000000, 1.000000000000000000 ) ) ;
#44537=CIRCLE ( 'NONE', #43365, 82.00000000000000000 ) ;
#44544=CIRCLE ( 'NONE', #51768, 32.00000000000000000 ) ;
#44546=CARTESIAN_POINT ( 'NONE',  ( 10.00000000000000000, 75.11764819372149304, -2.946379043146603482 ) ) ;
#44558=ORIENTED_EDGE ( 'NONE', *, *, #59741, .T. ) ;
#44564=EDGE_CURVE ( 'NONE', #20634, #70074, #52580, .T. ) ;
#44569=ORIENTED_EDGE ( 'NONE', *, *, #33938, .F. ) ;
#44570=VERTEX_POINT ( 'NONE', #13466 ) ;
#44590=DIRECTION ( 'NONE',  ( -1.000000000000000000, -0.000000000000000000, -0.000000000000000000 ) ) ;
#44613=CYLINDRICAL_SURFACE ( 'NONE', #62737, 77.49899999999999523 ) ;
#44617=VERTEX_POINT ( 'NONE', #46954 ) ;
#44619=CARTESIAN_POINT ( 'NONE',  ( 10.00000000000000000, 79.10210256391397365, -21.60688246758502373 ) ) ;
#44625=VERTEX_POINT ( 'NONE', #52961 ) ;
#44630=CIRCLE ( 'NONE', #63847, 32.00000000000000000 ) ;
#44631=FACE_OUTER_BOUND ( 'NONE', #12275, .T. ) ;
#44635=CARTESIAN_POINT ( 'NONE',  ( 0.000000000000000000, 0.000000000000000000, 0.000000000000000000 ) ) ;
#44639=AXIS2_PLACEMENT_3D ( 'NONE', #39708, #4386, #33293 ) ;
#44645=ORIENTED_EDGE ( 'NONE', *, *, #71042, .T. ) ;
#44659=EDGE_CURVE ( 'NONE', #70889, #42280, #36393, .T. ) ;
#44666=CARTESIAN_POINT ( 'NONE',  ( 10.00000000000000000, 0.000000000000000000, 0.000000000000000000 ) ) ;
#44673=ORIENTED_EDGE ( 'NONE', *, *, #22417, .T. ) ;
#44677=FACE_OUTER_BOUND ( 'NONE', #44524, .T. ) ;
#44689=ORIENTED_EDGE ( 'NONE', *, *, #16403, .F. ) ;
#44697=CYLINDRICAL_SURFACE ( 'NONE', #16186, 77.49899999999999523 ) ;
#44699=VERTEX_POINT ( 'NONE', #12356 ) ;
#44701=AXIS2_PLACEMENT_3D ( 'NONE', #25049, #54003, #14122 ) ;
#44706=DIRECTION ( 'NONE',  ( 0.000000000000000000, -0.8526401643540970632, 0.5224985647159409163 ) ) ;
#44722=CARTESIAN_POINT ( 'NONE',  ( 0.000000000000000000, 0.000000000000000000, 0.000000000000000000 ) ) ;
#44731=CARTESIAN_POINT ( 'NONE',  ( 10.00000000000000000, 73.72996012237460661, -14.67089635893632504 ) ) ;
#44733=CARTESIAN_POINT ( 'NONE',  ( 10.00000000000000000, 0.000000000000000000, 0.000000000000000000 ) ) ;
#44737=ADVANCED_FACE ( 'NONE', ( #20957 ), #49893, .T. ) ;
#44742=DIRECTION ( 'NONE',  ( -1.000000000000000000, 0.000000000000000000, 0.000000000000000000 ) ) ;
#44750=DIRECTION ( 'NONE',  ( -1.000000000000000000, -0.000000000000000000, -0.000000000000000000 ) ) ;
#44754=ADVANCED_FACE ( 'NONE', ( #43910 ), #15315, .T. ) ;
#44760=EDGE_CURVE ( 'NONE', #7655, #7152, #70812, .T. ) ;
#44768=ORIENTED_EDGE ( 'NONE', *, *, #34103, .F. ) ;
#44779=CARTESIAN_POINT ( 'NONE',  ( 10.00000000000000000, -3.894527615418464705, 81.90746397400387480 ) ) ;
#44785=CARTESIAN_POINT ( 'NONE',  ( 0.000000000000000000, 26.02418014898407961, -70.52718814184231633 ) ) ;
#44798=DIRECTION ( 'NONE',  ( 0.000000000000000000, 0.7604059656000322631, -0.6494480483301821039 ) ) ;
#44812=CYLINDRICAL_SURFACE ( 'NONE', #44850, 31.99999999999999289 ) ;
#44830=CARTESIAN_POINT ( 'NONE',  ( 0.000000000000000000, -39.47590169984793818, -71.87247863392457248 ) ) ;
#44831=VECTOR ( 'NONE', #32054, 1000.000000000000000 ) ;
#44848=VECTOR ( 'NONE', #32676, 1000.000000000000000 ) ;
#44850=AXIS2_PLACEMENT_3D ( 'NONE', #56083, #4602, #44446 ) ;
#44855=VERTEX_POINT ( 'NONE', #10051 ) ;
#44863=ORIENTED_EDGE ( 'NONE', *, *, #38868, .T. ) ;
#44866=ORIENTED_EDGE ( 'NONE', *, *, #71390, .T. ) ;
#44869=DIRECTION ( 'NONE',  ( -1.000000000000000000, 0.000000000000000000, -0.000000000000000000 ) ) ;
#44882=DIRECTION ( 'NONE',  ( -1.000000000000000000, 0.000000000000000000, 0.000000000000000000 ) ) ;
#44888=CYLINDRICAL_SURFACE ( 'NONE', #43899, 32.00000000000000000 ) ;
#44891=DIRECTION ( 'NONE',  ( -1.000000000000000000, -0.000000000000000000, 0.000000000000000000 ) ) ;
#44893=EDGE_LOOP ( 'NONE', ( #56974, #31234, #59819, #32245 ) ) ;
#44902=DIRECTION ( 'NONE',  ( -1.000000000000000000, -0.000000000000000000, 0.000000000000000000 ) ) ;
#44910=AXIS2_PLACEMENT_3D ( 'NONE', #68489, #16981, #39920 ) ;
#44912=DIRECTION ( 'NONE',  ( -1.000000000000000000, 0.000000000000000000, 0.000000000000000000 ) ) ;
#44916=DIRECTION ( 'NONE',  ( 0.000000000000000000, 0.000000000000000000, 1.000000000000000000 ) ) ;
#44930=ORIENTED_EDGE ( 'NONE', *, *, #67126, .T. ) ;
#44942=ORIENTED_EDGE ( 'NONE', *, *, #27311, .T. ) ;
#44951=VERTEX_POINT ( 'NONE', #73198 ) ;
#44963=VERTEX_POINT ( 'NONE', #16435 ) ;
#44972=LINE ( 'NONE', #73893, #22243 ) ;
#44979=CARTESIAN_POINT ( 'NONE',  ( 0.000000000000000000, 55.38113227695782115, 54.21277698773695164 ) ) ;
#44984=EDGE_CURVE ( 'NONE', #43091, #59828, #1222, .T. ) ;
#44996=CIRCLE ( 'NONE', #6563, 77.49900000000000944 ) ;
#45006=AXIS2_PLACEMENT_3D ( 'NONE', #10765, #67538, #33693 ) ;
#45007=EDGE_CURVE ( 'NONE', #67479, #53775, #16850, .T. ) ;
#45013=ORIENTED_EDGE ( 'NONE', *, *, #70260, .F. ) ;
#45017=DIRECTION ( 'NONE',  ( -1.000000000000000000, -0.000000000000000000, -0.000000000000000000 ) ) ;
#45019=ADVANCED_FACE ( 'NONE', ( #2795 ), #25684, .T. ) ;
#45030=DIRECTION ( 'NONE',  ( -1.000000000000000000, -0.000000000000000000, 0.000000000000000000 ) ) ;
#45038=ORIENTED_EDGE ( 'NONE', *, *, #30371, .T. ) ;
#45041=AXIS2_PLACEMENT_3D ( 'NONE', #37835, #49470, #42363 ) ;
#45044=ORIENTED_EDGE ( 'NONE', *, *, #12415, .F. ) ;
#45057=AXIS2_PLACEMENT_3D ( 'NONE', #52255, #63556, #46620 ) ;
#45062=CARTESIAN_POINT ( 'NONE',  ( 0.000000000000000000, 0.000000000000000000, 0.000000000000000000 ) ) ;
#45063=DIRECTION ( 'NONE',  ( -1.000000000000000000, 0.000000000000000000, -0.000000000000000000 ) ) ;
#45069=EDGE_LOOP ( 'NONE', ( #6849, #49553, #39763, #19606 ) ) ;
#45077=ORIENTED_EDGE ( 'NONE', *, *, #59722, .T. ) ;
#45083=DIRECTION ( 'NONE',  ( -1.000000000000000000, 0.000000000000000000, 0.000000000000000000 ) ) ;
#45084=FACE_OUTER_BOUND ( 'NONE', #58414, .T. ) ;
#45086=ADVANCED_FACE ( 'NONE', ( #53889 ), #6282, .T. ) ;
#45095=FACE_OUTER_BOUND ( 'NONE', #20945, .T. ) ;
#45099=EDGE_CURVE ( 'NONE', #71285, #31085, #69414, .T. ) ;
#45104=CARTESIAN_POINT ( 'NONE',  ( 5.000000000000002665, 10.30890764327501863, -81.34940948281325745 ) ) ;
#45107=ADVANCED_FACE ( 'NONE', ( #71903 ), #48251, .T. ) ;
#45113=CARTESIAN_POINT ( 'NONE',  ( -10.00000000000000000, 0.000000000000000000, 0.000000000000000000 ) ) ;
#45114=VECTOR ( 'NONE', #70081, 1000.000000000000000 ) ;
#45129=DIRECTION ( 'NONE',  ( 0.000000000000000000, 0.000000000000000000, 1.000000000000000000 ) ) ;
#45132=DIRECTION ( 'NONE',  ( -1.000000000000000000, 0.000000000000000000, 0.000000000000000000 ) ) ;
#45139=EDGE_CURVE ( 'NONE', #9979, #30261, #44485, .T. ) ;
#45142=VERTEX_POINT ( 'NONE', #56491 ) ;
#45145=VERTEX_POINT ( 'NONE', #62124 ) ;
#45148=CARTESIAN_POINT ( 'NONE',  ( -10.00000000000000000, 0.000000000000000000, 0.000000000000000000 ) ) ;
#45153=DIRECTION ( 'NONE',  ( -1.000000000000000000, -0.000000000000000000, -0.000000000000000000 ) ) ;
#45159=EDGE_LOOP ( 'NONE', ( #24156, #27725, #15524, #37732 ) ) ;
#45162=VERTEX_POINT ( 'NONE', #21889 ) ;
#45169=DIRECTION ( 'NONE',  ( -1.000000000000000000, -0.000000000000000000, 0.000000000000000000 ) ) ;
#45170=CARTESIAN_POINT ( 'NONE',  ( 0.000000000000000000, 5.256550761632864166, 77.32052557432842832 ) ) ;
#45173=ORIENTED_EDGE ( 'NONE', *, *, #28596, .F. ) ;
#45175=CIRCLE ( 'NONE', #36730, 77.49900000000000944 ) ;
#45188=FACE_OUTER_BOUND ( 'NONE', #6736, .T. ) ;
#45190=CARTESIAN_POINT ( 'NONE',  ( 0.000000000000000000, -78.73519480814938731, -22.90783923731713756 ) ) ;
#45195=DIRECTION ( 'NONE',  ( -1.000000000000000000, 0.000000000000000000, 0.000000000000000000 ) ) ;
#45203=DIRECTION ( 'NONE',  ( 0.000000000000000000, -0.3826834323650772363, -0.9238795325112919565 ) ) ;
#45215=ORIENTED_EDGE ( 'NONE', *, *, #69548, .T. ) ;
#45224=DIRECTION ( 'NONE',  ( 1.000000000000000000, 0.000000000000000000, 0.000000000000000000 ) ) ;
#45244=CARTESIAN_POINT ( 'NONE',  ( 10.00000000000000000, 0.000000000000000000, 0.000000000000000000 ) ) ;
#45258=CARTESIAN_POINT ( 'NONE',  ( 0.000000000000000000, -3.894527615418464705, 81.90746397400387480 ) ) ;
#45264=DIRECTION ( 'NONE',  ( 0.000000000000000000, 0.9510565162951544194, -0.3090169943749448422 ) ) ;
#45265=EDGE_LOOP ( 'NONE', ( #8237, #59626, #14425, #52243 ) ) ;
#45275=CARTESIAN_POINT ( 'NONE',  ( -10.00000000000000000, 0.000000000000000000, 0.000000000000000000 ) ) ;
#45283=EDGE_CURVE ( 'NONE', #44855, #32719, #11343, .T. ) ;
#45285=CARTESIAN_POINT ( 'NONE',  ( 10.00000000000000000, 74.65491531819105830, 8.830959090343693418 ) ) ;
#45286=FACE_OUTER_BOUND ( 'NONE', #29393, .T. ) ;
#45289=CARTESIAN_POINT ( 'NONE',  ( 10.00000000000000000, -74.65491531819111515, -8.830959090343204920 ) ) ;
#45291=CIRCLE ( 'NONE', #53634, 82.00000000000000000 ) ;
#45306=EDGE_LOOP ( 'NONE', ( #35999, #52795, #65235, #11731 ) ) ;
#45308=CARTESIAN_POINT ( 'NONE',  ( 10.00000000000000000, 41.76106447765489094, 62.50884508063442269 ) ) ;
#45311=ORIENTED_EDGE ( 'NONE', *, *, #55835, .F. ) ;
#45318=CARTESIAN_POINT ( 'NONE',  ( 0.000000000000000000, -62.50329211542465657, 41.76937507738766442 ) ) ;
#45326=VERTEX_POINT ( 'NONE', #35397 ) ;
#45331=CIRCLE ( 'NONE', #46493, 32.00000000000000000 ) ;
#45335=CARTESIAN_POINT ( 'NONE',  ( 0.000000000000000000, 0.000000000000000000, 0.000000000000000000 ) ) ;
#45347=ORIENTED_EDGE ( 'NONE', *, *, #18672, .T. ) ;
#45351=CYLINDRICAL_SURFACE ( 'NONE', #44639, 82.00000000000000000 ) ;
#45353=ORIENTED_EDGE ( 'NONE', *, *, #65020, .T. ) ;
#45363=CIRCLE ( 'NONE', #28530, 77.49899999999999523 ) ;
#45377=DIRECTION ( 'NONE',  ( -1.000000000000000000, 0.000000000000000000, -0.000000000000000000 ) ) ;
#45404=VECTOR ( 'NONE', #17828, 1000.000000000000000 ) ;
#45414=ADVANCED_FACE ( 'NONE', ( #56854 ), #51940, .T. ) ;
#45416=ORIENTED_EDGE ( 'NONE', *, *, #8009, .T. ) ;
#45422=CYLINDRICAL_SURFACE ( 'NONE', #30482, 77.49899999999999523 ) ;
#45424=DIRECTION ( 'NONE',  ( -1.000000000000000000, -0.000000000000000000, -0.000000000000000000 ) ) ;
#45427=ORIENTED_EDGE ( 'NONE', *, *, #72462, .T. ) ;
#45431=ORIENTED_EDGE ( 'NONE', *, *, #57494, .F. ) ;
#45434=EDGE_CURVE ( 'NONE', #38362, #66220, #34874, .T. ) ;
#45443=CARTESIAN_POINT ( 'NONE',  ( 5.000000000000000000, -59.75363087400035056, -56.15606465355021015 ) ) ;
#45462=AXIS2_PLACEMENT_3D ( 'NONE', #17813, #13283, #41134 ) ;
#45469=DIRECTION ( 'NONE',  ( 0.000000000000000000, 0.000000000000000000, 1.000000000000000000 ) ) ;
#45475=DIRECTION ( 'NONE',  ( 1.000000000000000000, 0.000000000000000000, -0.000000000000000000 ) ) ;
#45477=DIRECTION ( 'NONE',  ( 0.000000000000000000, 0.9510565162951521989, 0.3090169943749515591 ) ) ;
#45486=CIRCLE ( 'NONE', #14331, 31.99999999999999645 ) ;
#45488=DIRECTION ( 'NONE',  ( 0.000000000000000000, 0.000000000000000000, 1.000000000000000000 ) ) ;
#45495=ORIENTED_EDGE ( 'NONE', *, *, #6199, .T. ) ;
#45496=ADVANCED_FACE ( 'NONE', ( #36127 ), #48517, .T. ) ;
#45505=EDGE_CURVE ( 'NONE', #64894, #35896, #8295, .T. ) ;
#45506=VERTEX_POINT ( 'NONE', #53425 ) ;
#45509=VERTEX_POINT ( 'NONE', #53788 ) ;
#45523=DIRECTION ( 'NONE',  ( 0.000000000000000000, 0.000000000000000000, 1.000000000000000000 ) ) ;
#45525=ORIENTED_EDGE ( 'NONE', *, *, #52344, .F. ) ;
#45528=LINE ( 'NONE', #34589, #69306 ) ;
#45530=CYLINDRICAL_SURFACE ( 'NONE', #654, 31.99999999999999289 ) ;
#45531=ORIENTED_EDGE ( 'NONE', *, *, #36471, .T. ) ;
#45535=CARTESIAN_POINT ( 'NONE',  ( 10.00000000000000000, -65.64334221924939072, 41.19522573413710376 ) ) ;
#45539=VERTEX_POINT ( 'NONE', #7194 ) ;
#45562=CARTESIAN_POINT ( 'NONE',  ( 10.00000000000000000, -20.41045688087876897, 72.35160999960810102 ) ) ;
#45565=FACE_OUTER_BOUND ( 'NONE', #73499, .T. ) ;
#45573=AXIS2_PLACEMENT_3D ( 'NONE', #47409, #70314, #71424 ) ;
#45601=DIRECTION ( 'NONE',  ( 0.000000000000000000, -0.9969173337331287410, 0.07845909572783489605 ) ) ;
#45603=CIRCLE ( 'NONE', #26362, 77.49900000000002365 ) ;
#45627=CARTESIAN_POINT ( 'NONE',  ( 0.000000000000000000, 39.78640506895700213, -66.50666863321957578 ) ) ;
#45629=AXIS2_PLACEMENT_3D ( 'NONE', #30959, #25702, #19682 ) ;
#45630=CYLINDRICAL_SURFACE ( 'NONE', #62326, 31.99999999999999289 ) ;
#45631=AXIS2_PLACEMENT_3D ( 'NONE', #10506, #33429, #73655 ) ;
#45639=CARTESIAN_POINT ( 'NONE',  ( 0.000000000000000000, -6.903761155838323837, 77.19088730480521576 ) ) ;
#45648=ORIENTED_EDGE ( 'NONE', *, *, #35372, .T. ) ;
#45663=DIRECTION ( 'NONE',  ( 0.000000000000000000, 0.6494480483301793283, 0.7604059656000345946 ) ) ;
#45672=AXIS2_PLACEMENT_3D ( 'NONE', #57932, #51542, #41015 ) ;
#45685=DIRECTION ( 'NONE',  ( -1.000000000000000000, 0.000000000000000000, 0.000000000000000000 ) ) ;
#45686=VERTEX_POINT ( 'NONE', #21048 ) ;
#45693=ORIENTED_EDGE ( 'NONE', *, *, #21513, .T. ) ;
#45701=ORIENTED_EDGE ( 'NONE', *, *, #34797, .F. ) ;
#45711=DIRECTION ( 'NONE',  ( -1.000000000000000000, 0.000000000000000000, 0.000000000000000000 ) ) ;
#45712=FACE_OUTER_BOUND ( 'NONE', #3881, .T. ) ;
#45715=FACE_OUTER_BOUND ( 'NONE', #9871, .T. ) ;
#45717=CARTESIAN_POINT ( 'NONE',  ( 10.00000000000000000, 0.000000000000000000, 0.000000000000000000 ) ) ;
#45720=ORIENTED_EDGE ( 'NONE', *, *, #43376, .F. ) ;
#45721=CARTESIAN_POINT ( 'NONE',  ( 10.00000000000000000, -58.39081064771787766, 50.95692526931307498 ) ) ;
#45723=ORIENTED_EDGE ( 'NONE', *, *, #32566, .F. ) ;
#45729=CARTESIAN_POINT ( 'NONE',  ( 10.00000000000000000, -29.01471420065507090, -76.69515212746047439 ) ) ;
#45739=AXIS2_PLACEMENT_3D ( 'NONE', #13874, #65042, #7878 ) ;
#45741=AXIS2_PLACEMENT_3D ( 'NONE', #7292, #29093, #30206 ) ;
#45747=VERTEX_POINT ( 'NONE', #15409 ) ;
#45748=EDGE_LOOP ( 'NONE', ( #64701, #69743, #9459, #51221 ) ) ;
#45756=CARTESIAN_POINT ( 'NONE',  ( 10.00000000000000000, -66.50666863322028632, 39.78640506895582973 ) ) ;
#45758=CYLINDRICAL_SURFACE ( 'NONE', #50174, 77.49899999999999523 ) ;
#45761=DIRECTION ( 'NONE',  ( -1.000000000000000000, -0.000000000000000000, -0.000000000000000000 ) ) ;
#45763=CIRCLE ( 'NONE', #55338, 31.99999999999999289 ) ;
#45776=CIRCLE ( 'NONE', #25369, 82.00000000000000000 ) ;
#45778=CARTESIAN_POINT ( 'NONE',  ( 0.000000000000000000, -8.840884882374576037, -74.65374052328658649 ) ) ;
#45786=DIRECTION ( 'NONE',  ( 0.000000000000000000, 0.000000000000000000, 1.000000000000000000 ) ) ;
#45790=DIRECTION ( 'NONE',  ( 0.000000000000000000, -0.3826834323650772363, -0.9238795325112919565 ) ) ;
#45797=EDGE_CURVE ( 'NONE', #50744, #35896, #54411, .T. ) ;
#45803=ORIENTED_EDGE ( 'NONE', *, *, #63763, .F. ) ;
#45804=DIRECTION ( 'NONE',  ( -1.000000000000000000, 0.000000000000000000, 0.000000000000000000 ) ) ;
#45807=ORIENTED_EDGE ( 'NONE', *, *, #46764, .T. ) ;
#45811=ORIENTED_EDGE ( 'NONE', *, *, #59970, .T. ) ;
#45829=EDGE_LOOP ( 'NONE', ( #32076, #25804, #64961, #47836 ) ) ;
#45836=DIRECTION ( 'NONE',  ( 0.000000000000000000, 0.000000000000000000, 1.000000000000000000 ) ) ;
#45855=EDGE_CURVE ( 'NONE', #15896, #10469, #57521, .T. ) ;
#45867=FACE_OUTER_BOUND ( 'NONE', #3537, .T. ) ;
#45872=EDGE_CURVE ( 'NONE', #63343, #9632, #54085, .T. ) ;
#45876=VERTEX_POINT ( 'NONE', #54378 ) ;
#45885=ORIENTED_EDGE ( 'NONE', *, *, #6202, .T. ) ;
#45892=DIRECTION ( 'NONE',  ( 0.000000000000000000, -0.9238795325112906243, 0.3826834323650804004 ) ) ;
#45897=ORIENTED_EDGE ( 'NONE', *, *, #73186, .T. ) ;
#45899=CARTESIAN_POINT ( 'NONE',  ( 10.00000000000000000, 75.11764819372142199, 2.946379043147685728 ) ) ;
#45908=ORIENTED_EDGE ( 'NONE', *, *, #30473, .T. ) ;
#45909=LINE ( 'NONE', #1190, #57556 ) ;
#45919=CARTESIAN_POINT ( 'NONE',  ( 0.000000000000000000, 0.000000000000000000, 0.000000000000000000 ) ) ;
#45935=FACE_OUTER_BOUND ( 'NONE', #47159, .T. ) ;
#45943=EDGE_CURVE ( 'NONE', #73838, #15358, #64935, .T. ) ;
#45945=LINE ( 'NONE', #5723, #61097 ) ;
#45946=DIRECTION ( 'NONE',  ( -1.000000000000000000, 0.000000000000000000, -0.000000000000000000 ) ) ;
#45966=DIRECTION ( 'NONE',  ( 0.000000000000000000, 0.9723699203976773342, -0.2334453638559024213 ) ) ;
#45970=VERTEX_POINT ( 'NONE', #68259 ) ;
#46002=CARTESIAN_POINT ( 'NONE',  ( 0.000000000000000000, 80.28980883073758434, 16.65972982744963460 ) ) ;
#46006=ADVANCED_FACE ( 'NONE', ( #15999, #61506 ), #72395, .F. ) ;
#46014=CARTESIAN_POINT ( 'NONE',  ( 0.000000000000000000, 0.000000000000000000, 0.000000000000000000 ) ) ;
#46026=CIRCLE ( 'NONE', #20779, 31.99999999999998224 ) ;
#46042=EDGE_CURVE ( 'NONE', #37315, #33112, #7178, .T. ) ;
#46044=ORIENTED_EDGE ( 'NONE', *, *, #68326, .T. ) ;
#46047=CARTESIAN_POINT ( 'NONE',  ( 10.00000000000000000, -44.99326035066006568, -68.55367621811190304 ) ) ;
#46050=ORIENTED_EDGE ( 'NONE', *, *, #38873, .T. ) ;
#46052=CIRCLE ( 'NONE', #19569, 82.00000000000000000 ) ;
#46056=ORIENTED_EDGE ( 'NONE', *, *, #11275, .T. ) ;
#46079=CIRCLE ( 'NONE', #446, 31.99999999999999289 ) ;
#46084=CARTESIAN_POINT ( 'NONE',  ( 0.000000000000000000, -28.89263327155796901, 71.91182617369176455 ) ) ;
#46099=ORIENTED_EDGE ( 'NONE', *, *, #67416, .F. ) ;
#46126=AXIS2_PLACEMENT_3D ( 'NONE', #11194, #11550, #56702 ) ;
#46136=ORIENTED_EDGE ( 'NONE', *, *, #21445, .T. ) ;
#46141=DIRECTION ( 'NONE',  ( 0.000000000000000000, 0.000000000000000000, -1.000000000000000000 ) ) ;
#46151=DIRECTION ( 'NONE',  ( 1.000000000000000000, 0.000000000000000000, 0.000000000000000000 ) ) ;
#46169=CARTESIAN_POINT ( 'NONE',  ( 10.00000000000000000, -31.46837873495025306, 68.27212725128265447 ) ) ;
#46175=CIRCLE ( 'NONE', #68975, 32.00000000000000711 ) ;
#46179=DIRECTION ( 'NONE',  ( -1.000000000000000000, 0.000000000000000000, 0.000000000000000000 ) ) ;
#46189=CARTESIAN_POINT ( 'NONE',  ( 0.000000000000000000, -68.55367621811112144, -44.99326035066125939 ) ) ;
#46206=CARTESIAN_POINT ( 'NONE',  ( 10.00000000000000000, -36.72794159290288718, 65.59268652807197952 ) ) ;
#46207=AXIS2_PLACEMENT_3D ( 'NONE', #71719, #43188, #14587 ) ;
#46211=EDGE_CURVE ( 'NONE', #57222, #38625, #35987, .T. ) ;
#46219=DIRECTION ( 'NONE',  ( 0.000000000000000000, 0.07845909572784512398, -0.9969173337331279638 ) ) ;
#46224=DIRECTION ( 'NONE',  ( 0.000000000000000000, 0.000000000000000000, 1.000000000000000000 ) ) ;
#46225=VERTEX_POINT ( 'NONE', #46432 ) ;
#46227=CARTESIAN_POINT ( 'NONE',  ( 0.000000000000000000, -51.29473840253177741, -63.97538442413482329 ) ) ;
#46228=VECTOR ( 'NONE', #24840, 1000.000000000000000 ) ;
#46229=ORIENTED_EDGE ( 'NONE', *, *, #69543, .T. ) ;
#46243=EDGE_LOOP ( 'NONE', ( #17979, #67406, #54648, #18757 ) ) ;
#46254=DIRECTION ( 'NONE',  ( 0.000000000000000000, 0.000000000000000000, 1.000000000000000000 ) ) ;
#46256=ORIENTED_EDGE ( 'NONE', *, *, #59497, .T. ) ;
#46264=EDGE_LOOP ( 'NONE', ( #6923, #31699, #13859, #47360 ) ) ;
#46288=AXIS2_PLACEMENT_3D ( 'NONE', #40067, #63026, #26918 ) ;
#46300=DIRECTION ( 'NONE',  ( 1.000000000000000000, 0.000000000000000000, 0.000000000000000000 ) ) ;
#46310=DIRECTION ( 'NONE',  ( 0.000000000000000000, 0.000000000000000000, 1.000000000000000000 ) ) ;
#46324=ORIENTED_EDGE ( 'NONE', *, *, #46689, .F. ) ;
#46330=EDGE_CURVE ( 'NONE', #7213, #68917, #5969, .T. ) ;
#46333=AXIS2_PLACEMENT_3D ( 'NONE', #31275, #14359, #25639 ) ;
#46355=CIRCLE ( 'NONE', #48758, 31.99999999999998579 ) ;
#46383=DIRECTION ( 'NONE',  ( 0.000000000000000000, 0.000000000000000000, 1.000000000000000000 ) ) ;
#46385=CARTESIAN_POINT ( 'NONE',  ( 0.000000000000000000, 46.21855187248628738, 62.20884554314034887 ) ) ;
#46388=CIRCLE ( 'NONE', #39193, 31.99999999999998934 ) ;
#46391=LINE ( 'NONE', #34741, #39869 ) ;
#46397=AXIS2_PLACEMENT_3D ( 'NONE', #28159, #15771, #50717 ) ;
#46403=CARTESIAN_POINT ( 'NONE',  ( 10.00000000000000000, -14.67089635893658794, -73.72996012237454977 ) ) ;
#46407=ORIENTED_EDGE ( 'NONE', *, *, #54267, .T. ) ;
#46415=EDGE_CURVE ( 'NONE', #1159, #4950, #30976, .T. ) ;
#46416=ORIENTED_EDGE ( 'NONE', *, *, #15604, .F. ) ;
#46428=CYLINDRICAL_SURFACE ( 'NONE', #25877, 77.49899999999999523 ) ;
#46432=CARTESIAN_POINT ( 'NONE',  ( 10.00000000000000000, 50.95692526931414790, -58.39081064771693974 ) ) ;
#46436=ORIENTED_EDGE ( 'NONE', *, *, #915, .F. ) ;
#46437=CARTESIAN_POINT ( 'NONE',  ( -10.00000000000000000, 0.000000000000000000, 0.000000000000000000 ) ) ;
#46451=CARTESIAN_POINT ( 'NONE',  ( 10.00000000000000000, 50.23322058963347558, 64.81221759200361987 ) ) ;
#46452=FACE_OUTER_BOUND ( 'NONE', #41628, .T. ) ;
#46457=EDGE_CURVE ( 'NONE', #62129, #3606, #66065, .T. ) ;
#46470=DIRECTION ( 'NONE',  ( 0.000000000000000000, -0.6494480483301903195, 0.7604059656000252687 ) ) ;
#46476=CARTESIAN_POINT ( 'NONE',  ( 0.000000000000000000, 72.35432306680455383, 20.40083707023012494 ) ) ;
#46485=ORIENTED_EDGE ( 'NONE', *, *, #39318, .F. ) ;
#46487=DIRECTION ( 'NONE',  ( 0.000000000000000000, 0.8090169943749446757, 0.5877852522924769119 ) ) ;
#46490=DIRECTION ( 'NONE',  ( -1.000000000000000000, 0.000000000000000000, -0.000000000000000000 ) ) ;
#46491=EDGE_CURVE ( 'NONE', #58612, #62434, #40837, .T. ) ;
#46493=AXIS2_PLACEMENT_3D ( 'NONE', #38405, #67718, #3838 ) ;
#46495=VECTOR ( 'NONE', #50535, 1000.000000000000000 ) ;
#46496=EDGE_CURVE ( 'NONE', #12032, #14707, #21170, .T. ) ;
#46500=CIRCLE ( 'NONE', #21259, 77.49899999999999523 ) ;
#46506=VERTEX_POINT ( 'NONE', #26818 ) ;
#46533=CARTESIAN_POINT ( 'NONE',  ( 10.00000000000000000, 0.000000000000000000, 0.000000000000000000 ) ) ;
#46535=ORIENTED_EDGE ( 'NONE', *, *, #29338, .F. ) ;
#46560=AXIS2_PLACEMENT_3D ( 'NONE', #52666, #30096, #6447 ) ;
#46561=CARTESIAN_POINT ( 'NONE',  ( 0.000000000000000000, 0.000000000000000000, 0.000000000000000000 ) ) ;
#46566=CARTESIAN_POINT ( 'NONE',  ( 10.00000000000000000, 58.39081064771823293, -50.95692526931266286 ) ) ;
#46577=CIRCLE ( 'NONE', #9381, 77.49900000000000944 ) ;
#46581=CARTESIAN_POINT ( 'NONE',  ( 0.000000000000000000, 0.000000000000000000, 0.000000000000000000 ) ) ;
#46585=ADVANCED_FACE ( 'NONE', ( #12492 ), #57639, .T. ) ;
#46599=ORIENTED_EDGE ( 'NONE', *, *, #69208, .T. ) ;
#46601=EDGE_LOOP ( 'NONE', ( #48784, #18317, #1520, #5277 ) ) ;
#46606=VERTEX_POINT ( 'NONE', #62926 ) ;
#46609=ORIENTED_EDGE ( 'NONE', *, *, #16809, .F. ) ;
#46620=DIRECTION ( 'NONE',  ( 0.000000000000000000, 0.000000000000000000, 1.000000000000000000 ) ) ;
#46622=AXIS2_PLACEMENT_3D ( 'NONE', #33090, #21433, #54554 ) ;
#46623=ORIENTED_EDGE ( 'NONE', *, *, #8009, .F. ) ;
#46640=CARTESIAN_POINT ( 'NONE',  ( 0.000000000000000000, -60.67117009219098378, -55.16347631943106933 ) ) ;
#46658=CARTESIAN_POINT ( 'NONE',  ( 0.000000000000000000, 10.30890764327501863, -81.34940948281325745 ) ) ;
#46659=CIRCLE ( 'NONE', #55078, 31.99999999999998934 ) ;
#46664=DIRECTION ( 'NONE',  ( -1.000000000000000000, 0.000000000000000000, -0.000000000000000000 ) ) ;
#46671=EDGE_CURVE ( 'NONE', #70724, #52790, #25210, .T. ) ;
#46680=LINE ( 'NONE', #12820, #40354 ) ;
#46681=ORIENTED_EDGE ( 'NONE', *, *, #35555, .T. ) ;
#46689=EDGE_CURVE ( 'NONE', #64668, #65945, #6500, .T. ) ;
#46693=ORIENTED_EDGE ( 'NONE', *, *, #49325, .F. ) ;
#46694=VERTEX_POINT ( 'NONE', #46721 ) ;
#46696=DIRECTION ( 'NONE',  ( 0.000000000000000000, 0.000000000000000000, 1.000000000000000000 ) ) ;
#46697=DIRECTION ( 'NONE',  ( -1.000000000000000000, -0.000000000000000000, 0.000000000000000000 ) ) ;
#46715=DIRECTION ( 'NONE',  ( -1.000000000000000000, 0.000000000000000000, 0.000000000000000000 ) ) ;
#46721=CARTESIAN_POINT ( 'NONE',  ( 10.00000000000000000, -76.69515212746036070, 29.01471420065537643 ) ) ;
#46728=CYLINDRICAL_SURFACE ( 'NONE', #41933, 31.99999999999999289 ) ;
#46732=AXIS2_PLACEMENT_3D ( 'NONE', #73544, #18258, #69037 ) ;
#46737=DIRECTION ( 'NONE',  ( 1.000000000000000000, 0.000000000000000000, 0.000000000000000000 ) ) ;
#46751=DIRECTION ( 'NONE',  ( -1.000000000000000000, 0.000000000000000000, -0.000000000000000000 ) ) ;
#46753=ORIENTED_EDGE ( 'NONE', *, *, #27311, .F. ) ;
#46764=EDGE_CURVE ( 'NONE', #54641, #24857, #14409, .T. ) ;
#46765=CIRCLE ( 'NONE', #34736, 77.49899999999999523 ) ;
#46774=VECTOR ( 'NONE', #2753, 1000.000000000000000 ) ;
#46779=ORIENTED_EDGE ( 'NONE', *, *, #54405, .F. ) ;
#46783=DIRECTION ( 'NONE',  ( 1.000000000000000000, -0.000000000000000000, 0.000000000000000000 ) ) ;
#46786=CARTESIAN_POINT ( 'NONE',  ( 10.00000000000000000, -54.21277698773636899, -55.38113227695839669 ) ) ;
#46789=ORIENTED_EDGE ( 'NONE', *, *, #31331, .F. ) ;
#46791=VECTOR ( 'NONE', #56881, 1000.000000000000000 ) ;
#46792=ORIENTED_EDGE ( 'NONE', *, *, #49246, .F. ) ;
#46797=VERTEX_POINT ( 'NONE', #64752 ) ;
#46806=DIRECTION ( 'NONE',  ( 0.000000000000000000, 0.3090169943749483394, -0.9510565162951534202 ) ) ;
#46809=DIRECTION ( 'NONE',  ( -1.000000000000000000, -0.000000000000000000, 0.000000000000000000 ) ) ;
#46811=DIRECTION ( 'NONE',  ( -1.000000000000000000, -0.000000000000000000, 0.000000000000000000 ) ) ;
#46825=CARTESIAN_POINT ( 'NONE',  ( 10.00000000000000000, 27.74655509720669144, 77.16300072079670258 ) ) ;
#46846=CARTESIAN_POINT ( 'NONE',  ( 0.000000000000000000, 18.89407956138362010, -75.16055320797013906 ) ) ;
#46850=CARTESIAN_POINT ( 'NONE',  ( 0.000000000000000000, 74.65491531819118620, -8.830959090342659579 ) ) ;
#46853=CIRCLE ( 'NONE', #48024, 31.99999999999998579 ) ;
#46855=AXIS2_PLACEMENT_3D ( 'NONE', #20418, #63425, #46487 ) ;
#46857=EDGE_CURVE ( 'NONE', #31085, #34215, #28851, .T. ) ;
#46863=ORIENTED_EDGE ( 'NONE', *, *, #3231, .T. ) ;
#46882=DIRECTION ( 'NONE',  ( 1.000000000000000000, 0.000000000000000000, 0.000000000000000000 ) ) ;
#46884=CARTESIAN_POINT ( 'NONE',  ( 10.00000000000000000, 0.000000000000000000, 0.000000000000000000 ) ) ;
#46891=ORIENTED_EDGE ( 'NONE', *, *, #43251, .T. ) ;
#46892=ORIENTED_EDGE ( 'NONE', *, *, #23330, .F. ) ;
#46906=ORIENTED_EDGE ( 'NONE', *, *, #20017, .F. ) ;
#46909=VERTEX_POINT ( 'NONE', #67707 ) ;
#46911=DIRECTION ( 'NONE',  ( -1.000000000000000000, -0.000000000000000000, -0.000000000000000000 ) ) ;
#46915=FACE_OUTER_BOUND ( 'NONE', #53735, .T. ) ;
#46928=ORIENTED_EDGE ( 'NONE', *, *, #15523, .T. ) ;
#46929=AXIS2_PLACEMENT_3D ( 'NONE', #29905, #42321, #6979 ) ;
#46933=DIRECTION ( 'NONE',  ( -1.000000000000000000, 0.000000000000000000, -0.000000000000000000 ) ) ;
#46951=ADVANCED_FACE ( 'NONE', ( #10550 ), #9441, .T. ) ;
#46954=CARTESIAN_POINT ( 'NONE',  ( 0.000000000000000000, 34.94270380257639630, 74.18225833017899618 ) ) ;
#46971=AXIS2_PLACEMENT_3D ( 'NONE', #19339, #20824, #59963 ) ;
#46975=AXIS2_PLACEMENT_3D ( 'NONE', #3765, #32669, #13628 ) ;
#46984=ORIENTED_EDGE ( 'NONE', *, *, #45872, .T. ) ;
#46985=DIRECTION ( 'NONE',  ( 0.000000000000000000, -0.5877852522924802425, 0.8090169943749422332 ) ) ;
#46994=EDGE_LOOP ( 'NONE', ( #7791, #51519, #43120, #17743 ) ) ;
#47010=ORIENTED_EDGE ( 'NONE', *, *, #54061, .F. ) ;
#47015=DIRECTION ( 'NONE',  ( 0.000000000000000000, 0.000000000000000000, 1.000000000000000000 ) ) ;
#47018=ADVANCED_FACE ( 'NONE', ( #21837 ), #39135, .T. ) ;
#47022=EDGE_CURVE ( 'NONE', #46909, #25971, #51666, .T. ) ;
#47033=STYLED_ITEM ( 'NONE', ( #18047 ), #40864 ) ;
#47036=CARTESIAN_POINT ( 'NONE',  ( -10.00000000000000000, 0.000000000000000000, 0.000000000000000000 ) ) ;
#47039=CIRCLE ( 'NONE', #57873, 77.49900000000000944 ) ;
#47042=CARTESIAN_POINT ( 'NONE',  ( 10.00000000000000000, 16.00000000000000000, 2.500000000000000000 ) ) ;
#47045=ORIENTED_EDGE ( 'NONE', *, *, #74190, .T. ) ;
#47046=DIRECTION ( 'NONE',  ( -1.000000000000000000, -0.000000000000000000, 0.000000000000000000 ) ) ;
#47050=DIRECTION ( 'NONE',  ( -1.000000000000000000, 0.000000000000000000, -0.000000000000000000 ) ) ;
#47054=AXIS2_PLACEMENT_3D ( 'NONE', #64198, #17951, #58537 ) ;
#47057=ORIENTED_EDGE ( 'NONE', *, *, #72382, .T. ) ;
#47069=VERTEX_POINT ( 'NONE', #68460 ) ;
#47078=DIRECTION ( 'NONE',  ( -1.000000000000000000, 0.000000000000000000, 0.000000000000000000 ) ) ;
#47080=AXIS2_PLACEMENT_3D ( 'NONE', #11524, #45017, #11892 ) ;
#47090=AXIS2_PLACEMENT_3D ( 'NONE', #57118, #6714, #52566 ) ;
#47099=ORIENTED_EDGE ( 'NONE', *, *, #51937, .F. ) ;
#47108=DIRECTION ( 'NONE',  ( 0.000000000000000000, 0.000000000000000000, -1.000000000000000000 ) ) ;
#47112=AXIS2_PLACEMENT_3D ( 'NONE', #46884, #18658, #24317 ) ;
#47116=ORIENTED_EDGE ( 'NONE', *, *, #26560, .T. ) ;
#47117=EDGE_CURVE ( 'NONE', #59210, #11931, #27677, .T. ) ;
#47145=CIRCLE ( 'NONE', #53147, 77.49899999999999523 ) ;
#47159=EDGE_LOOP ( 'NONE', ( #20424, #1379, #51142, #57060 ) ) ;
#47171=LINE ( 'NONE', #57717, #45114 ) ;
#47174=CARTESIAN_POINT ( 'NONE',  ( 10.00000000000000000, -3.894527615417343824, -81.90746397400393164 ) ) ;
#47197=VERTEX_POINT ( 'NONE', #70271 ) ;
#47201=CARTESIAN_POINT ( 'NONE',  ( 0.000000000000000000, -65.58780272294100655, 36.73666225445870737 ) ) ;
#47205=AXIS2_PLACEMENT_3D ( 'NONE', #54253, #20401, #8751 ) ;
#47218=EDGE_CURVE ( 'NONE', #50757, #9891, #48062, .T. ) ;
#47223=DIRECTION ( 'NONE',  ( -1.000000000000000000, 0.000000000000000000, -0.000000000000000000 ) ) ;
#47233=EDGE_LOOP ( 'NONE', ( #36415, #58895, #40996, #52872 ) ) ;
#47239=VERTEX_POINT ( 'NONE', #7145 ) ;
#47247=DIRECTION ( 'NONE',  ( -1.000000000000000000, -0.000000000000000000, 0.000000000000000000 ) ) ;
#47256=ORIENTED_EDGE ( 'NONE', *, *, #70319, .F. ) ;
#47258=VECTOR ( 'NONE', #49234, 1000.000000000000000 ) ;
#47262=LINE ( 'NONE', #13770, #14937 ) ;
#47264=DIRECTION ( 'NONE',  ( -1.000000000000000000, 0.000000000000000000, -0.000000000000000000 ) ) ;
#47276=DIRECTION ( 'NONE',  ( -1.000000000000000000, 0.000000000000000000, -0.000000000000000000 ) ) ;
#47277=AXIS2_PLACEMENT_3D ( 'NONE', #64747, #22498, #10462 ) ;
#47282=VERTEX_POINT ( 'NONE', #55878 ) ;
#47287=CARTESIAN_POINT ( 'NONE',  ( 0.000000000000000000, -68.26794271651239399, -31.47745569255214093 ) ) ;
#47294=EDGE_CURVE ( 'NONE', #31131, #38013, #44537, .T. ) ;
#47295=LINE ( 'NONE', #13063, #23679 ) ;
#47306=DIRECTION ( 'NONE',  ( -1.000000000000000000, 0.000000000000000000, -0.000000000000000000 ) ) ;
#47315=CYLINDRICAL_SURFACE ( 'NONE', #9593, 31.99999999999999289 ) ;
#47319=CARTESIAN_POINT ( 'NONE',  ( 10.00000000000000000, 11.30684508768339569, 76.66974797899841576 ) ) ;
#47328=VERTEX_POINT ( 'NONE', #73900 ) ;
#47330=ORIENTED_EDGE ( 'NONE', *, *, #49157, .T. ) ;
#47341=VECTOR ( 'NONE', #16177, 1000.000000000000000 ) ;
#47344=EDGE_CURVE ( 'NONE', #34327, #66429, #11130, .T. ) ;
#47346=CARTESIAN_POINT ( 'NONE',  ( 10.00000000000000000, 77.19088730480524418, 6.903761155838049390 ) ) ;
#47353=ORIENTED_EDGE ( 'NONE', *, *, #26545, .T. ) ;
#47360=ORIENTED_EDGE ( 'NONE', *, *, #18191, .T. ) ;
#47362=ORIENTED_EDGE ( 'NONE', *, *, #54598, .T. ) ;
#47373=LINE ( 'NONE', #41364, #26320 ) ;
#47374=CIRCLE ( 'NONE', #24565, 31.99999999999998579 ) ;
#47376=ORIENTED_EDGE ( 'NONE', *, *, #33252, .F. ) ;
#47387=CARTESIAN_POINT ( 'NONE',  ( 10.00000000000000000, -27.74655509720617275, -77.16300072079690153 ) ) ;
#47389=CARTESIAN_POINT ( 'NONE',  ( 10.00000000000000000, 74.65491531819118620, -8.830959090342659579 ) ) ;
#47409=CARTESIAN_POINT ( 'NONE',  ( 0.000000000000000000, -73.73191006444561424, -14.66109333815538918 ) ) ;
#47413=AXIS2_PLACEMENT_3D ( 'NONE', #24025, #61750, #18364 ) ;
#47416=CARTESIAN_POINT ( 'NONE',  ( -10.00000000000000000, 0.000000000000000000, 0.000000000000000000 ) ) ;
#47425=DIRECTION ( 'NONE',  ( -1.000000000000000000, -0.000000000000000000, -0.000000000000000000 ) ) ;
#47430=EDGE_CURVE ( 'NONE', #56810, #61359, #51341, .T. ) ;
#47443=ORIENTED_EDGE ( 'NONE', *, *, #39831, .F. ) ;
#47449=CIRCLE ( 'NONE', #642, 82.00000000000000000 ) ;
#47463=DIRECTION ( 'NONE',  ( -1.000000000000000000, -0.000000000000000000, -0.000000000000000000 ) ) ;
#47470=CARTESIAN_POINT ( 'NONE',  ( 10.00000000000000000, 0.000000000000000000, 0.000000000000000000 ) ) ;
#47476=ORIENTED_EDGE ( 'NONE', *, *, #61385, .T. ) ;
#47492=DIRECTION ( 'NONE',  ( -1.000000000000000000, -0.000000000000000000, 0.000000000000000000 ) ) ;
#47509=CARTESIAN_POINT ( 'NONE',  ( 5.000000000000000000, -77.16300072079641836, -27.74655509720751567 ) ) ;
#47542=LINE ( 'NONE', #2086, #73480 ) ;
#47545=ADVANCED_FACE ( 'NONE', ( #58847 ), #7345, .T. ) ;
#47548=DIRECTION ( 'NONE',  ( -1.000000000000000000, -0.000000000000000000, -0.000000000000000000 ) ) ;
#47557=FACE_OUTER_BOUND ( 'NONE', #17737, .T. ) ;
#47573=DIRECTION ( 'NONE',  ( -1.000000000000000000, 0.000000000000000000, -0.000000000000000000 ) ) ;
#47583=CIRCLE ( 'NONE', #36777, 32.00000000000000000 ) ;
#47594=VERTEX_POINT ( 'NONE', #46451 ) ;
#47599=EDGE_CURVE ( 'NONE', #53775, #56493, #42167, .T. ) ;
#47601=ORIENTED_EDGE ( 'NONE', *, *, #23573, .T. ) ;
#47607=DIRECTION ( 'NONE',  ( 0.000000000000000000, 0.000000000000000000, 1.000000000000000000 ) ) ;
#47611=DIRECTION ( 'NONE',  ( -1.000000000000000000, 0.000000000000000000, 0.000000000000000000 ) ) ;
#47631=FACE_OUTER_BOUND ( 'NONE', #41934, .T. ) ;
#47642=CARTESIAN_POINT ( 'NONE',  ( 10.00000000000000000, -72.35160999960831418, 20.41045688087797672 ) ) ;
#47652=DIRECTION ( 'NONE',  ( 1.000000000000000000, 0.000000000000000000, 0.000000000000000000 ) ) ;
#47661=FACE_OUTER_BOUND ( 'NONE', #2078, .T. ) ;
#47662=CARTESIAN_POINT ( 'NONE',  ( 10.00000000000000000, 79.10210256391367523, 21.60688246758613218 ) ) ;
#47670=CIRCLE ( 'NONE', #30808, 77.49899999999999523 ) ;
#47674=DIRECTION ( 'NONE',  ( -1.000000000000000000, 0.000000000000000000, -0.000000000000000000 ) ) ;
#47675=CIRCLE ( 'NONE', #44084, 32.00000000000000000 ) ;
#47682=CYLINDRICAL_SURFACE ( 'NONE', #22245, 82.00000000000000000 ) ;
#47689=EDGE_CURVE ( 'NONE', #968, #19228, #49405, .T. ) ;
#47700=CARTESIAN_POINT ( 'NONE',  ( 0.000000000000000000, 0.000000000000000000, 0.000000000000000000 ) ) ;
#47701=ORIENTED_EDGE ( 'NONE', *, *, #54061, .T. ) ;
#47702=ORIENTED_EDGE ( 'NONE', *, *, #50042, .T. ) ;
#47705=ORIENTED_EDGE ( 'NONE', *, *, #69333, .F. ) ;
#47721=ORIENTED_EDGE ( 'NONE', *, *, #17726, .F. ) ;
#47734=FACE_OUTER_BOUND ( 'NONE', #71074, .T. ) ;
#47739=DIRECTION ( 'NONE',  ( -1.000000000000000000, -0.000000000000000000, 0.000000000000000000 ) ) ;
#47755=DIRECTION ( 'NONE',  ( -1.000000000000000000, 0.000000000000000000, 0.000000000000000000 ) ) ;
#47757=CARTESIAN_POINT ( 'NONE',  ( 10.00000000000000000, -5.256550761632340141, -77.32052557432847095 ) ) ;
#47767=DIRECTION ( 'NONE',  ( 0.000000000000000000, 0.9238795325112851842, 0.3826834323650937786 ) ) ;
#47787=FACE_OUTER_BOUND ( 'NONE', #9799, .T. ) ;
#47791=ORIENTED_EDGE ( 'NONE', *, *, #14358, .T. ) ;
#47792=ORIENTED_EDGE ( 'NONE', *, *, #74005, .T. ) ;
#47795=AXIS2_PLACEMENT_3D ( 'NONE', #27150, #3891, #21146 ) ;
#47797=FACE_OUTER_BOUND ( 'NONE', #23022, .T. ) ;
#47800=EDGE_CURVE ( 'NONE', #19857, #54641, #15188, .T. ) ;
#47802=DIRECTION ( 'NONE',  ( 0.000000000000000000, 0.8090169943749446757, 0.5877852522924769119 ) ) ;
#47803=VERTEX_POINT ( 'NONE', #26836 ) ;
#47806=EDGE_CURVE ( 'NONE', #44570, #57845, #38122, .T. ) ;
#47809=VERTEX_POINT ( 'NONE', #38869 ) ;
#47815=CARTESIAN_POINT ( 'NONE',  ( 10.00000000000000000, 0.000000000000000000, 0.000000000000000000 ) ) ;
#47816=DIRECTION ( 'NONE',  ( 0.000000000000000000, 0.000000000000000000, 1.000000000000000000 ) ) ;
#47818=CARTESIAN_POINT ( 'NONE',  ( 10.00000000000000000, 78.73519480814954363, 22.90783923731657978 ) ) ;
#47834=CARTESIAN_POINT ( 'NONE',  ( 10.00000000000000000, 6.903761155837774943, 77.19088730480525840 ) ) ;
#47836=ORIENTED_EDGE ( 'NONE', *, *, #66287, .T. ) ;
#47840=CARTESIAN_POINT ( 'NONE',  ( 10.00000000000000000, 62.20884554314086046, -46.21855187248561236 ) ) ;
#47848=AXIS2_PLACEMENT_3D ( 'NONE', #6189, #11431, #40020 ) ;
#47849=DIRECTION ( 'NONE',  ( 0.000000000000000000, -0.2334453638559125521, 0.9723699203976750027 ) ) ;
#47859=DIRECTION ( 'NONE',  ( -1.000000000000000000, -0.000000000000000000, -0.000000000000000000 ) ) ;
#47861=CARTESIAN_POINT ( 'NONE',  ( 10.00000000000000000, 0.000000000000000000, 0.000000000000000000 ) ) ;
#47865=EDGE_CURVE ( 'NONE', #53435, #49109, #67377, .T. ) ;
#47868=DIRECTION ( 'NONE',  ( 0.000000000000000000, -0.7604059656000228262, -0.6494480483301932061 ) ) ;
#47872=AXIS2_PLACEMENT_3D ( 'NONE', #7757, #36319, #70896 ) ;
#47878=EDGE_CURVE ( 'NONE', #72116, #9910, #33212, .T. ) ;
#47882=CARTESIAN_POINT ( 'NONE',  ( 10.00000000000000000, -31.47745569255189224, 68.26794271651249346 ) ) ;
#47901=CARTESIAN_POINT ( 'NONE',  ( 10.00000000000000000, 80.55351364060609853, -15.33399622253395478 ) ) ;
#47905=CARTESIAN_POINT ( 'NONE',  ( 10.00000000000000000, 0.000000000000000000, 0.000000000000000000 ) ) ;
#47907=LINE ( 'NONE', #17486, #41091 ) ;
#47908=CARTESIAN_POINT ( 'NONE',  ( 10.00000000000000000, -50.23322058963299241, -64.81221759200398935 ) ) ;
#47910=AXIS2_PLACEMENT_3D ( 'NONE', #31510, #36049, #64627 ) ;
#47921=DIRECTION ( 'NONE',  ( -1.000000000000000000, 0.000000000000000000, 0.000000000000000000 ) ) ;
#47926=ORIENTED_EDGE ( 'NONE', *, *, #54069, .F. ) ;
#47928=CARTESIAN_POINT ( 'NONE',  ( 10.00000000000000000, 6.903761155838878061, -77.19088730480517313 ) ) ;
#47941=CIRCLE ( 'NONE', #30062, 31.99999999999999645 ) ;
#47944=AXIS2_PLACEMENT_3D ( 'NONE', #15769, #9379, #4138 ) ;
#47949=CIRCLE ( 'NONE', #23910, 77.49899999999999523 ) ;
#47951=DIRECTION ( 'NONE',  ( 0.000000000000000000, 0.000000000000000000, 1.000000000000000000 ) ) ;
#47962=ORIENTED_EDGE ( 'NONE', *, *, #48708, .F. ) ;
#47975=EDGE_CURVE ( 'NONE', #66404, #32719, #2603, .T. ) ;
#47981=ORIENTED_EDGE ( 'NONE', *, *, #16413, .T. ) ;
#47988=CARTESIAN_POINT ( 'NONE',  ( -10.00000000000000000, 0.000000000000000000, 0.000000000000000000 ) ) ;
#47990=DIRECTION ( 'NONE',  ( -1.000000000000000000, 0.000000000000000000, 0.000000000000000000 ) ) ;
#47993=ORIENTED_EDGE ( 'NONE', *, *, #26329, .F. ) ;
#47996=ORIENTED_EDGE ( 'NONE', *, *, #4803, .F. ) ;
#48001=FACE_OUTER_BOUND ( 'NONE', #631, .T. ) ;
#48015=VERTEX_POINT ( 'NONE', #64400 ) ;
#48018=AXIS2_PLACEMENT_3D ( 'NONE', #10276, #38851, #10646 ) ;
#48024=AXIS2_PLACEMENT_3D ( 'NONE', #30503, #53447, #65846 ) ;
#48026=CARTESIAN_POINT ( 'NONE',  ( 10.00000000000000000, -16.65972982744878195, -80.28980883073774066 ) ) ;
#48030=VERTEX_POINT ( 'NONE', #40350 ) ;
#48044=CARTESIAN_POINT ( 'NONE',  ( 0.000000000000000000, 0.000000000000000000, 0.000000000000000000 ) ) ;
#48047=CARTESIAN_POINT ( 'NONE',  ( 10.00000000000000000, 0.000000000000000000, 0.000000000000000000 ) ) ;
#48062=CIRCLE ( 'NONE', #67281, 32.00000000000000000 ) ;
#48066=ORIENTED_EDGE ( 'NONE', *, *, #22169, .F. ) ;
#48077=CARTESIAN_POINT ( 'NONE',  ( 10.00000000000000000, -35.91791733033426226, -68.67312586195033930 ) ) ;
#48088=DIRECTION ( 'NONE',  ( -1.000000000000000000, 0.000000000000000000, -0.000000000000000000 ) ) ;
#48089=DIRECTION ( 'NONE',  ( -1.000000000000000000, 0.000000000000000000, 0.000000000000000000 ) ) ;
#48101=EDGE_LOOP ( 'NONE', ( #55392, #66716, #14036, #32261 ) ) ;
#48113=ORIENTED_EDGE ( 'NONE', *, *, #49695, .T. ) ;
#48116=FACE_OUTER_BOUND ( 'NONE', #406, .T. ) ;
#48127=AXIS2_PLACEMENT_3D ( 'NONE', #48047, #31112, #36021 ) ;
#48129=CARTESIAN_POINT ( 'NONE',  ( 0.000000000000000000, 62.50329211542494789, -41.76937507738723099 ) ) ;
#48130=ADVANCED_FACE ( 'NONE', ( #18882 ), #37312, .T. ) ;
#48140=DIRECTION ( 'NONE',  ( -1.000000000000000000, 0.000000000000000000, -0.000000000000000000 ) ) ;
#48146=DIRECTION ( 'NONE',  ( -1.000000000000000000, -0.000000000000000000, 0.000000000000000000 ) ) ;
#48166=CARTESIAN_POINT ( 'NONE',  ( 0.000000000000000000, 0.000000000000000000, 0.000000000000000000 ) ) ;
#48175=DIRECTION ( 'NONE',  ( -1.000000000000000000, -0.000000000000000000, 0.000000000000000000 ) ) ;
#48176=ORIENTED_EDGE ( 'NONE', *, *, #48297, .T. ) ;
#48177=DIRECTION ( 'NONE',  ( -1.000000000000000000, 0.000000000000000000, 0.000000000000000000 ) ) ;
#48205=CARTESIAN_POINT ( 'NONE',  ( -10.00000000000000000, 0.000000000000000000, 0.000000000000000000 ) ) ;
#48208=AXIS2_PLACEMENT_3D ( 'NONE', #20106, #20495, #43064 ) ;
#48214=ORIENTED_EDGE ( 'NONE', *, *, #4766, .T. ) ;
#48217=CARTESIAN_POINT ( 'NONE',  ( 5.000000000000000000, 71.21200624218795383, 40.65526001592638039 ) ) ;
#48218=CARTESIAN_POINT ( 'NONE',  ( 10.00000000000000000, -73.44644590900078640, 24.73286445877676343 ) ) ;
#48219=CARTESIAN_POINT ( 'NONE',  ( 10.00000000000000000, 77.19088730480524418, 6.903761155838049390 ) ) ;
#48229=DIRECTION ( 'NONE',  ( -1.000000000000000000, 0.000000000000000000, 0.000000000000000000 ) ) ;
#48230=AXIS2_PLACEMENT_3D ( 'NONE', #50673, #73601, #11202 ) ;
#48239=EDGE_CURVE ( 'NONE', #4854, #42442, #3859, .T. ) ;
#48241=DIRECTION ( 'NONE',  ( 0.000000000000000000, 0.000000000000000000, 1.000000000000000000 ) ) ;
#48251=CYLINDRICAL_SURFACE ( 'NONE', #55260, 82.00000000000000000 ) ;
#48255=ORIENTED_EDGE ( 'NONE', *, *, #16187, .T. ) ;
#48257=CYLINDRICAL_SURFACE ( 'NONE', #23822, 31.99999999999998579 ) ;
#48261=CARTESIAN_POINT ( 'NONE',  ( 0.000000000000000000, 0.000000000000000000, 0.000000000000000000 ) ) ;
#48271=ADVANCED_FACE ( 'NONE', ( #72963 ), #26740, .T. ) ;
#48278=DIRECTION ( 'NONE',  ( -1.000000000000000000, -0.000000000000000000, -0.000000000000000000 ) ) ;
#48283=CARTESIAN_POINT ( 'NONE',  ( 5.000000000000002665, 39.47590169984944453, -71.87247863392373404 ) ) ;
#48284=CARTESIAN_POINT ( 'NONE',  ( 10.00000000000000000, 73.73191006444551476, 14.66109333815590254 ) ) ;
#48286=EDGE_CURVE ( 'NONE', #68809, #38655, #16584, .T. ) ;
#48287=DIRECTION ( 'NONE',  ( -1.000000000000000000, -0.000000000000000000, 0.000000000000000000 ) ) ;
#48290=VERTEX_POINT ( 'NONE', #9088 ) ;
#48297=EDGE_CURVE ( 'NONE', #65655, #39425, #61348, .T. ) ;
#48306=CYLINDRICAL_SURFACE ( 'NONE', #5155, 32.00000000000000000 ) ;
#48307=DIRECTION ( 'NONE',  ( 0.000000000000000000, 0.000000000000000000, -1.000000000000000000 ) ) ;
#48308=CARTESIAN_POINT ( 'NONE',  ( -10.00000000000000000, 0.000000000000000000, 0.000000000000000000 ) ) ;
#48309=EDGE_CURVE ( 'NONE', #48877, #23492, #8623, .T. ) ;
#48312=DIRECTION ( 'NONE',  ( -1.000000000000000000, 0.000000000000000000, 0.000000000000000000 ) ) ;
#48316=DIRECTION ( 'NONE',  ( -1.000000000000000000, -0.000000000000000000, -0.000000000000000000 ) ) ;
#48317=CARTESIAN_POINT ( 'NONE',  ( 5.000000000000002665, 3.894527615417891830, 81.90746397400390322 ) ) ;
#48318=DIRECTION ( 'NONE',  ( -1.000000000000000000, 0.000000000000000000, 0.000000000000000000 ) ) ;
#48320=CARTESIAN_POINT ( 'NONE',  ( 0.000000000000000000, 0.000000000000000000, 0.000000000000000000 ) ) ;
#48330=DIRECTION ( 'NONE',  ( 1.000000000000000000, 0.000000000000000000, -0.000000000000000000 ) ) ;
#48334=CIRCLE ( 'NONE', #3913, 82.00000000000000000 ) ;
#48341=ORIENTED_EDGE ( 'NONE', *, *, #37770, .F. ) ;
#48349=DIRECTION ( 'NONE',  ( 0.000000000000000000, 0.000000000000000000, 1.000000000000000000 ) ) ;
#48355=ORIENTED_EDGE ( 'NONE', *, *, #6202, .F. ) ;
#48357=CARTESIAN_POINT ( 'NONE',  ( 0.000000000000000000, 0.000000000000000000, 0.000000000000000000 ) ) ;
#48359=AXIS2_PLACEMENT_3D ( 'NONE', #36620, #66326, #54657 ) ;
#48368=ORIENTED_EDGE ( 'NONE', *, *, #39247, .F. ) ;
#48388=FACE_OUTER_BOUND ( 'NONE', #68816, .T. ) ;
#48394=EDGE_LOOP ( 'NONE', ( #67706, #11213, #29574, #69974 ) ) ;
#48395=LINE ( 'NONE', #70946, #42645 ) ;
#48399=DIRECTION ( 'NONE',  ( -1.000000000000000000, 0.000000000000000000, 0.000000000000000000 ) ) ;
#48401=DIRECTION ( 'NONE',  ( -1.000000000000000000, -0.000000000000000000, 0.000000000000000000 ) ) ;
#48414=ORIENTED_EDGE ( 'NONE', *, *, #24809, .T. ) ;
#48427=AXIS2_PLACEMENT_3D ( 'NONE', #71693, #43535, #66448 ) ;
#48429=ORIENTED_EDGE ( 'NONE', *, *, #41261, .T. ) ;
#48430=ORIENTED_EDGE ( 'NONE', *, *, #8309, .T. ) ;
#48434=FACE_OUTER_BOUND ( 'NONE', #41755, .T. ) ;
#48435=ORIENTED_EDGE ( 'NONE', *, *, #12711, .F. ) ;
#48445=ORIENTED_EDGE ( 'NONE', *, *, #24460, .T. ) ;
#48448=EDGE_CURVE ( 'NONE', #10067, #54928, #29064, .T. ) ;
#48452=DIRECTION ( 'NONE',  ( -1.000000000000000000, -0.000000000000000000, 0.000000000000000000 ) ) ;
#48453=LINE ( 'NONE', #65026, #57314 ) ;
#48454=AXIS2_PLACEMENT_3D ( 'NONE', #7366, #53227, #15214 ) ;
#48455=ORIENTED_EDGE ( 'NONE', *, *, #28881, .F. ) ;
#48464=EDGE_LOOP ( 'NONE', ( #54394, #64617, #42253, #46407 ) ) ;
#48475=EDGE_LOOP ( 'NONE', ( #34849, #67564, #18048, #73948 ) ) ;
#48477=VECTOR ( 'NONE', #37638, 1000.000000000000000 ) ;
#48478=FACE_OUTER_BOUND ( 'NONE', #45306, .T. ) ;
#48493=CARTESIAN_POINT ( 'NONE',  ( -10.00000000000000000, 0.000000000000000000, 0.000000000000000000 ) ) ;
#48505=DIRECTION ( 'NONE',  ( 0.000000000000000000, 0.000000000000000000, 1.000000000000000000 ) ) ;
#48507=DIRECTION ( 'NONE',  ( -1.000000000000000000, -0.000000000000000000, 0.000000000000000000 ) ) ;
#48513=CARTESIAN_POINT ( 'NONE',  ( 0.000000000000000000, -71.91182617369207719, 28.89263327155721228 ) ) ;
#48517=CYLINDRICAL_SURFACE ( 'NONE', #20312, 82.00000000000000000 ) ;
#48524=ORIENTED_EDGE ( 'NONE', *, *, #29965, .T. ) ;
#48530=CYLINDRICAL_SURFACE ( 'NONE', #51454, 82.00000000000000000 ) ;
#48542=ORIENTED_EDGE ( 'NONE', *, *, #5280, .T. ) ;
#48546=DIRECTION ( 'NONE',  ( 0.000000000000000000, 0.000000000000000000, 1.000000000000000000 ) ) ;
#48556=DIRECTION ( 'NONE',  ( 0.000000000000000000, 0.000000000000000000, 1.000000000000000000 ) ) ;
#48559=CARTESIAN_POINT ( 'NONE',  ( 10.00000000000000000, 0.000000000000000000, 0.000000000000000000 ) ) ;
#48580=CARTESIAN_POINT ( 'NONE',  ( 10.00000000000000000, -20.41045688087772092, -72.35160999960838524 ) ) ;
#48582=ADVANCED_FACE ( 'NONE', ( #33353 ), #38266, .T. ) ;
#48592=DIRECTION ( 'NONE',  ( 0.000000000000000000, 0.000000000000000000, 1.000000000000000000 ) ) ;
#48593=CIRCLE ( 'NONE', #16166, 82.00000000000000000 ) ;
#48609=DIRECTION ( 'NONE',  ( -1.000000000000000000, -0.000000000000000000, -0.000000000000000000 ) ) ;
#48610=ORIENTED_EDGE ( 'NONE', *, *, #60886, .F. ) ;
#48613=ADVANCED_FACE ( 'NONE', ( #39016 ), #3714, .T. ) ;
#48626=VECTOR ( 'NONE', #32165, 1000.000000000000000 ) ;
#48631=ORIENTED_EDGE ( 'NONE', *, *, #3699, .T. ) ;
#48639=AXIS2_PLACEMENT_3D ( 'NONE', #56800, #69552, #69187 ) ;
#48644=DIRECTION ( 'NONE',  ( 1.000000000000000000, 0.000000000000000000, 0.000000000000000000 ) ) ;
#48645=ORIENTED_EDGE ( 'NONE', *, *, #42018, .F. ) ;
#48649=DIRECTION ( 'NONE',  ( -1.000000000000000000, -0.000000000000000000, 0.000000000000000000 ) ) ;
#48656=EDGE_CURVE ( 'NONE', #11931, #62260, #16829, .T. ) ;
#48663=CARTESIAN_POINT ( 'NONE',  ( 10.00000000000000000, -17.28742895386139722, 75.54627589209937355 ) ) ;
#48664=DIRECTION ( 'NONE',  ( 0.000000000000000000, -0.8910065241883722287, 0.4539904997395383113 ) ) ;
#48679=ORIENTED_EDGE ( 'NONE', *, *, #10073, .F. ) ;
#48681=CIRCLE ( 'NONE', #10245, 82.00000000000000000 ) ;
#48689=ADVANCED_FACE ( 'NONE', ( #35583 ), #64178, .T. ) ;
#48696=FACE_OUTER_BOUND ( 'NONE', #13344, .T. ) ;
#48698=EDGE_CURVE ( 'NONE', #55747, #1142, #17929, .T. ) ;
#48708=EDGE_CURVE ( 'NONE', #16263, #1076, #69886, .T. ) ;
#48712=CARTESIAN_POINT ( 'NONE',  ( 5.000000000000002665, 16.65972982745046238, -80.28980883073738539 ) ) ;
#48714=DIRECTION ( 'NONE',  ( -1.000000000000000000, 0.000000000000000000, 0.000000000000000000 ) ) ;
#48716=CYLINDRICAL_SURFACE ( 'NONE', #43652, 31.99999999999999289 ) ;
#48718=EDGE_CURVE ( 'NONE', #19226, #72116, #27877, .T. ) ;
#48737=ORIENTED_EDGE ( 'NONE', *, *, #61876, .F. ) ;
#48740=EDGE_CURVE ( 'NONE', #39808, #14784, #30293, .T. ) ;
#48745=DIRECTION ( 'NONE',  ( 1.000000000000000000, 0.000000000000000000, -0.000000000000000000 ) ) ;
#48752=ORIENTED_EDGE ( 'NONE', *, *, #65869, .F. ) ;
#48758=AXIS2_PLACEMENT_3D ( 'NONE', #52647, #34995, #69206 ) ;
#48762=CARTESIAN_POINT ( 'NONE',  ( 5.000000000000000000, 40.65526001592713357, -71.21200624218752750 ) ) ;
#48766=AXIS2_PLACEMENT_3D ( 'NONE', #66915, #65460, #43277 ) ;
#48776=DIRECTION ( 'NONE',  ( -1.000000000000000000, 0.000000000000000000, 0.000000000000000000 ) ) ;
#48783=DIRECTION ( 'NONE',  ( 0.000000000000000000, -0.9510565162951565288, 0.3090169943749382919 ) ) ;
#48784=ORIENTED_EDGE ( 'NONE', *, *, #41191, .T. ) ;
#48786=FACE_OUTER_BOUND ( 'NONE', #38502, .T. ) ;
#48789=FACE_OUTER_BOUND ( 'NONE', #67389, .T. ) ;
#48794=CIRCLE ( 'NONE', #38017, 31.99999999999999645 ) ;
#48801=ADVANCED_FACE ( 'NONE', ( #23569 ), #69431, .T. ) ;
#48802=ORIENTED_EDGE ( 'NONE', *, *, #29628, .F. ) ;
#48814=LINE ( 'NONE', #37555, #71358 ) ;
#48819=EDGE_CURVE ( 'NONE', #67020, #14528, #8506, .T. ) ;
#48821=ORIENTED_EDGE ( 'NONE', *, *, #62696, .T. ) ;
#48859=CIRCLE ( 'NONE', #20034, 31.99999999999998934 ) ;
#48867=LINE ( 'NONE', #72165, #27404 ) ;
#48869=ADVANCED_FACE ( 'NONE', ( #31426 ), #2161, .T. ) ;
#48877=VERTEX_POINT ( 'NONE', #59637 ) ;
#48879=FACE_OUTER_BOUND ( 'NONE', #24154, .T. ) ;
#48881=CARTESIAN_POINT ( 'NONE',  ( 0.000000000000000000, -49.70050353004846500, -59.46389618802017907 ) ) ;
#48892=EDGE_CURVE ( 'NONE', #18118, #59010, #7398, .T. ) ;
#48896=AXIS2_PLACEMENT_3D ( 'NONE', #66965, #54949, #61346 ) ;
#48897=EDGE_LOOP ( 'NONE', ( #21285, #77, #14633, #66143 ) ) ;
#48902=DIRECTION ( 'NONE',  ( 0.000000000000000000, -0.3826834323650774028, -0.9238795325112919565 ) ) ;
#48903=ORIENTED_EDGE ( 'NONE', *, *, #16970, .F. ) ;
#48912=CARTESIAN_POINT ( 'NONE',  ( 0.000000000000000000, -41.76937507738831812, 62.50329211542423025 ) ) ;
#48921=DIRECTION ( 'NONE',  ( 1.000000000000000000, -0.000000000000000000, -0.000000000000000000 ) ) ;
#48923=ORIENTED_EDGE ( 'NONE', *, *, #74332, .T. ) ;
#48925=ORIENTED_EDGE ( 'NONE', *, *, #5001, .F. ) ;
#48930=DIRECTION ( 'NONE',  ( -1.000000000000000000, 0.000000000000000000, -0.000000000000000000 ) ) ;
#48933=CARTESIAN_POINT ( 'NONE',  ( 0.000000000000000000, 70.53064760720278059, 26.01480285779964774 ) ) ;
#48937=CARTESIAN_POINT ( 'NONE',  ( 10.00000000000000000, 0.000000000000000000, 0.000000000000000000 ) ) ;
#48941=CARTESIAN_POINT ( 'NONE',  ( 10.00000000000000000, 0.000000000000000000, 0.000000000000000000 ) ) ;
#48943=DIRECTION ( 'NONE',  ( -1.000000000000000000, -0.000000000000000000, -0.000000000000000000 ) ) ;
#48944=CIRCLE ( 'NONE', #42961, 77.49899999999999523 ) ;
#48949=CIRCLE ( 'NONE', #6935, 82.00000000000000000 ) ;
#48959=EDGE_CURVE ( 'NONE', #6553, #44444, #63906, .T. ) ;
#48962=CARTESIAN_POINT ( 'NONE',  ( 0.000000000000000000, 0.000000000000000000, 0.000000000000000000 ) ) ;
#48974=DIRECTION ( 'NONE',  ( -1.000000000000000000, 0.000000000000000000, 0.000000000000000000 ) ) ;
#48975=( NAMED_UNIT ( * ) SI_UNIT ( $, .STERADIAN. ) SOLID_ANGLE_UNIT ( ) );
#48978=CARTESIAN_POINT ( 'NONE',  ( -10.00000000000000000, 0.000000000000000000, 0.000000000000000000 ) ) ;
#48996=AXIS2_PLACEMENT_3D ( 'NONE', #51005, #34447, #5903 ) ;
#48998=ORIENTED_EDGE ( 'NONE', *, *, #28930, .F. ) ;
#49007=CIRCLE ( 'NONE', #14182, 77.49899999999999523 ) ;
#49008=DIRECTION ( 'NONE',  ( 0.000000000000000000, 0.8910065241883691201, -0.4539904997395446951 ) ) ;
#49010=DIRECTION ( 'NONE',  ( -1.000000000000000000, -0.000000000000000000, -0.000000000000000000 ) ) ;
#49020=FACE_OUTER_BOUND ( 'NONE', #22667, .T. ) ;
#49034=DIRECTION ( 'NONE',  ( -1.000000000000000000, 0.000000000000000000, 0.000000000000000000 ) ) ;
#49038=CARTESIAN_POINT ( 'NONE',  ( 10.00000000000000000, 0.000000000000000000, 0.000000000000000000 ) ) ;
#49039=DIRECTION ( 'NONE',  ( 0.000000000000000000, 0.000000000000000000, -1.000000000000000000 ) ) ;
#49044=ADVANCED_FACE ( 'NONE', ( #66353 ), #37027, .T. ) ;
#49045=DIRECTION ( 'NONE',  ( 1.000000000000000000, -0.000000000000000000, 0.000000000000000000 ) ) ;
#49048=ADVANCED_FACE ( 'NONE', ( #71964 ), #48306, .T. ) ;
#49051=DIRECTION ( 'NONE',  ( -1.000000000000000000, 0.000000000000000000, 0.000000000000000000 ) ) ;
#49061=DIRECTION ( 'NONE',  ( -1.000000000000000000, -0.000000000000000000, -0.000000000000000000 ) ) ;
#49063=CARTESIAN_POINT ( 'NONE',  ( 10.00000000000000000, 0.000000000000000000, 0.000000000000000000 ) ) ;
#49065=DIRECTION ( 'NONE',  ( -1.000000000000000000, 0.000000000000000000, 0.000000000000000000 ) ) ;
#49076=CIRCLE ( 'NONE', #1267, 82.00000000000000000 ) ;
#49078=CYLINDRICAL_SURFACE ( 'NONE', #73119, 77.49899999999999523 ) ;
#49080=ORIENTED_EDGE ( 'NONE', *, *, #14163, .F. ) ;
#49086=DIRECTION ( 'NONE',  ( -1.000000000000000000, 0.000000000000000000, -0.000000000000000000 ) ) ;
#49098=CARTESIAN_POINT ( 'NONE',  ( -10.00000000000000000, 0.000000000000000000, 0.000000000000000000 ) ) ;
#49106=ORIENTED_EDGE ( 'NONE', *, *, #56873, .T. ) ;
#49109=VERTEX_POINT ( 'NONE', #64869 ) ;
#49117=CARTESIAN_POINT ( 'NONE',  ( 10.00000000000000000, 63.97538442413500093, -51.29473840253157135 ) ) ;
#49119=CARTESIAN_POINT ( 'NONE',  ( 10.00000000000000000, 75.11764819372149304, -2.946379043146603482 ) ) ;
#49124=EDGE_CURVE ( 'NONE', #27817, #10962, #18328, .T. ) ;
#49125=DIRECTION ( 'NONE',  ( -1.000000000000000000, 0.000000000000000000, 0.000000000000000000 ) ) ;
#49128=CYLINDRICAL_SURFACE ( 'NONE', #29285, 77.49899999999999523 ) ;
#49131=CARTESIAN_POINT ( 'NONE',  ( 10.00000000000000000, -28.89263327155693517, -71.91182617369219088 ) ) ;
#49132=ORIENTED_EDGE ( 'NONE', *, *, #44760, .F. ) ;
#49153=ORIENTED_EDGE ( 'NONE', *, *, #44564, .T. ) ;
#49156=DIRECTION ( 'NONE',  ( -1.000000000000000000, -0.000000000000000000, -0.000000000000000000 ) ) ;
#49157=EDGE_CURVE ( 'NONE', #55565, #11405, #72691, .T. ) ;
#49168=AXIS2_PLACEMENT_3D ( 'NONE', #28451, #21316, #20958 ) ;
#49171=CARTESIAN_POINT ( 'NONE',  ( 0.000000000000000000, -28.89263327155693517, -71.91182617369219088 ) ) ;
#49184=DIRECTION ( 'NONE',  ( -1.000000000000000000, 0.000000000000000000, -0.000000000000000000 ) ) ;
#49187=DIRECTION ( 'NONE',  ( 0.000000000000000000, -0.5877852522924625900, -0.8090169943749551118 ) ) ;
#49190=ORIENTED_EDGE ( 'NONE', *, *, #45797, .T. ) ;
#49198=DIRECTION ( 'NONE',  ( -1.000000000000000000, 0.000000000000000000, 0.000000000000000000 ) ) ;
#49201=ORIENTED_EDGE ( 'NONE', *, *, #51278, .T. ) ;
#49205=FACE_OUTER_BOUND ( 'NONE', #66762, .T. ) ;
#49206=EDGE_CURVE ( 'NONE', #71846, #62877, #4689, .T. ) ;
#49220=AXIS2_PLACEMENT_3D ( 'NONE', #73072, #73820, #44532 ) ;
#49223=CIRCLE ( 'NONE', #50456, 31.99999999999999289 ) ;
#49233=EDGE_CURVE ( 'NONE', #42280, #18118, #30343, .T. ) ;
#49234=DIRECTION ( 'NONE',  ( -1.000000000000000000, 0.000000000000000000, 0.000000000000000000 ) ) ;
#49237=AXIS2_PLACEMENT_3D ( 'NONE', #67045, #61423, #22303 ) ;
#49239=AXIS2_PLACEMENT_3D ( 'NONE', #14069, #65979, #20084 ) ;
#49244=AXIS2_PLACEMENT_3D ( 'NONE', #70322, #31225, #59077 ) ;
#49245=DIRECTION ( 'NONE',  ( -1.000000000000000000, 0.000000000000000000, 0.000000000000000000 ) ) ;
#49246=EDGE_CURVE ( 'NONE', #71442, #3546, #57942, .T. ) ;
#49270=ORIENTED_EDGE ( 'NONE', *, *, #70110, .F. ) ;
#49271=ORIENTED_EDGE ( 'NONE', *, *, #67204, .F. ) ;
#49274=ORIENTED_EDGE ( 'NONE', *, *, #13057, .F. ) ;
#49275=LINE ( 'NONE', #37275, #18521 ) ;
#49280=CARTESIAN_POINT ( 'NONE',  ( 0.000000000000000000, -81.50828551894234408, 8.966570791700407383 ) ) ;
#49283=ORIENTED_EDGE ( 'NONE', *, *, #71170, .F. ) ;
#49284=ORIENTED_EDGE ( 'NONE', *, *, #36061, .F. ) ;
#49288=ORIENTED_EDGE ( 'NONE', *, *, #30390, .F. ) ;
#49291=ORIENTED_EDGE ( 'NONE', *, *, #74193, .F. ) ;
#49292=VERTEX_POINT ( 'NONE', #56558 ) ;
#49294=ADVANCED_FACE ( 'NONE', ( #3947 ), #50894, .T. ) ;
#49302=DIRECTION ( 'NONE',  ( 0.000000000000000000, -0.9723699203976740035, -0.2334453638559160216 ) ) ;
#49311=ORIENTED_EDGE ( 'NONE', *, *, #9782, .T. ) ;
#49313=DIRECTION ( 'NONE',  ( -1.000000000000000000, -0.000000000000000000, 0.000000000000000000 ) ) ;
#49316=DIRECTION ( 'NONE',  ( -1.000000000000000000, -0.000000000000000000, -0.000000000000000000 ) ) ;
#49317=DIRECTION ( 'NONE',  ( -1.000000000000000000, -0.000000000000000000, 0.000000000000000000 ) ) ;
#49322=CIRCLE ( 'NONE', #38546, 31.99999999999998934 ) ;
#49325=EDGE_CURVE ( 'NONE', #50470, #22556, #23174, .T. ) ;
#49329=DIRECTION ( 'NONE',  ( -1.000000000000000000, 0.000000000000000000, 0.000000000000000000 ) ) ;
#49338=VECTOR ( 'NONE', #41734, 1000.000000000000000 ) ;
#49346=AXIS2_PLACEMENT_3D ( 'NONE', #6003, #68773, #10884 ) ;
#49352=ORIENTED_EDGE ( 'NONE', *, *, #13982, .T. ) ;
#49356=CARTESIAN_POINT ( 'NONE',  ( 10.00000000000000000, -68.55367621811110723, -44.99326035066125939 ) ) ;
#49358=CARTESIAN_POINT ( 'NONE',  ( 0.000000000000000000, 50.95692526931328104, 58.39081064771769292 ) ) ;
#49361=ORIENTED_EDGE ( 'NONE', *, *, #58078, .F. ) ;
#49369=DIRECTION ( 'NONE',  ( 0.000000000000000000, 0.000000000000000000, -1.000000000000000000 ) ) ;
#49393=VERTEX_POINT ( 'NONE', #11411 ) ;
#49399=CARTESIAN_POINT ( 'NONE',  ( 10.00000000000000000, -62.50884508063453637, 41.76106447765467777 ) ) ;
#49404=CARTESIAN_POINT ( 'NONE',  ( 0.000000000000000000, 41.76937507738875155, -62.50329211542393892 ) ) ;
#49405=CIRCLE ( 'NONE', #29002, 32.00000000000000000 ) ;
#49406=DIRECTION ( 'NONE',  ( 0.000000000000000000, 0.000000000000000000, -1.000000000000000000 ) ) ;
#49408=VERTEX_POINT ( 'NONE', #34344 ) ;
#49409=AXIS2_PLACEMENT_3D ( 'NONE', #53596, #47223, #1768 ) ;
#49426=CARTESIAN_POINT ( 'NONE',  ( 10.00000000000000000, 73.95703589263975175, 23.16143007188454206 ) ) ;
#49428=DIRECTION ( 'NONE',  ( 0.000000000000000000, 0.000000000000000000, 1.000000000000000000 ) ) ;
#49434=( GEOMETRIC_REPRESENTATION_CONTEXT ( 3 ) GLOBAL_UNCERTAINTY_ASSIGNED_CONTEXT ( ( #27138 ) ) GLOBAL_UNIT_ASSIGNED_CONTEXT ( ( #37042, #8475, #42594 ) ) REPRESENTATION_CONTEXT ( 'NONE', 'WORKASPACE' ) );
#49436=AXIS2_PLACEMENT_3D ( 'NONE', #36092, #47739, #25547 ) ;
#49444=ORIENTED_EDGE ( 'NONE', *, *, #42018, .T. ) ;
#49462=ORIENTED_EDGE ( 'NONE', *, *, #24786, .T. ) ;
#49466=CARTESIAN_POINT ( 'NONE',  ( 10.00000000000000000, 0.000000000000000000, -2.500000000000000000 ) ) ;
#49468=EDGE_CURVE ( 'NONE', #29598, #29474, #1932, .T. ) ;
#49470=DIRECTION ( 'NONE',  ( 1.000000000000000000, 0.000000000000000000, 0.000000000000000000 ) ) ;
#49474=VERTEX_POINT ( 'NONE', #71774 ) ;
#49477=FACE_OUTER_BOUND ( 'NONE', #14990, .T. ) ;
#49483=CARTESIAN_POINT ( 'NONE',  ( 10.00000000000000000, -51.03279382321048985, -55.19960302592120627 ) ) ;
#49484=DIRECTION ( 'NONE',  ( 0.000000000000000000, 0.000000000000000000, 1.000000000000000000 ) ) ;
#49490=DIRECTION ( 'NONE',  ( 0.000000000000000000, -0.07845909572783053842, -0.9969173337331290741 ) ) ;
#49495=AXIS2_PLACEMENT_3D ( 'NONE', #21764, #67632, #66526 ) ;
#49499=AXIS2_PLACEMENT_3D ( 'NONE', #7046, #25080, #8540 ) ;
#49502=CARTESIAN_POINT ( 'NONE',  ( 0.000000000000000000, 68.27212725128275395, -31.46837873495001503 ) ) ;
#49506=CIRCLE ( 'NONE', #1579, 77.49899999999999523 ) ;
#49511=CARTESIAN_POINT ( 'NONE',  ( 10.00000000000000000, -31.46837873495025306, 68.27212725128265447 ) ) ;
#49513=DIRECTION ( 'NONE',  ( -1.000000000000000000, 0.000000000000000000, -0.000000000000000000 ) ) ;
#49515=FACE_OUTER_BOUND ( 'NONE', #9153, .T. ) ;
#49517=CARTESIAN_POINT ( 'NONE',  ( 10.00000000000000000, 68.26794271651262136, 31.47745569255165066 ) ) ;
#49522=CARTESIAN_POINT ( 'NONE',  ( 10.00000000000000000, 0.000000000000000000, 0.000000000000000000 ) ) ;
#49525=DIRECTION ( 'NONE',  ( 0.000000000000000000, 0.000000000000000000, 1.000000000000000000 ) ) ;
#49527=EDGE_CURVE ( 'NONE', #10067, #62877, #23223, .T. ) ;
#49533=EDGE_CURVE ( 'NONE', #34583, #8597, #19905, .T. ) ;
#49538=LINE ( 'NONE', #32613, #37778 ) ;
#49539=AXIS2_PLACEMENT_3D ( 'NONE', #23944, #46882, #46141 ) ;
#49544=EDGE_CURVE ( 'NONE', #45145, #3846, #64008, .T. ) ;
#49553=ORIENTED_EDGE ( 'NONE', *, *, #19333, .T. ) ;
#49560=VERTEX_POINT ( 'NONE', #14272 ) ;
#49567=ORIENTED_EDGE ( 'NONE', *, *, #22227, .F. ) ;
#49569=VERTEX_POINT ( 'NONE', #36834 ) ;
#49576=EDGE_LOOP ( 'NONE', ( #11268, #58, #17693, #59023 ) ) ;
#49579=ORIENTED_EDGE ( 'NONE', *, *, #54807, .F. ) ;
#49584=CYLINDRICAL_SURFACE ( 'NONE', #49495, 31.99999999999998579 ) ;
#49596=AXIS2_PLACEMENT_3D ( 'NONE', #37457, #20880, #26145 ) ;
#49597=DIRECTION ( 'NONE',  ( -1.000000000000000000, -0.000000000000000000, -0.000000000000000000 ) ) ;
#49603=DIRECTION ( 'NONE',  ( -1.000000000000000000, 0.000000000000000000, 0.000000000000000000 ) ) ;
#49606=DIRECTION ( 'NONE',  ( 0.000000000000000000, 0.8090169943749445647, 0.5877852522924770229 ) ) ;
#49607=CARTESIAN_POINT ( 'NONE',  ( 50.00005079999999680, 0.000000000000000000, 12.50000000000000000 ) ) ;
#49615=CARTESIAN_POINT ( 'NONE',  ( 10.00000000000000000, 0.000000000000000000, 0.000000000000000000 ) ) ;
#49617=AXIS2_PLACEMENT_3D ( 'NONE', #21683, #9667, #32588 ) ;
#49629=EDGE_LOOP ( 'NONE', ( #13790, #15083, #69616, #72853 ) ) ;
#49632=ORIENTED_EDGE ( 'NONE', *, *, #31831, .T. ) ;
#49633=CARTESIAN_POINT ( 'NONE',  ( 10.00000000000000000, 39.78640506895700213, -66.50666863321957578 ) ) ;
#49640=DIRECTION ( 'NONE',  ( 0.000000000000000000, 0.000000000000000000, 1.000000000000000000 ) ) ;
#49662=DIRECTION ( 'NONE',  ( 0.000000000000000000, -0.5877852522924625900, -0.8090169943749551118 ) ) ;
#49674=DIRECTION ( 'NONE',  ( -1.000000000000000000, 0.000000000000000000, 0.000000000000000000 ) ) ;
#49679=DIRECTION ( 'NONE',  ( -0.000000000000000000, 0.000000000000000000, 1.000000000000000000 ) ) ;
#49681=ORIENTED_EDGE ( 'NONE', *, *, #36001, .F. ) ;
#49683=DIRECTION ( 'NONE',  ( 1.000000000000000000, -0.000000000000000000, -0.000000000000000000 ) ) ;
#49691=AXIS2_PLACEMENT_3D ( 'NONE', #63094, #33750, #63450 ) ;
#49695=EDGE_CURVE ( 'NONE', #15962, #57613, #11589, .T. ) ;
#49696=DIRECTION ( 'NONE',  ( -1.000000000000000000, 0.000000000000000000, -0.000000000000000000 ) ) ;
#49699=LINE ( 'NONE', #26770, #61743 ) ;
#49704=EDGE_CURVE ( 'NONE', #11557, #15750, #53217, .T. ) ;
#49706=EDGE_LOOP ( 'NONE', ( #18217, #42155, #63920, #21916 ) ) ;
#49708=PRESENTATION_STYLE_ASSIGNMENT (( #3152 ) ) ;
#49711=CYLINDRICAL_SURFACE ( 'NONE', #64054, 31.99999999999999289 ) ;
#49720=ORIENTED_EDGE ( 'NONE', *, *, #25857, .F. ) ;
#49723=ORIENTED_EDGE ( 'NONE', *, *, #30784, .F. ) ;
#49735=ADVANCED_FACE ( 'NONE', ( #47661 ), #6707, .T. ) ;
#49742=CYLINDRICAL_SURFACE ( 'NONE', #8896, 31.99999999999999289 ) ;
#49752=AXIS2_PLACEMENT_3D ( 'NONE', #36706, #7408, #70166 ) ;
#49758=CARTESIAN_POINT ( 'NONE',  ( 10.00000000000000000, 10.30890764327502573, -81.34940948281324324 ) ) ;
#49762=CIRCLE ( 'NONE', #14771, 77.49900000000000944 ) ;
#49764=AXIS2_PLACEMENT_3D ( 'NONE', #37054, #49065, #19746 ) ;
#49767=ORIENTED_EDGE ( 'NONE', *, *, #34115, .F. ) ;
#49768=VECTOR ( 'NONE', #47755, 1000.000000000000000 ) ;
#49770=DIRECTION ( 'NONE',  ( -1.000000000000000000, -0.000000000000000000, -0.000000000000000000 ) ) ;
#49775=DIRECTION ( 'NONE',  ( 0.000000000000000000, 0.000000000000000000, 1.000000000000000000 ) ) ;
#49781=DIRECTION ( 'NONE',  ( -1.000000000000000000, 0.000000000000000000, -0.000000000000000000 ) ) ;
#49787=SHAPE_REPRESENTATION ( 'big gear_ISO - Spur gear 2M 80T 20PA 10FW ---S80A75H50L20.0N', ( #43395 ), #56652 ) ;
#49795=ADVANCED_FACE ( 'NONE', ( #13072 ), #374, .T. ) ;
#49796=DIRECTION ( 'NONE',  ( -1.000000000000000000, -0.000000000000000000, 0.000000000000000000 ) ) ;
#49797=AXIS2_PLACEMENT_3D ( 'NONE', #38573, #55488, #27268 ) ;
#49805=CIRCLE ( 'NONE', #20992, 32.00000000000000000 ) ;
#49811=ORIENTED_EDGE ( 'NONE', *, *, #8000, .T. ) ;
#49817=CARTESIAN_POINT ( 'NONE',  ( 0.000000000000000000, 68.67312586194995561, 35.91791733033500122 ) ) ;
#49828=EDGE_CURVE ( 'NONE', #18411, #16727, #10009, .T. ) ;
#49829=EDGE_CURVE ( 'NONE', #25328, #35339, #71224, .T. ) ;
#49845=ORIENTED_EDGE ( 'NONE', *, *, #34814, .F. ) ;
#49854=DIRECTION ( 'NONE',  ( -1.000000000000000000, 0.000000000000000000, -0.000000000000000000 ) ) ;
#49864=ORIENTED_EDGE ( 'NONE', *, *, #35476, .T. ) ;
#49870=FACE_OUTER_BOUND ( 'NONE', #47233, .T. ) ;
#49874=CARTESIAN_POINT ( 'NONE',  ( 10.00000000000000000, 73.73191006444551476, 14.66109333815590254 ) ) ;
#49883=ADVANCED_FACE ( 'NONE', ( #29993 ), #41647, .T. ) ;
#49893=CYLINDRICAL_SURFACE ( 'NONE', #20383, 32.00000000000000000 ) ;
#49898=ORIENTED_EDGE ( 'NONE', *, *, #15424, .T. ) ;
#49901=EDGE_CURVE ( 'NONE', #66429, #34383, #52085, .T. ) ;
#49906=AXIS2_PLACEMENT_3D ( 'NONE', #53476, #71487, #26373 ) ;
#49918=CIRCLE ( 'NONE', #29452, 31.99999999999998579 ) ;
#49925=CYLINDRICAL_SURFACE ( 'NONE', #37064, 77.49899999999999523 ) ;
#49931=LINE ( 'NONE', #10839, #51194 ) ;
#49936=LINE ( 'NONE', #71377, #18054 ) ;
#49944=ORIENTED_EDGE ( 'NONE', *, *, #33634, .T. ) ;
#49949=VERTEX_POINT ( 'NONE', #9662 ) ;
#49959=FACE_OUTER_BOUND ( 'NONE', #34962, .T. ) ;
#49968=EDGE_CURVE ( 'NONE', #37734, #68371, #54439, .T. ) ;
#49977=VECTOR ( 'NONE', #32021, 1000.000000000000000 ) ;
#49979=DIRECTION ( 'NONE',  ( -1.000000000000000000, -0.000000000000000000, -0.000000000000000000 ) ) ;
#49985=ORIENTED_EDGE ( 'NONE', *, *, #12557, .F. ) ;
#49991=ORIENTED_EDGE ( 'NONE', *, *, #35385, .F. ) ;
#49997=LINE ( 'NONE', #16170, #3497 ) ;
#50001=DIRECTION ( 'NONE',  ( 0.000000000000000000, 0.9723699203976773342, -0.2334453638559024213 ) ) ;
#50005=EDGE_LOOP ( 'NONE', ( #66662, #11015, #2609, #11461 ) ) ;
#50008=DIRECTION ( 'NONE',  ( -1.000000000000000000, 0.000000000000000000, -0.000000000000000000 ) ) ;
#50019=VECTOR ( 'NONE', #1756, 1000.000000000000000 ) ;
#50032=CARTESIAN_POINT ( 'NONE',  ( 10.00000000000000178, 0.000000000000000000, 0.000000000000000000 ) ) ;
#50033=FACE_OUTER_BOUND ( 'NONE', #20720, .T. ) ;
#50038=ORIENTED_EDGE ( 'NONE', *, *, #30135, .T. ) ;
#50039=AXIS2_PLACEMENT_3D ( 'NONE', #20879, #13755, #59634 ) ;
#50042=EDGE_CURVE ( 'NONE', #8336, #24236, #60080, .T. ) ;
#50043=CARTESIAN_POINT ( 'NONE',  ( 0.000000000000000000, 0.000000000000000000, 0.000000000000000000 ) ) ;
#50055=CARTESIAN_POINT ( 'NONE',  ( 10.00000000000000000, -44.88180994100329713, -63.18004540533077318 ) ) ;
#50063=CARTESIAN_POINT ( 'NONE',  ( 5.000000000000000000, -46.11716303203136391, -67.80270845531939017 ) ) ;
#50071=VECTOR ( 'NONE', #52381, 1000.000000000000000 ) ;
#50089=EDGE_LOOP ( 'NONE', ( #64287, #10637, #58040, #41150 ) ) ;
#50095=CARTESIAN_POINT ( 'NONE',  ( 10.00000000000000000, 0.000000000000000000, 0.000000000000000000 ) ) ;
#50097=ORIENTED_EDGE ( 'NONE', *, *, #25748, .T. ) ;
#50101=EDGE_LOOP ( 'NONE', ( #34237, #31526, #61157, #74227 ) ) ;
#50114=ORIENTED_EDGE ( 'NONE', *, *, #25227, .F. ) ;
#50116=AXIS2_PLACEMENT_3D ( 'NONE', #15673, #38603, #61540 ) ;
#50119=DIRECTION ( 'NONE',  ( -1.000000000000000000, -0.000000000000000000, -0.000000000000000000 ) ) ;
#50129=AXIS2_PLACEMENT_3D ( 'NONE', #53044, #18809, #41750 ) ;
#50133=DIRECTION ( 'NONE',  ( -1.000000000000000000, 0.000000000000000000, 0.000000000000000000 ) ) ;
#50145=VECTOR ( 'NONE', #19033, 1000.000000000000000 ) ;
#50146=DIRECTION ( 'NONE',  ( -1.000000000000000000, -0.000000000000000000, 0.000000000000000000 ) ) ;
#50147=CARTESIAN_POINT ( 'NONE',  ( 0.000000000000000000, 75.11725578898472122, -2.956366410619845730 ) ) ;
#50160=ORIENTED_EDGE ( 'NONE', *, *, #32514, .T. ) ;
#50167=EDGE_CURVE ( 'NONE', #19199, #7429, #61920, .T. ) ;
#50174=AXIS2_PLACEMENT_3D ( 'NONE', #73552, #22439, #57025 ) ;
#50177=ORIENTED_EDGE ( 'NONE', *, *, #30107, .F. ) ;
#50178=VERTEX_POINT ( 'NONE', #10028 ) ;
#50190=ORIENTED_EDGE ( 'NONE', *, *, #19284, .F. ) ;
#50194=CARTESIAN_POINT ( 'NONE',  ( 10.00000000000000000, -51.02545421589285723, -55.20638768913812555 ) ) ;
#50197=CARTESIAN_POINT ( 'NONE',  ( 10.00000000000000000, -65.59268652807237743, 36.72794159290217664 ) ) ;
#50219=CARTESIAN_POINT ( 'NONE',  ( 10.00000000000000000, 0.000000000000000000, 0.000000000000000000 ) ) ;
#50230=ADVANCED_FACE ( 'NONE', ( #49870 ), #50243, .T. ) ;
#50235=VERTEX_POINT ( 'NONE', #64141 ) ;
#50237=VECTOR ( 'NONE', #23366, 1000.000000000000000 ) ;
#50243=CYLINDRICAL_SURFACE ( 'NONE', #64069, 31.99999999999999289 ) ;
#50251=CARTESIAN_POINT ( 'NONE',  ( 0.000000000000000000, 64.81221759200417409, -50.23322058963276504 ) ) ;
#50260=CIRCLE ( 'NONE', #10666, 77.49900000000002365 ) ;
#50261=CIRCLE ( 'NONE', #37068, 32.00000000000000000 ) ;
#50268=CARTESIAN_POINT ( 'NONE',  ( 10.00000000000000000, -0.8261519478425671803, -77.49459641780887864 ) ) ;
#50269=DIRECTION ( 'NONE',  ( 0.000000000000000000, 0.000000000000000000, -1.000000000000000000 ) ) ;
#50271=ORIENTED_EDGE ( 'NONE', *, *, #25725, .F. ) ;
#50273=CIRCLE ( 'NONE', #70716, 31.99999999999999645 ) ;
#50284=CARTESIAN_POINT ( 'NONE',  ( 10.00000000000000000, -23.16143007188481207, 73.95703589263968070 ) ) ;
#50291=ORIENTED_EDGE ( 'NONE', *, *, #38950, .T. ) ;
#50314=ORIENTED_EDGE ( 'NONE', *, *, #47800, .F. ) ;
#50315=EDGE_CURVE ( 'NONE', #3906, #2716, #56867, .T. ) ;
#50317=DIRECTION ( 'NONE',  ( -1.000000000000000000, 0.000000000000000000, 0.000000000000000000 ) ) ;
#50330=DIRECTION ( 'NONE',  ( 0.000000000000000000, 0.3090169943749411785, 0.9510565162951556406 ) ) ;
#50332=FACE_OUTER_BOUND ( 'NONE', #61048, .T. ) ;
#50333=FACE_OUTER_BOUND ( 'NONE', #63034, .T. ) ;
#50339=EDGE_CURVE ( 'NONE', #688, #40404, #43670, .T. ) ;
#50341=CARTESIAN_POINT ( 'NONE',  ( 10.00000000000000000, -75.54627589209931671, -17.28742895386164591 ) ) ;
#50353=CARTESIAN_POINT ( 'NONE',  ( 10.00000000000000000, 0.000000000000000000, 0.000000000000000000 ) ) ;
#50360=CARTESIAN_POINT ( 'NONE',  ( 0.000000000000000000, -79.10210256391353312, -21.60688246758668640 ) ) ;
#50362=AXIS2_PLACEMENT_3D ( 'NONE', #52816, #51321, #74255 ) ;
#50366=CIRCLE ( 'NONE', #38352, 77.49899999999998101 ) ;
#50386=CYLINDRICAL_SURFACE ( 'NONE', #34826, 77.49899999999999523 ) ;
#50390=CIRCLE ( 'NONE', #27601, 31.99999999999999289 ) ;
#50401=ORIENTED_EDGE ( 'NONE', *, *, #47599, .T. ) ;
#50418=CARTESIAN_POINT ( 'NONE',  ( 10.00000000000000000, 0.000000000000000000, 0.000000000000000000 ) ) ;
#50429=DIRECTION ( 'NONE',  ( 0.000000000000000000, 0.000000000000000000, 1.000000000000000000 ) ) ;
#50432=EDGE_CURVE ( 'NONE', #69505, #73572, #43445, .T. ) ;
#50434=DIRECTION ( 'NONE',  ( -1.000000000000000000, 0.000000000000000000, 0.000000000000000000 ) ) ;
#50435=DIRECTION ( 'NONE',  ( -1.000000000000000000, 0.000000000000000000, 0.000000000000000000 ) ) ;
#50436=EDGE_LOOP ( 'NONE', ( #4643, #55497, #54669, #51226 ) ) ;
#50445=CARTESIAN_POINT ( 'NONE',  ( 0.000000000000000000, -26.01480285779785362, -70.53064760720343429 ) ) ;
#50446=EDGE_LOOP ( 'NONE', ( #38503, #3584, #65737, #155 ) ) ;
#50447=LINE ( 'NONE', #66279, #19090 ) ;
#50451=CARTESIAN_POINT ( 'NONE',  ( 10.00000000000000000, 77.19088730480534366, -6.903761155836915187 ) ) ;
#50453=DIRECTION ( 'NONE',  ( 0.000000000000000000, 0.6494480483301793283, 0.7604059656000345946 ) ) ;
#50454=CIRCLE ( 'NONE', #18050, 82.00000000000000000 ) ;
#50456=AXIS2_PLACEMENT_3D ( 'NONE', #7895, #24452, #65428 ) ;
#50464=VERTEX_POINT ( 'NONE', #25393 ) ;
#50465=EDGE_CURVE ( 'NONE', #34383, #64804, #25755, .T. ) ;
#50470=VERTEX_POINT ( 'NONE', #49426 ) ;
#50476=CIRCLE ( 'NONE', #37297, 31.99999999999999289 ) ;
#50479=EDGE_CURVE ( 'NONE', #5506, #58503, #65999, .T. ) ;
#50483=DIRECTION ( 'NONE',  ( -1.000000000000000000, -0.000000000000000000, -0.000000000000000000 ) ) ;
#50495=DIRECTION ( 'NONE',  ( 0.000000000000000000, 0.3826834323650841752, 0.9238795325112891810 ) ) ;
#50517=EDGE_CURVE ( 'NONE', #48877, #34480, #42679, .T. ) ;
#50535=DIRECTION ( 'NONE',  ( -1.000000000000000000, 0.000000000000000000, 0.000000000000000000 ) ) ;
#50544=DIRECTION ( 'NONE',  ( 0.000000000000000000, 0.000000000000000000, 1.000000000000000000 ) ) ;
#50557=AXIS2_PLACEMENT_3D ( 'NONE', #18714, #64589, #41292 ) ;
#50561=VERTEX_POINT ( 'NONE', #8093 ) ;
#50565=DIRECTION ( 'NONE',  ( 0.000000000000000000, 0.9238795325112851842, 0.3826834323650938341 ) ) ;
#50583=ORIENTED_EDGE ( 'NONE', *, *, #47218, .F. ) ;
#50586=DIRECTION ( 'NONE',  ( -1.000000000000000000, 0.000000000000000000, -0.000000000000000000 ) ) ;
#50599=DIRECTION ( 'NONE',  ( 0.000000000000000000, 0.000000000000000000, 1.000000000000000000 ) ) ;
#50613=CIRCLE ( 'NONE', #66250, 77.49900000000000944 ) ;
#50621=CARTESIAN_POINT ( 'NONE',  ( 10.00000000000000000, 50.95692526931414790, -58.39081064771693974 ) ) ;
#50628=DIRECTION ( 'NONE',  ( -1.000000000000000000, 0.000000000000000000, -0.000000000000000000 ) ) ;
#50634=AXIS2_PLACEMENT_3D ( 'NONE', #35242, #58173, #6671 ) ;
#50636=DIRECTION ( 'NONE',  ( -1.000000000000000000, 0.000000000000000000, 0.000000000000000000 ) ) ;
#50639=CARTESIAN_POINT ( 'NONE',  ( 10.00000000000000000, -54.21277698773636899, -55.38113227695839669 ) ) ;
#50645=ADVANCED_FACE ( 'NONE', ( #27606 ), #4700, .T. ) ;
#50650=DIRECTION ( 'NONE',  ( -1.000000000000000000, -0.000000000000000000, -0.000000000000000000 ) ) ;
#50657=VECTOR ( 'NONE', #38691, 1000.000000000000000 ) ;
#50659=CARTESIAN_POINT ( 'NONE',  ( 0.000000000000000000, -41.76106447765533147, 62.50884508063410294 ) ) ;
#50661=ORIENTED_EDGE ( 'NONE', *, *, #39986, .F. ) ;
#50673=CARTESIAN_POINT ( 'NONE',  ( 10.00000000000000000, 0.000000000000000000, 0.000000000000000000 ) ) ;
#50680=ADVANCED_FACE ( 'NONE', ( #62586 ), #55439, .T. ) ;
#50699=VERTEX_POINT ( 'NONE', #57677 ) ;
#50706=EDGE_CURVE ( 'NONE', #68597, #47328, #37714, .T. ) ;
#50717=DIRECTION ( 'NONE',  ( 0.000000000000000000, 0.000000000000000000, -1.000000000000000000 ) ) ;
#50726=CIRCLE ( 'NONE', #1514, 82.00000000000000000 ) ;
#50730=CYLINDRICAL_SURFACE ( 'NONE', #13796, 82.00000000000000000 ) ;
#50744=VERTEX_POINT ( 'NONE', #35104 ) ;
#50755=DIRECTION ( 'NONE',  ( -1.000000000000000000, -0.000000000000000000, -0.000000000000000000 ) ) ;
#50757=VERTEX_POINT ( 'NONE', #46385 ) ;
#50761=CARTESIAN_POINT ( 'NONE',  ( 10.00000000000000000, 0.000000000000000000, 0.000000000000000000 ) ) ;
#50770=ORIENTED_EDGE ( 'NONE', *, *, #49206, .F. ) ;
#50772=EDGE_LOOP ( 'NONE', ( #69799, #30071, #70929, #10907 ) ) ;
#50778=CIRCLE ( 'NONE', #61577, 82.00000000000000000 ) ;
#50785=LINE ( 'NONE', #18067, #72874 ) ;
#50791=AXIS2_PLACEMENT_3D ( 'NONE', #10875, #34172, #57115 ) ;
#50797=LINE ( 'NONE', #73723, #44248 ) ;
#50798=CARTESIAN_POINT ( 'NONE',  ( 0.000000000000000000, -74.65374052328644439, -8.840884882375878107 ) ) ;
#50802=DIRECTION ( 'NONE',  ( -1.000000000000000000, 0.000000000000000000, 0.000000000000000000 ) ) ;
#50809=AXIS2_PLACEMENT_3D ( 'NONE', #24737, #41651, #42402 ) ;
#50813=CARTESIAN_POINT ( 'NONE',  ( 0.000000000000000000, -64.81221759200306565, -50.23322058963418613 ) ) ;
#50819=CIRCLE ( 'NONE', #19581, 31.99999999999998579 ) ;
#50820=EDGE_CURVE ( 'NONE', #59815, #71840, #72407, .T. ) ;
#50824=DIRECTION ( 'NONE',  ( 0.000000000000000000, 0.5877852522924685852, 0.8090169943749507819 ) ) ;
#50828=EDGE_CURVE ( 'NONE', #64812, #8792, #17358, .T. ) ;
#50830=CARTESIAN_POINT ( 'NONE',  ( 0.000000000000000000, -49.70050353004932475, 59.46389618801944721 ) ) ;
#50832=VERTEX_POINT ( 'NONE', #11780 ) ;
#50837=ORIENTED_EDGE ( 'NONE', *, *, #40264, .T. ) ;
#50839=AXIS2_PLACEMENT_3D ( 'NONE', #18265, #24648, #64144 ) ;
#50847=ORIENTED_EDGE ( 'NONE', *, *, #69750, .F. ) ;
#50850=DIRECTION ( 'NONE',  ( 0.000000000000000000, 0.000000000000000000, 1.000000000000000000 ) ) ;
#50860=EDGE_CURVE ( 'NONE', #62434, #68980, #43620, .T. ) ;
#50871=AXIS2_PLACEMENT_3D ( 'NONE', #44546, #66366, #37792 ) ;
#50878=CARTESIAN_POINT ( 'NONE',  ( 10.00000000000000000, 46.11716303203284184, -67.80270845531838120 ) ) ;
#50881=DIRECTION ( 'NONE',  ( -1.000000000000000000, -0.000000000000000000, 0.000000000000000000 ) ) ;
#50894=CYLINDRICAL_SURFACE ( 'NONE', #68790, 82.00000000000000000 ) ;
#50909=EDGE_CURVE ( 'NONE', #53791, #27456, #53213, .T. ) ;
#50913=ADVANCED_FACE ( 'NONE', ( #65906 ), #42970, .T. ) ;
#50917=CARTESIAN_POINT ( 'NONE',  ( 10.00000000000000000, 0.000000000000000000, 0.000000000000000000 ) ) ;
#50940=DIRECTION ( 'NONE',  ( -1.000000000000000000, 0.000000000000000000, 0.000000000000000000 ) ) ;
#50941=CIRCLE ( 'NONE', #19704, 31.99999999999999289 ) ;
#50966=VERTEX_POINT ( 'NONE', #8005 ) ;
#50982=ORIENTED_EDGE ( 'NONE', *, *, #62785, .F. ) ;
#50992=ORIENTED_EDGE ( 'NONE', *, *, #71563, .F. ) ;
#51005=CARTESIAN_POINT ( 'NONE',  ( 0.000000000000000000, 0.000000000000000000, 0.000000000000000000 ) ) ;
#51007=CARTESIAN_POINT ( 'NONE',  ( 0.000000000000000000, 12.24744871391589207, 2.500000000000000000 ) ) ;
#51017=DIRECTION ( 'NONE',  ( -1.000000000000000000, 0.000000000000000000, 0.000000000000000000 ) ) ;
#51022=DIRECTION ( 'NONE',  ( 0.000000000000000000, 0.1564344650402312020, -0.9876883405951376593 ) ) ;
#51047=EDGE_LOOP ( 'NONE', ( #65514, #71268, #53535, #4653 ) ) ;
#51050=DIRECTION ( 'NONE',  ( 0.000000000000000000, -0.9238795325112906243, 0.3826834323650804559 ) ) ;
#51061=ORIENTED_EDGE ( 'NONE', *, *, #8716, .T. ) ;
#51062=DIRECTION ( 'NONE',  ( -1.000000000000000000, -0.000000000000000000, 0.000000000000000000 ) ) ;
#51079=CYLINDRICAL_SURFACE ( 'NONE', #21908, 77.49899999999999523 ) ;
#51080=AXIS2_PLACEMENT_3D ( 'NONE', #52361, #18881, #64766 ) ;
#51082=EDGE_CURVE ( 'NONE', #49949, #67626, #73748, .T. ) ;
#51087=DIRECTION ( 'NONE',  ( -1.000000000000000000, -0.000000000000000000, 0.000000000000000000 ) ) ;
#51088=EDGE_CURVE ( 'NONE', #67020, #46606, #37765, .T. ) ;
#51090=DIRECTION ( 'NONE',  ( -1.000000000000000000, -0.000000000000000000, -0.000000000000000000 ) ) ;
#51112=AXIS2_PLACEMENT_3D ( 'NONE', #60825, #32228, #53423 ) ;
#51121=ORIENTED_EDGE ( 'NONE', *, *, #20156, .F. ) ;
#51125=ORIENTED_EDGE ( 'NONE', *, *, #29005, .T. ) ;
#51126=ORIENTED_EDGE ( 'NONE', *, *, #25637, .F. ) ;
#51128=( GEOMETRIC_REPRESENTATION_CONTEXT ( 3 ) GLOBAL_UNCERTAINTY_ASSIGNED_CONTEXT ( ( #65436 ) ) GLOBAL_UNIT_ASSIGNED_CONTEXT ( ( #44088, #54627, #48975 ) ) REPRESENTATION_CONTEXT ( 'NONE', 'WORKASPACE' ) );
#51129=CARTESIAN_POINT ( 'NONE',  ( 0.000000000000000000, 0.000000000000000000, 0.000000000000000000 ) ) ;
#51136=DIRECTION ( 'NONE',  ( -1.000000000000000000, 0.000000000000000000, -0.000000000000000000 ) ) ;
#51142=ORIENTED_EDGE ( 'NONE', *, *, #25527, .T. ) ;
#51149=CARTESIAN_POINT ( 'NONE',  ( 0.000000000000000000, -63.18004540533059554, 44.88180994100355292 ) ) ;
#51156=LINE ( 'NONE', #40259, #11653 ) ;
#51161=FACE_OUTER_BOUND ( 'NONE', #66913, .T. ) ;
#51162=EDGE_CURVE ( 'NONE', #33442, #42798, #30550, .T. ) ;
#51165=AXIS2_PLACEMENT_3D ( 'NONE', #66358, #53216, #1753 ) ;
#51191=DIRECTION ( 'NONE',  ( -1.000000000000000000, -0.000000000000000000, -0.000000000000000000 ) ) ;
#51194=VECTOR ( 'NONE', #56333, 1000.000000000000000 ) ;
#51212=VECTOR ( 'NONE', #15613, 1000.000000000000000 ) ;
#51213=CARTESIAN_POINT ( 'NONE',  ( 10.00000000000000000, -62.20884554313985149, -46.21855187248698371 ) ) ;
#51220=AXIS2_PLACEMENT_3D ( 'NONE', #17256, #5994, #64234 ) ;
#51221=ORIENTED_EDGE ( 'NONE', *, *, #66544, .T. ) ;
#51226=ORIENTED_EDGE ( 'NONE', *, *, #63066, .T. ) ;
#51227=ORIENTED_EDGE ( 'NONE', *, *, #73767, .F. ) ;
#51232=CIRCLE ( 'NONE', #29593, 82.00000000000000000 ) ;
#51244=DIRECTION ( 'NONE',  ( 0.000000000000000000, 0.000000000000000000, 1.000000000000000000 ) ) ;
#51246=DIRECTION ( 'NONE',  ( -1.000000000000000000, -0.000000000000000000, 0.000000000000000000 ) ) ;
#51247=CARTESIAN_POINT ( 'NONE',  ( 0.000000000000000000, 0.000000000000000000, 0.000000000000000000 ) ) ;
#51266=EDGE_LOOP ( 'NONE', ( #61990, #15048, #47057, #23110 ) ) ;
#51270=DIRECTION ( 'NONE',  ( -1.000000000000000000, 0.000000000000000000, 0.000000000000000000 ) ) ;
#51276=AXIS2_PLACEMENT_3D ( 'NONE', #4795, #45377, #61919 ) ;
#51278=EDGE_CURVE ( 'NONE', #30710, #52760, #49762, .T. ) ;
#51279=AXIS2_PLACEMENT_3D ( 'NONE', #57590, #28995, #68114 ) ;
#51289=CIRCLE ( 'NONE', #20043, 77.49899999999999523 ) ;
#51293=AXIS2_PLACEMENT_3D ( 'NONE', #42633, #14040, #61026 ) ;
#51312=ORIENTED_EDGE ( 'NONE', *, *, #23573, .F. ) ;
#51313=VERTEX_POINT ( 'NONE', #19192 ) ;
#51319=CIRCLE ( 'NONE', #29681, 31.99999999999999289 ) ;
#51321=DIRECTION ( 'NONE',  ( -1.000000000000000000, -0.000000000000000000, 0.000000000000000000 ) ) ;
#51322=CYLINDRICAL_SURFACE ( 'NONE', #8019, 77.49899999999999523 ) ;
#51327=ADVANCED_FACE ( 'NONE', ( #24469 ), #13183, .T. ) ;
#51328=ORIENTED_EDGE ( 'NONE', *, *, #47689, .F. ) ;
#51338=DIRECTION ( 'NONE',  ( -1.000000000000000000, -0.000000000000000000, 0.000000000000000000 ) ) ;
#51341=LINE ( 'NONE', #74278, #28908 ) ;
#51359=DIRECTION ( 'NONE',  ( 0.000000000000000000, 0.000000000000000000, 1.000000000000000000 ) ) ;
#51362=DIRECTION ( 'NONE',  ( -1.000000000000000000, 0.000000000000000000, -0.000000000000000000 ) ) ;
#51393=CIRCLE ( 'NONE', #65797, 82.00000000000000000 ) ;
#51399=ORIENTED_EDGE ( 'NONE', *, *, #29959, .T. ) ;
#51400=EDGE_LOOP ( 'NONE', ( #5880, #11585, #2558, #27065 ) ) ;
#51416=DIRECTION ( 'NONE',  ( 0.000000000000000000, -0.07845909572785220165, 0.9969173337331274087 ) ) ;
#51427=CARTESIAN_POINT ( 'NONE',  ( 5.000000000000002665, 78.73519480814955784, 22.90783923731657268 ) ) ;
#51429=CARTESIAN_POINT ( 'NONE',  ( 10.00000000000000000, -62.50329211542465657, 41.76937507738766442 ) ) ;
#51433=VERTEX_POINT ( 'NONE', #67941 ) ;
#51445=CARTESIAN_POINT ( 'NONE',  ( 0.000000000000000000, 0.000000000000000000, 0.000000000000000000 ) ) ;
#51454=AXIS2_PLACEMENT_3D ( 'NONE', #43285, #7573, #37632 ) ;
#51461=EDGE_CURVE ( 'NONE', #57911, #51433, #494, .T. ) ;
#51475=AXIS2_PLACEMENT_3D ( 'NONE', #60630, #19643, #36943 ) ;
#51479=AXIS2_PLACEMENT_3D ( 'NONE', #33887, #57937, #69215 ) ;
#51490=AXIS2_PLACEMENT_3D ( 'NONE', #71026, #7151, #1188 ) ;
#51492=ORIENTED_EDGE ( 'NONE', *, *, #74282, .F. ) ;
#51498=CIRCLE ( 'NONE', #3491, 31.99999999999998579 ) ;
#51501=AXIS2_PLACEMENT_3D ( 'NONE', #50659, #67590, #37908 ) ;
#51506=ADVANCED_FACE ( 'NONE', ( #3408 ), #11164, .T. ) ;
#51508=CARTESIAN_POINT ( 'NONE',  ( 10.00000000000000000, -55.19960302592029677, -51.03279382321147750 ) ) ;
#51519=ORIENTED_EDGE ( 'NONE', *, *, #22151, .F. ) ;
#51525=ORIENTED_EDGE ( 'NONE', *, *, #66821, .F. ) ;
#51528=DIRECTION ( 'NONE',  ( 0.000000000000000000, 0.000000000000000000, 1.000000000000000000 ) ) ;
#51531=CIRCLE ( 'NONE', #64737, 32.00000000000000000 ) ;
#51539=VECTOR ( 'NONE', #3290, 1000.000000000000000 ) ;
#51542=DIRECTION ( 'NONE',  ( -1.000000000000000000, -0.000000000000000000, -0.000000000000000000 ) ) ;
#51549=CARTESIAN_POINT ( 'NONE',  ( 10.00000000000000000, 74.65491531819118620, 23.16904090965733332 ) ) ;
#51550=EDGE_CURVE ( 'NONE', #31993, #25646, #5171, .T. ) ;
#51557=CIRCLE ( 'NONE', #35936, 31.99999999999998934 ) ;
#51558=CARTESIAN_POINT ( 'NONE',  ( 10.00000000000000000, 46.53671651294032330, -59.03961581697353012 ) ) ;
#51564=CARTESIAN_POINT ( 'NONE',  ( 0.000000000000000000, -34.44570377933549565, -69.42325613327476219 ) ) ;
#51583=EDGE_LOOP ( 'NONE', ( #6164, #12845, #15068, #36151 ) ) ;
#51618=EDGE_CURVE ( 'NONE', #50744, #18038, #46079, .T. ) ;
#51630=DIRECTION ( 'NONE',  ( 0.000000000000000000, 1.000000000000000000, 3.491481338843133355E-15 ) ) ;
#51642=LINE ( 'NONE', #10307, #63729 ) ;
#51645=AXIS2_PLACEMENT_3D ( 'NONE', #21519, #67393, #38830 ) ;
#51656=DIRECTION ( 'NONE',  ( -1.000000000000000000, 0.000000000000000000, 0.000000000000000000 ) ) ;
#51665=CARTESIAN_POINT ( 'NONE',  ( 0.000000000000000000, -15.33399622253423722, -80.55351364060604169 ) ) ;
#51666=CIRCLE ( 'NONE', #58914, 82.00000000000000000 ) ;
#51678=CARTESIAN_POINT ( 'NONE',  ( 10.00000000000000000, -2.946379043146863719, 75.11764819372146462 ) ) ;
#51681=EDGE_LOOP ( 'NONE', ( #43871, #16999, #28, #17967 ) ) ;
#51696=VECTOR ( 'NONE', #286, 1000.000000000000000 ) ;
#51701=CARTESIAN_POINT ( 'NONE',  ( 10.00000000000000000, -59.75363087400112505, 56.15606465354937882 ) ) ;
#51719=LINE ( 'NONE', #57737, #25846 ) ;
#51742=DIRECTION ( 'NONE',  ( 0.000000000000000000, 0.9723699203976773342, -0.2334453638559023381 ) ) ;
#51747=CARTESIAN_POINT ( 'NONE',  ( 0.000000000000000000, -75.16055320797043748, 18.89407956138229494 ) ) ;
#51750=CIRCLE ( 'NONE', #40925, 31.99999999999998579 ) ;
#51755=DIRECTION ( 'NONE',  ( 0.000000000000000000, 1.000000000000000000, 3.491481338843133355E-15 ) ) ;
#51763=CARTESIAN_POINT ( 'NONE',  ( 10.00000000000000000, 20.40083707022882820, 72.35432306680490910 ) ) ;
#51767=VERTEX_POINT ( 'NONE', #43817 ) ;
#51768=AXIS2_PLACEMENT_3D ( 'NONE', #25481, #70579, #2958 ) ;
#51782=EDGE_LOOP ( 'NONE', ( #12923, #29420, #28099, #15435 ) ) ;
#51783=ORIENTED_EDGE ( 'NONE', *, *, #42775, .T. ) ;
#51796=CARTESIAN_POINT ( 'NONE',  ( 10.00000000000000000, -70.53064760720336324, 26.01480285779810231 ) ) ;
#51807=CIRCLE ( 'NONE', #46975, 31.99999999999999289 ) ;
#51820=ORIENTED_EDGE ( 'NONE', *, *, #59353, .F. ) ;
#51825=DIRECTION ( 'NONE',  ( -1.000000000000000000, -0.000000000000000000, -0.000000000000000000 ) ) ;
#51827=AXIS2_PLACEMENT_3D ( 'NONE', #73973, #39035, #34879 ) ;
#51830=VECTOR ( 'NONE', #59617, 1000.000000000000000 ) ;
#51831=FACE_OUTER_BOUND ( 'NONE', #72508, .T. ) ;
#51834=CARTESIAN_POINT ( 'NONE',  ( 10.00000000000000000, -74.65491531819124305, 8.830959090342128448 ) ) ;
#51839=DIRECTION ( 'NONE',  ( 0.000000000000000000, 0.000000000000000000, 1.000000000000000000 ) ) ;
#51841=CARTESIAN_POINT ( 'NONE',  ( 0.000000000000000000, 51.29473840253223926, 63.97538442413444670 ) ) ;
#51846=ADVANCED_FACE ( 'NONE', ( #65631 ), #3607, .T. ) ;
#51850=EDGE_CURVE ( 'NONE', #67382, #16471, #53978, .T. ) ;
#51856=ORIENTED_EDGE ( 'NONE', *, *, #10623, .T. ) ;
#51857=ORIENTED_EDGE ( 'NONE', *, *, #72795, .F. ) ;
#51873=DIRECTION ( 'NONE',  ( 0.000000000000000000, 0.000000000000000000, 1.000000000000000000 ) ) ;
#51877=ORIENTED_EDGE ( 'NONE', *, *, #31831, .F. ) ;
#51880=ADVANCED_FACE ( 'NONE', ( #37434 ), #60367, .T. ) ;
#51890=DIRECTION ( 'NONE',  ( 0.000000000000000000, -0.5877852522924803536, 0.8090169943749422332 ) ) ;
#51892=ORIENTED_EDGE ( 'NONE', *, *, #26329, .T. ) ;
#51898=ORIENTED_EDGE ( 'NONE', *, *, #27313, .F. ) ;
#51901=CYLINDRICAL_SURFACE ( 'NONE', #37214, 77.49899999999999523 ) ;
#51905=DIRECTION ( 'NONE',  ( 0.000000000000000000, 0.000000000000000000, 1.000000000000000000 ) ) ;
#51918=AXIS2_PLACEMENT_3D ( 'NONE', #58937, #35986, #54395 ) ;
#51923=CIRCLE ( 'NONE', #21924, 31.99999999999999289 ) ;
#51928=EDGE_CURVE ( 'NONE', #46606, #45876, #38885, .T. ) ;
#51937=EDGE_CURVE ( 'NONE', #37162, #5395, #25671, .T. ) ;
#51939=EDGE_LOOP ( 'NONE', ( #69326, #17581, #68897, #47981 ) ) ;
#51940=CYLINDRICAL_SURFACE ( 'NONE', #52859, 31.99999999999999289 ) ;
#51954=CARTESIAN_POINT ( 'NONE',  ( 10.00000000000000000, -66.50666863321973210, -39.78640506895676765 ) ) ;
#51955=ORIENTED_EDGE ( 'NONE', *, *, #19758, .F. ) ;
#51957=DIRECTION ( 'NONE',  ( -1.000000000000000000, 0.000000000000000000, 0.000000000000000000 ) ) ;
#51960=ORIENTED_EDGE ( 'NONE', *, *, #39318, .T. ) ;
#51964=ADVANCED_FACE ( 'NONE', ( #21219 ), #61471, .T. ) ;
#51971=AXIS2_PLACEMENT_3D ( 'NONE', #57854, #39075, #52195 ) ;
#51974=DIRECTION ( 'NONE',  ( -1.000000000000000000, -0.000000000000000000, 0.000000000000000000 ) ) ;
#51975=CYLINDRICAL_SURFACE ( 'NONE', #6543, 31.99999999999998579 ) ;
#51978=CARTESIAN_POINT ( 'NONE',  ( 0.000000000000000000, 26.02418014898310261, 70.52718814184268581 ) ) ;
#51986=DIRECTION ( 'NONE',  ( 1.000000000000000000, -0.000000000000000000, 0.000000000000000000 ) ) ;
#51988=CARTESIAN_POINT ( 'NONE',  ( 10.00000000000000000, 41.19522573413826194, -65.64334221924865176 ) ) ;
#51990=DIRECTION ( 'NONE',  ( -1.000000000000000000, 0.000000000000000000, 0.000000000000000000 ) ) ;
#52000=CARTESIAN_POINT ( 'NONE',  ( 50.00005079999999680, 12.24744871391589207, 2.500000000000000000 ) ) ;
#52020=CARTESIAN_POINT ( 'NONE',  ( 10.00000000000000000, -70.53064760720297954, -26.01480285779911839 ) ) ;
#52026=AXIS2_PLACEMENT_3D ( 'NONE', #29251, #46933, #13449 ) ;
#52045=ORIENTED_EDGE ( 'NONE', *, *, #40182, .F. ) ;
#52046=CIRCLE ( 'NONE', #18452, 31.99999999999998579 ) ;
#52059=AXIS2_PLACEMENT_3D ( 'NONE', #19031, #14877, #47607 ) ;
#52063=CARTESIAN_POINT ( 'NONE',  ( 10.00000000000000000, -69.42325613327415113, -34.44570377933673910 ) ) ;
#52070=DIRECTION ( 'NONE',  ( 0.000000000000000000, 0.8090169943749486725, -0.5877852522924713607 ) ) ;
#52074=CIRCLE ( 'NONE', #35285, 82.00000000000000000 ) ;
#52085=CIRCLE ( 'NONE', #10053, 31.99999999999999289 ) ;
#52104=DIRECTION ( 'NONE',  ( -1.000000000000000000, 0.000000000000000000, 0.000000000000000000 ) ) ;
#52125=CARTESIAN_POINT ( 'NONE',  ( -10.00000000000000000, 0.000000000000000000, 0.000000000000000000 ) ) ;
#52127=DIRECTION ( 'NONE',  ( -1.000000000000000000, -0.000000000000000000, 0.000000000000000000 ) ) ;
#52135=DIRECTION ( 'NONE',  ( -1.000000000000000000, 0.000000000000000000, 0.000000000000000000 ) ) ;
#52139=DIRECTION ( 'NONE',  ( -1.000000000000000000, -0.000000000000000000, -0.000000000000000000 ) ) ;
#52140=CARTESIAN_POINT ( 'NONE',  ( 10.00000000000000000, 0.000000000000000000, 0.000000000000000000 ) ) ;
#52150=CARTESIAN_POINT ( 'NONE',  ( 0.000000000000000000, -71.91182617369166508, -28.89263327155821770 ) ) ;
#52166=LINE ( 'NONE', #53283, #62505 ) ;
#52174=ORIENTED_EDGE ( 'NONE', *, *, #72872, .T. ) ;
#52181=CARTESIAN_POINT ( 'NONE',  ( 10.00000000000000000, -41.76937507738831812, 62.50329211542423025 ) ) ;
#52183=VECTOR ( 'NONE', #36161, 1000.000000000000000 ) ;
#52189=ADVANCED_FACE ( 'NONE', ( #53880 ), #70788, .T. ) ;
#52192=DIRECTION ( 'NONE',  ( -1.000000000000000000, -0.000000000000000000, 0.000000000000000000 ) ) ;
#52193=CARTESIAN_POINT ( 'NONE',  ( 0.000000000000000000, 77.16300072079700101, -27.74655509720590985 ) ) ;
#52195=DIRECTION ( 'NONE',  ( 0.000000000000000000, 0.000000000000000000, 1.000000000000000000 ) ) ;
#52196=FACE_OUTER_BOUND ( 'NONE', #21098, .T. ) ;
#52197=EDGE_CURVE ( 'NONE', #33517, #49560, #65345, .T. ) ;
#52200=AXIS2_PLACEMENT_3D ( 'NONE', #15916, #38848, #33194 ) ;
#52202=DIRECTION ( 'NONE',  ( -1.000000000000000000, 0.000000000000000000, -0.000000000000000000 ) ) ;
#52204=CARTESIAN_POINT ( 'NONE',  ( 10.00000000000000000, 0.000000000000000000, 0.000000000000000000 ) ) ;
#52214=DIRECTION ( 'NONE',  ( 0.000000000000000000, 0.000000000000000000, 1.000000000000000000 ) ) ;
#52219=AXIS2_PLACEMENT_3D ( 'NONE', #50197, #62251, #56981 ) ;
#52223=CARTESIAN_POINT ( 'NONE',  ( 10.00000000000000000, 76.41127070299292257, -12.93880638057232346 ) ) ;
#52236=CARTESIAN_POINT ( 'NONE',  ( 0.000000000000000000, -76.41127070299280888, 12.93880638057289012 ) ) ;
#52238=CARTESIAN_POINT ( 'NONE',  ( 0.000000000000000000, 73.44644590900094272, -24.73286445877628026 ) ) ;
#52239=VECTOR ( 'NONE', #2585, 1000.000000000000000 ) ;
#52243=ORIENTED_EDGE ( 'NONE', *, *, #48959, .F. ) ;
#52246=VERTEX_POINT ( 'NONE', #8016 ) ;
#52247=CARTESIAN_POINT ( 'NONE',  ( 10.00000000000000000, -51.03279382321048985, -55.19960302592120627 ) ) ;
#52248=ORIENTED_EDGE ( 'NONE', *, *, #47344, .T. ) ;
#52255=CARTESIAN_POINT ( 'NONE',  ( 10.00000000000000000, 0.000000000000000000, 0.000000000000000000 ) ) ;
#52256=ORIENTED_EDGE ( 'NONE', *, *, #65548, .F. ) ;
#52257=VERTEX_POINT ( 'NONE', #2788 ) ;
#52258=AXIS2_PLACEMENT_3D ( 'NONE', #26111, #49781, #66720 ) ;
#52271=ORIENTED_EDGE ( 'NONE', *, *, #33362, .F. ) ;
#52289=ORIENTED_EDGE ( 'NONE', *, *, #9082, .F. ) ;
#52307=DIRECTION ( 'NONE',  ( 0.000000000000000000, 0.000000000000000000, 1.000000000000000000 ) ) ;
#52311=EDGE_LOOP ( 'NONE', ( #15752, #18133, #327, #6565 ) ) ;
#52313=DIRECTION ( 'NONE',  ( -1.000000000000000000, 0.000000000000000000, 0.000000000000000000 ) ) ;
#52317=ORIENTED_EDGE ( 'NONE', *, *, #28168, .T. ) ;
#52326=FACE_OUTER_BOUND ( 'NONE', #72859, .T. ) ;
#52332=AXIS2_PLACEMENT_3D ( 'NONE', #20369, #32008, #54948 ) ;
#52333=VERTEX_POINT ( 'NONE', #67753 ) ;
#52343=DIRECTION ( 'NONE',  ( 0.000000000000000000, 0.000000000000000000, 1.000000000000000000 ) ) ;
#52344=EDGE_CURVE ( 'NONE', #69008, #8792, #49699, .T. ) ;
#52349=EDGE_CURVE ( 'NONE', #30795, #1255, #9862, .T. ) ;
#52355=ORIENTED_EDGE ( 'NONE', *, *, #30457, .F. ) ;
#52361=CARTESIAN_POINT ( 'NONE',  ( -10.00000000000000000, 0.000000000000000000, 0.000000000000000000 ) ) ;
#52381=DIRECTION ( 'NONE',  ( -1.000000000000000000, 0.000000000000000000, 0.000000000000000000 ) ) ;
#52394=CARTESIAN_POINT ( 'NONE',  ( 10.00000000000000000, -34.44570377933549565, -69.42325613327476219 ) ) ;
#52395=AXIS2_PLACEMENT_3D ( 'NONE', #48559, #31626, #64750 ) ;
#52400=CIRCLE ( 'NONE', #19981, 82.00000000000000000 ) ;
#52409=CYLINDRICAL_SURFACE ( 'NONE', #63519, 31.99999999999999289 ) ;
#52411=ORIENTED_EDGE ( 'NONE', *, *, #21395, .F. ) ;
#52418=ORIENTED_EDGE ( 'NONE', *, *, #72027, .T. ) ;
#52423=CARTESIAN_POINT ( 'NONE',  ( 10.00000000000000000, 65.59268652807263322, -36.72794159290169347 ) ) ;
#52437=EDGE_LOOP ( 'NONE', ( #30346, #69782, #9998, #34662 ) ) ;
#52453=CIRCLE ( 'NONE', #15218, 32.00000000000000000 ) ;
#52464=AXIS2_PLACEMENT_3D ( 'NONE', #39387, #62328, #45786 ) ;
#52466=LINE ( 'NONE', #1017, #10487 ) ;
#52468=CYLINDRICAL_SURFACE ( 'NONE', #44460, 32.00000000000000000 ) ;
#52485=CARTESIAN_POINT ( 'NONE',  ( 10.00000000000000000, -36.73666225445940370, 65.58780272294062286 ) ) ;
#52489=DIRECTION ( 'NONE',  ( 0.000000000000000000, 0.000000000000000000, 1.000000000000000000 ) ) ;
#52500=CARTESIAN_POINT ( 'NONE',  ( -10.00000000000000000, 0.000000000000000000, 0.000000000000000000 ) ) ;
#52502=ADVANCED_FACE ( 'NONE', ( #1228 ), #23379, .T. ) ;
#52506=ORIENTED_EDGE ( 'NONE', *, *, #44465, .T. ) ;
#52507=DIRECTION ( 'NONE',  ( 0.000000000000000000, 0.000000000000000000, -1.000000000000000000 ) ) ;
#52515=EDGE_CURVE ( 'NONE', #45539, #60065, #12084, .T. ) ;
#52523=DIRECTION ( 'NONE',  ( -1.000000000000000000, 0.000000000000000000, 0.000000000000000000 ) ) ;
#52534=CARTESIAN_POINT ( 'NONE',  ( 10.00000000000000000, 67.80270845531956070, -46.11716303203112943 ) ) ;
#52537=ORIENTED_EDGE ( 'NONE', *, *, #35099, .F. ) ;
#52542=ORIENTED_EDGE ( 'NONE', *, *, #14283, .T. ) ;
#52553=CARTESIAN_POINT ( 'NONE',  ( 10.00000000000000000, -18.89407956138203204, -75.16055320797050854 ) ) ;
#52561=CARTESIAN_POINT ( 'NONE',  ( 10.00000000000000000, 51.02545421589402252, -55.20638768913705263 ) ) ;
#52566=DIRECTION ( 'NONE',  ( 0.000000000000000000, 0.000000000000000000, 1.000000000000000000 ) ) ;
#52569=DIRECTION ( 'NONE',  ( -1.000000000000000000, -0.000000000000000000, -0.000000000000000000 ) ) ;
#52573=VECTOR ( 'NONE', #5107, 1000.000000000000000 ) ;
#52579=CARTESIAN_POINT ( 'NONE',  ( 0.000000000000000000, 51.03279382321166224, -55.19960302592011914 ) ) ;
#52580=LINE ( 'NONE', #65360, #63605 ) ;
#52582=CARTESIAN_POINT ( 'NONE',  ( 0.000000000000000000, -8.966570791700153364, -81.50828551894237251 ) ) ;
#52598=ORIENTED_EDGE ( 'NONE', *, *, #28095, .F. ) ;
#52599=VERTEX_POINT ( 'NONE', #8672 ) ;
#52601=CIRCLE ( 'NONE', #38229, 77.49899999999998101 ) ;
#52602=EDGE_CURVE ( 'NONE', #10842, #10255, #31584, .T. ) ;
#52606=VERTEX_POINT ( 'NONE', #19203 ) ;
#52622=DIRECTION ( 'NONE',  ( -1.000000000000000000, 0.000000000000000000, 0.000000000000000000 ) ) ;
#52624=VERTEX_POINT ( 'NONE', #48881 ) ;
#52635=ORIENTED_EDGE ( 'NONE', *, *, #73273, .T. ) ;
#52647=CARTESIAN_POINT ( 'NONE',  ( 0.000000000000000000, 20.40083707022987625, -72.35432306680462489 ) ) ;
#52656=CARTESIAN_POINT ( 'NONE',  ( 5.000000000000000000, 33.71516098798740302, 74.74816331893443078 ) ) ;
#52661=CIRCLE ( 'NONE', #26238, 77.49899999999999523 ) ;
#52666=CARTESIAN_POINT ( 'NONE',  ( -10.00000000000000000, 0.000000000000000000, 0.000000000000000000 ) ) ;
#52674=AXIS2_PLACEMENT_3D ( 'NONE', #48580, #8360, #66253 ) ;
#52678=AXIS2_PLACEMENT_3D ( 'NONE', #13125, #69897, #1532 ) ;
#52681=ORIENTED_EDGE ( 'NONE', *, *, #34386, .F. ) ;
#52686=APPLICATION_CONTEXT ( 'automotive_design' ) ;
#52705=EDGE_CURVE ( 'NONE', #39783, #62434, #70317, .T. ) ;
#52708=EDGE_LOOP ( 'NONE', ( #67306, #21855, #30481, #6026 ) ) ;
#52710=EDGE_CURVE ( 'NONE', #35415, #26778, #36121, .T. ) ;
#52719=CIRCLE ( 'NONE', #37113, 31.99999999999998934 ) ;
#52723=DIRECTION ( 'NONE',  ( 0.000000000000000000, 0.000000000000000000, 1.000000000000000000 ) ) ;
#52729=ORIENTED_EDGE ( 'NONE', *, *, #60851, .F. ) ;
#52732=DIRECTION ( 'NONE',  ( 0.000000000000000000, 0.000000000000000000, 1.000000000000000000 ) ) ;
#52733=DIRECTION ( 'NONE',  ( 0.000000000000000000, 0.000000000000000000, 1.000000000000000000 ) ) ;
#52740=CIRCLE ( 'NONE', #51490, 82.00000000000000000 ) ;
#52760=VERTEX_POINT ( 'NONE', #56393 ) ;
#52770=CARTESIAN_POINT ( 'NONE',  ( 10.00000000000000000, 0.000000000000000000, 0.000000000000000000 ) ) ;
#52775=FACE_OUTER_BOUND ( 'NONE', #69438, .T. ) ;
#52788=VERTEX_POINT ( 'NONE', #32321 ) ;
#52790=VERTEX_POINT ( 'NONE', #50360 ) ;
#52795=ORIENTED_EDGE ( 'NONE', *, *, #11275, .F. ) ;
#52799=DIRECTION ( 'NONE',  ( 0.000000000000000000, 0.5877852522924743583, -0.8090169943749466741 ) ) ;
#52800=ORIENTED_EDGE ( 'NONE', *, *, #51461, .T. ) ;
#52801=EDGE_LOOP ( 'NONE', ( #60128, #1172, #66035, #56587 ) ) ;
#52807=ORIENTED_EDGE ( 'NONE', *, *, #48286, .T. ) ;
#52809=CARTESIAN_POINT ( 'NONE',  ( 10.00000000000000000, -8.966570791700142706, -81.50828551894234408 ) ) ;
#52816=CARTESIAN_POINT ( 'NONE',  ( 10.00000000000000000, 31.46837873495072913, -68.27212725128242710 ) ) ;
#52823=ORIENTED_EDGE ( 'NONE', *, *, #24362, .F. ) ;
#52828=EDGE_CURVE ( 'NONE', #53528, #39808, #49805, .T. ) ;
#52840=ORIENTED_EDGE ( 'NONE', *, *, #70421, .F. ) ;
#52841=CIRCLE ( 'NONE', #39642, 31.99999999999998579 ) ;
#52849=AXIS2_PLACEMENT_3D ( 'NONE', #62780, #62018, #11246 ) ;
#52856=DIRECTION ( 'NONE',  ( -1.000000000000000000, 0.000000000000000000, 0.000000000000000000 ) ) ;
#52859=AXIS2_PLACEMENT_3D ( 'NONE', #68877, #23384, #46310 ) ;
#52872=ORIENTED_EDGE ( 'NONE', *, *, #40178, .T. ) ;
#52876=ADVANCED_FACE ( 'NONE', ( #27804 ), #50730, .T. ) ;
#52878=LINE ( 'NONE', #29184, #33345 ) ;
#52888=ADVANCED_FACE ( 'NONE', ( #10897 ), #15404, .T. ) ;
#52895=ORIENTED_EDGE ( 'NONE', *, *, #5820, .F. ) ;
#52897=AXIS2_PLACEMENT_3D ( 'NONE', #54938, #63195, #436 ) ;
#52901=CIRCLE ( 'NONE', #57745, 32.00000000000000000 ) ;
#52902=DIRECTION ( 'NONE',  ( 0.000000000000000000, 0.8910065241883691201, -0.4539904997395446951 ) ) ;
#52914=VERTEX_POINT ( 'NONE', #29638 ) ;
#52933=VECTOR ( 'NONE', #64143, 1000.000000000000000 ) ;
#52936=AXIS2_PLACEMENT_3D ( 'NONE', #36651, #60712, #9191 ) ;
#52942=CYLINDRICAL_SURFACE ( 'NONE', #7597, 31.99999999999999289 ) ;
#52945=DIRECTION ( 'NONE',  ( -1.000000000000000000, -0.000000000000000000, -0.000000000000000000 ) ) ;
#52946=ADVANCED_FACE ( 'NONE', ( #6728 ), #68788, .T. ) ;
#52955=CIRCLE ( 'NONE', #45739, 77.49900000000000944 ) ;
#52956=EDGE_CURVE ( 'NONE', #8743, #31993, #72604, .T. ) ;
#52961=CARTESIAN_POINT ( 'NONE',  ( 10.00000000000000000, -11.30684508768284680, -76.66974797899850103 ) ) ;
#52981=AXIS2_PLACEMENT_3D ( 'NONE', #56748, #40188, #12339 ) ;
#52988=ORIENTED_EDGE ( 'NONE', *, *, #39813, .F. ) ;
#52989=DIRECTION ( 'NONE',  ( -1.000000000000000000, 0.000000000000000000, 0.000000000000000000 ) ) ;
#52998=ORIENTED_EDGE ( 'NONE', *, *, #26287, .T. ) ;
#53019=DIRECTION ( 'NONE',  ( -1.000000000000000000, 0.000000000000000000, 0.000000000000000000 ) ) ;
#53020=ORIENTED_EDGE ( 'NONE', *, *, #71887, .F. ) ;
#53023=ORIENTED_EDGE ( 'NONE', *, *, #60886, .T. ) ;
#53024=DIRECTION ( 'NONE',  ( -1.000000000000000000, -0.000000000000000000, 0.000000000000000000 ) ) ;
#53041=CARTESIAN_POINT ( 'NONE',  ( 0.000000000000000000, 29.01471420065564644, 76.69515212746026123 ) ) ;
#53044=CARTESIAN_POINT ( 'NONE',  ( 0.000000000000000000, 0.000000000000000000, 0.000000000000000000 ) ) ;
#53060=EDGE_CURVE ( 'NONE', #34583, #17670, #48593, .T. ) ;
#53072=ADVANCED_FACE ( 'NONE', ( #28418 ), #4035, .T. ) ;
#53073=EDGE_CURVE ( 'NONE', #32793, #38655, #3001, .T. ) ;
#53079=DIRECTION ( 'NONE',  ( -1.000000000000000000, 0.000000000000000000, -0.000000000000000000 ) ) ;
#53080=ORIENTED_EDGE ( 'NONE', *, *, #53945, .F. ) ;
#53081=CARTESIAN_POINT ( 'NONE',  ( 0.000000000000000000, -55.20638768913797634, 51.02545421589302777 ) ) ;
#53094=FACE_OUTER_BOUND ( 'NONE', #50089, .T. ) ;
#53114=VECTOR ( 'NONE', #25788, 1000.000000000000000 ) ;
#53124=DIRECTION ( 'NONE',  ( 1.000000000000000000, -0.000000000000000000, -0.000000000000000000 ) ) ;
#53126=ORIENTED_EDGE ( 'NONE', *, *, #45099, .T. ) ;
#53130=DIRECTION ( 'NONE',  ( 0.000000000000000000, -0.7071067811865389130, -0.7071067811865561215 ) ) ;
#53140=CARTESIAN_POINT ( 'NONE',  ( 10.00000000000000000, 0.000000000000000000, 0.000000000000000000 ) ) ;
#53147=AXIS2_PLACEMENT_3D ( 'NONE', #28363, #33253, #40773 ) ;
#53150=ADVANCED_FACE ( 'NONE', ( #34065 ), #5515, .T. ) ;
#53164=ORIENTED_EDGE ( 'NONE', *, *, #34535, .T. ) ;
#53199=ORIENTED_EDGE ( 'NONE', *, *, #54267, .F. ) ;
#53200=CARTESIAN_POINT ( 'NONE',  ( 10.00000000000000000, 0.000000000000000000, 0.000000000000000000 ) ) ;
#53213=CIRCLE ( 'NONE', #56975, 82.00000000000000000 ) ;
#53216=DIRECTION ( 'NONE',  ( -1.000000000000000000, 0.000000000000000000, -0.000000000000000000 ) ) ;
#53217=CIRCLE ( 'NONE', #8774, 31.99999999999999289 ) ;
#53227=DIRECTION ( 'NONE',  ( -1.000000000000000000, 0.000000000000000000, -0.000000000000000000 ) ) ;
#53253=DIRECTION ( 'NONE',  ( -1.000000000000000000, 0.000000000000000000, 0.000000000000000000 ) ) ;
#53264=DIRECTION ( 'NONE',  ( -1.000000000000000000, -0.000000000000000000, -0.000000000000000000 ) ) ;
#53283=CARTESIAN_POINT ( 'NONE',  ( 5.000000000000002665, -76.69515212745996280, -29.01471420065644580 ) ) ;
#53284=ORIENTED_EDGE ( 'NONE', *, *, #2584, .T. ) ;
#53285=CYLINDRICAL_SURFACE ( 'NONE', #31504, 31.99999999999999289 ) ;
#53288=ORIENTED_EDGE ( 'NONE', *, *, #38353, .F. ) ;
#53294=CARTESIAN_POINT ( 'NONE',  ( 10.00000000000000000, -39.78640506895653317, 66.50666863321987421 ) ) ;
#53298=ORIENTED_EDGE ( 'NONE', *, *, #42883, .F. ) ;
#53313=CARTESIAN_POINT ( 'NONE',  ( 10.00000000000000000, 2.956366410621684260, -75.11725578898465017 ) ) ;
#53314=VECTOR ( 'NONE', #26618, 1000.000000000000000 ) ;
#53317=CARTESIAN_POINT ( 'NONE',  ( 0.000000000000000000, -39.47590169984898978, 71.87247863392400404 ) ) ;
#53330=AXIS2_PLACEMENT_3D ( 'NONE', #61421, #15546, #61791 ) ;
#53333=ORIENTED_EDGE ( 'NONE', *, *, #55522, .T. ) ;
#53342=VERTEX_POINT ( 'NONE', #36316 ) ;
#53368=LINE ( 'NONE', #61151, #55831 ) ;
#53375=CARTESIAN_POINT ( 'NONE',  ( 10.00000000000000000, -50.23322058963393033, 64.81221759200326460 ) ) ;
#53376=CIRCLE ( 'NONE', #17360, 82.00000000000000000 ) ;
#53378=EDGE_CURVE ( 'NONE', #28922, #45162, #64528, .T. ) ;
#53387=FACE_OUTER_BOUND ( 'NONE', #28320, .T. ) ;
#53394=CARTESIAN_POINT ( 'NONE',  ( 5.000000000000002665, -22.90783923731686045, 78.73519480814945837 ) ) ;
#53397=DIRECTION ( 'NONE',  ( -1.000000000000000000, 0.000000000000000000, 0.000000000000000000 ) ) ;
#53406=EDGE_CURVE ( 'NONE', #9362, #31085, #59485, .T. ) ;
#53423=DIRECTION ( 'NONE',  ( 0.000000000000000000, 0.000000000000000000, 1.000000000000000000 ) ) ;
#53425=CARTESIAN_POINT ( 'NONE',  ( 10.00000000000000000, -12.93880638057259169, -76.41127070299286572 ) ) ;
#53431=CIRCLE ( 'NONE', #42658, 82.00000000000000000 ) ;
#53435=VERTEX_POINT ( 'NONE', #58145 ) ;
#53442=CARTESIAN_POINT ( 'NONE',  ( 0.000000000000000000, -8.830959090341869100, -74.65491531819127147 ) ) ;
#53447=DIRECTION ( 'NONE',  ( 1.000000000000000000, 0.000000000000000000, 0.000000000000000000 ) ) ;
#53453=DIRECTION ( 'NONE',  ( -1.000000000000000000, 0.000000000000000000, -0.000000000000000000 ) ) ;
#53461=CARTESIAN_POINT ( 'NONE',  ( 0.000000000000000000, -55.38113227695743745, -54.21277698773734244 ) ) ;
#53472=CARTESIAN_POINT ( 'NONE',  ( 5.000000000000002665, -29.01471420065617224, 76.69515212746007649 ) ) ;
#53476=CARTESIAN_POINT ( 'NONE',  ( 10.00000000000000000, -46.54456581323762521, -59.03342792756313884 ) ) ;
#53482=AXIS2_PLACEMENT_3D ( 'NONE', #50194, #22386, #15637 ) ;
#53484=ORIENTED_EDGE ( 'NONE', *, *, #68856, .F. ) ;
#53486=CIRCLE ( 'NONE', #28298, 32.00000000000000000 ) ;
#53500=CARTESIAN_POINT ( 'NONE',  ( 5.000000000000000000, -50.23322058963298531, -64.81221759200398935 ) ) ;
#53503=COLOUR_RGB ( '', 0.08235294, 0.09019608, 0.10196078) ;
#53517=ORIENTED_EDGE ( 'NONE', *, *, #68768, .T. ) ;
#53524=CARTESIAN_POINT ( 'NONE',  ( 10.00000000000000000, 70.52718814184260054, 26.02418014898334420 ) ) ;
#53528=VERTEX_POINT ( 'NONE', #33165 ) ;
#53535=ORIENTED_EDGE ( 'NONE', *, *, #15776, .F. ) ;
#53538=CARTESIAN_POINT ( 'NONE',  ( 0.000000000000000000, 75.11764819372142199, 2.946379043147685728 ) ) ;
#53568=ORIENTED_EDGE ( 'NONE', *, *, #58305, .T. ) ;
#53583=DIRECTION ( 'NONE',  ( 0.000000000000000000, 0.8910065241883655673, 0.4539904997395510233 ) ) ;
#53596=CARTESIAN_POINT ( 'NONE',  ( 0.000000000000000000, 0.000000000000000000, 0.000000000000000000 ) ) ;
#53602=VERTEX_POINT ( 'NONE', #49356 ) ;
#53604=ORIENTED_EDGE ( 'NONE', *, *, #42703, .T. ) ;
#53606=DIRECTION ( 'NONE',  ( 0.000000000000000000, -0.3090169943749548342, 0.9510565162951510887 ) ) ;
#53610=VERTEX_POINT ( 'NONE', #39196 ) ;
#53615=DIRECTION ( 'NONE',  ( -1.000000000000000000, 0.000000000000000000, 0.000000000000000000 ) ) ;
#53619=DIRECTION ( 'NONE',  ( 0.000000000000000000, -6.982962677686266711E-15, 1.000000000000000000 ) ) ;
#53624=ORIENTED_EDGE ( 'NONE', *, *, #19671, .T. ) ;
#53627=EDGE_LOOP ( 'NONE', ( #72994, #4016, #45525, #46623 ) ) ;
#53634=AXIS2_PLACEMENT_3D ( 'NONE', #11506, #16418, #51359 ) ;
#53635=CARTESIAN_POINT ( 'NONE',  ( 10.00000000000000000, 44.88180994100468268, -63.18004540532978552 ) ) ;
#53641=ORIENTED_EDGE ( 'NONE', *, *, #73405, .F. ) ;
#53643=CIRCLE ( 'NONE', #25998, 32.00000000000000000 ) ;
#53656=AXIS2_PLACEMENT_3D ( 'NONE', #22090, #56684, #32979 ) ;
#53670=CARTESIAN_POINT ( 'NONE',  ( 10.00000000000000000, -63.18004540532994184, -44.88180994100446952 ) ) ;
#53694=DIRECTION ( 'NONE',  ( 0.000000000000000000, 0.000000000000000000, -1.000000000000000000 ) ) ;
#53698=ORIENTED_EDGE ( 'NONE', *, *, #60199, .F. ) ;
#53700=ORIENTED_EDGE ( 'NONE', *, *, #72893, .T. ) ;
#53702=EDGE_CURVE ( 'NONE', #21621, #72558, #29644, .T. ) ;
#53712=ORIENTED_EDGE ( 'NONE', *, *, #38527, .F. ) ;
#53735=EDGE_LOOP ( 'NONE', ( #71905, #45038, #60119, #33282 ) ) ;
#53743=ORIENTED_EDGE ( 'NONE', *, *, #64698, .T. ) ;
#53748=DIRECTION ( 'NONE',  ( 0.000000000000000000, 0.000000000000000000, 1.000000000000000000 ) ) ;
#53750=ORIENTED_EDGE ( 'NONE', *, *, #30011, .T. ) ;
#53767=CIRCLE ( 'NONE', #12971, 31.99999999999999289 ) ;
#53769=CARTESIAN_POINT ( 'NONE',  ( 10.00000000000000000, -55.20638768913797634, 51.02545421589302777 ) ) ;
#53770=CARTESIAN_POINT ( 'NONE',  ( 5.000000000000002665, 81.50828551894240093, -8.966570791699803422 ) ) ;
#53771=FACE_OUTER_BOUND ( 'NONE', #73672, .T. ) ;
#53774=FACE_OUTER_BOUND ( 'NONE', #72205, .T. ) ;
#53775=VERTEX_POINT ( 'NONE', #23747 ) ;
#53788=CARTESIAN_POINT ( 'NONE',  ( 0.000000000000000000, -44.99326035066006568, -68.55367621811190304 ) ) ;
#53791=VERTEX_POINT ( 'NONE', #13567 ) ;
#53801=AXIS2_PLACEMENT_3D ( 'NONE', #42538, #13944, #58719 ) ;
#53809=AXIS2_PLACEMENT_3D ( 'NONE', #52770, #30928, #48241 ) ;
#53814=CARTESIAN_POINT ( 'NONE',  ( 0.000000000000000000, 20.41045688087824317, 72.35160999960824313 ) ) ;
#53824=DIRECTION ( 'NONE',  ( -1.000000000000000000, 0.000000000000000000, -0.000000000000000000 ) ) ;
#53831=EDGE_CURVE ( 'NONE', #53610, #60557, #26061, .T. ) ;
#53843=AXIS2_PLACEMENT_3D ( 'NONE', #64418, #58029, #46383 ) ;
#53851=CARTESIAN_POINT ( 'NONE',  ( 10.00000000000000000, -62.50884508063395373, -41.76106447765554464 ) ) ;
#53854=CARTESIAN_POINT ( 'NONE',  ( 0.000000000000000000, 0.000000000000000000, 0.000000000000000000 ) ) ;
#53867=DIRECTION ( 'NONE',  ( -1.000000000000000000, -0.000000000000000000, -0.000000000000000000 ) ) ;
#53878=DIRECTION ( 'NONE',  ( -1.000000000000000000, 0.000000000000000000, 0.000000000000000000 ) ) ;
#53880=FACE_OUTER_BOUND ( 'NONE', #7928, .T. ) ;
#53887=ORIENTED_EDGE ( 'NONE', *, *, #42339, .F. ) ;
#53889=FACE_OUTER_BOUND ( 'NONE', #17179, .T. ) ;
#53890=DIRECTION ( 'NONE',  ( 0.000000000000000000, 0.000000000000000000, 1.000000000000000000 ) ) ;
#53897=AXIS2_PLACEMENT_3D ( 'NONE', #70304, #18808, #36113 ) ;
#53902=VERTEX_POINT ( 'NONE', #7674 ) ;
#53904=ORIENTED_EDGE ( 'NONE', *, *, #50860, .F. ) ;
#53906=ORIENTED_EDGE ( 'NONE', *, *, #69096, .F. ) ;
#53908=EDGE_LOOP ( 'NONE', ( #63987, #4025, #59756, #3427 ) ) ;
#53919=ORIENTED_EDGE ( 'NONE', *, *, #47430, .F. ) ;
#53927=CARTESIAN_POINT ( 'NONE',  ( -10.00000000000000000, 0.000000000000000000, 0.000000000000000000 ) ) ;
#53930=CIRCLE ( 'NONE', #10719, 32.00000000000000000 ) ;
#53943=DIRECTION ( 'NONE',  ( -1.000000000000000000, 0.000000000000000000, 0.000000000000000000 ) ) ;
#53944=DIRECTION ( 'NONE',  ( -1.000000000000000000, -0.000000000000000000, -0.000000000000000000 ) ) ;
#53945=EDGE_CURVE ( 'NONE', #47197, #62527, #14035, .T. ) ;
#53948=CARTESIAN_POINT ( 'NONE',  ( 10.00000000000000000, 0.000000000000000000, 0.000000000000000000 ) ) ;
#53957=DIRECTION ( 'NONE',  ( 0.000000000000000000, 0.4539904997395413089, 0.8910065241883705633 ) ) ;
#53965=VECTOR ( 'NONE', #33709, 1000.000000000000000 ) ;
#53969=DIRECTION ( 'NONE',  ( 1.000000000000000000, -0.000000000000000000, -0.000000000000000000 ) ) ;
#53971=DIRECTION ( 'NONE',  ( -1.000000000000000000, -0.000000000000000000, -0.000000000000000000 ) ) ;
#53978=LINE ( 'NONE', #2522, #32893 ) ;
#53993=DIRECTION ( 'NONE',  ( 0.000000000000000000, 0.3090169943749482839, -0.9510565162951533091 ) ) ;
#54003=DIRECTION ( 'NONE',  ( -1.000000000000000000, 0.000000000000000000, -0.000000000000000000 ) ) ;
#54012=EDGE_CURVE ( 'NONE', #25891, #31993, #66855, .T. ) ;
#54018=CARTESIAN_POINT ( 'NONE',  ( 10.00000000000000000, 75.11764819372149304, -2.946379043146603482 ) ) ;
#54020=ORIENTED_EDGE ( 'NONE', *, *, #28605, .T. ) ;
#54024=ORIENTED_EDGE ( 'NONE', *, *, #50339, .T. ) ;
#54030=CARTESIAN_POINT ( 'NONE',  ( 10.00000000000000000, -65.64334221924939072, 41.19522573413710376 ) ) ;
#54036=AXIS2_PLACEMENT_3D ( 'NONE', #59972, #44139, #9919 ) ;
#54056=DIRECTION ( 'NONE',  ( 0.000000000000000000, 0.000000000000000000, 1.000000000000000000 ) ) ;
#54061=EDGE_CURVE ( 'NONE', #29988, #71738, #72841, .T. ) ;
#54069=EDGE_CURVE ( 'NONE', #63900, #7213, #45363, .T. ) ;
#54070=AXIS2_PLACEMENT_3D ( 'NONE', #13892, #65786, #19175 ) ;
#54071=ADVANCED_FACE ( 'NONE', ( #72302 ), #20801, .T. ) ;
#54073=ORIENTED_EDGE ( 'NONE', *, *, #45872, .F. ) ;
#54077=CARTESIAN_POINT ( 'NONE',  ( 0.000000000000000000, 0.000000000000000000, 0.000000000000000000 ) ) ;
#54078=CIRCLE ( 'NONE', #18070, 32.00000000000000000 ) ;
#54083=CIRCLE ( 'NONE', #73282, 82.00000000000000000 ) ;
#54084=EDGE_LOOP ( 'NONE', ( #5065, #66018, #38287, #49190 ) ) ;
#54085=CIRCLE ( 'NONE', #21665, 77.49900000000000944 ) ;
#54097=VERTEX_POINT ( 'NONE', #56883 ) ;
#54108=DIRECTION ( 'NONE',  ( 0.000000000000000000, 0.000000000000000000, 1.000000000000000000 ) ) ;
#54114=VERTEX_POINT ( 'NONE', #28285 ) ;
#54117=CYLINDRICAL_SURFACE ( 'NONE', #44462, 77.49899999999999523 ) ;
#54131=CYLINDRICAL_SURFACE ( 'NONE', #60024, 31.99999999999999289 ) ;
#54133=ORIENTED_EDGE ( 'NONE', *, *, #64006, .F. ) ;
#54134=CARTESIAN_POINT ( 'NONE',  ( 10.00000000000000000, -24.73286445877757345, 73.44644590900053061 ) ) ;
#54144=DIRECTION ( 'NONE',  ( -1.000000000000000000, 0.000000000000000000, -0.000000000000000000 ) ) ;
#54152=DIRECTION ( 'NONE',  ( 0.000000000000000000, 0.000000000000000000, 1.000000000000000000 ) ) ;
#54157=CYLINDRICAL_SURFACE ( 'NONE', #40622, 31.99999999999999289 ) ;
#54163=CARTESIAN_POINT ( 'NONE',  ( 10.00000000000000000, -65.59268652807183742, -36.72794159290312166 ) ) ;
#54165=ORIENTED_EDGE ( 'NONE', *, *, #29671, .T. ) ;
#54168=CARTESIAN_POINT ( 'NONE',  ( 0.000000000000000000, -75.16055320797016748, -18.89407956138335365 ) ) ;
#54169=CARTESIAN_POINT ( 'NONE',  ( 0.000000000000000000, -40.65526001592664329, 71.21200624218782593 ) ) ;
#54173=AXIS2_PLACEMENT_3D ( 'NONE', #15382, #59508, #9008 ) ;
#54177=ADVANCED_FACE ( 'NONE', ( #38839 ), #67783, .T. ) ;
#54178=FACE_OUTER_BOUND ( 'NONE', #4264, .T. ) ;
#54193=VECTOR ( 'NONE', #61091, 1000.000000000000000 ) ;
#54194=ORIENTED_EDGE ( 'NONE', *, *, #64193, .T. ) ;
#54202=ORIENTED_EDGE ( 'NONE', *, *, #11930, .F. ) ;
#54208=ORIENTED_EDGE ( 'NONE', *, *, #68865, .T. ) ;
#54230=CARTESIAN_POINT ( 'NONE',  ( 5.000000000000000000, -44.99326035066101781, 68.55367621811127776 ) ) ;
#54253=CARTESIAN_POINT ( 'NONE',  ( -10.00000000000000000, 0.000000000000000000, 0.000000000000000000 ) ) ;
#54256=DIRECTION ( 'NONE',  ( 0.000000000000000000, 0.000000000000000000, 1.000000000000000000 ) ) ;
#54263=DIRECTION ( 'NONE',  ( 0.000000000000000000, 0.000000000000000000, 1.000000000000000000 ) ) ;
#54264=DIRECTION ( 'NONE',  ( -1.000000000000000000, -0.000000000000000000, 0.000000000000000000 ) ) ;
#54266=ORIENTED_EDGE ( 'NONE', *, *, #915, .T. ) ;
#54267=EDGE_CURVE ( 'NONE', #25004, #28623, #25163, .T. ) ;
#54289=VERTEX_POINT ( 'NONE', #18765 ) ;
#54294=EDGE_LOOP ( 'NONE', ( #46891, #20702, #33866, #21334 ) ) ;
#54305=EDGE_CURVE ( 'NONE', #9979, #17228, #48453, .T. ) ;
#54312=CYLINDRICAL_SURFACE ( 'NONE', #28720, 31.99999999999999289 ) ;
#54313=DIRECTION ( 'NONE',  ( 0.000000000000000000, 0.000000000000000000, -1.000000000000000000 ) ) ;
#54317=ORIENTED_EDGE ( 'NONE', *, *, #29959, .F. ) ;
#54321=DIRECTION ( 'NONE',  ( -1.000000000000000000, 0.000000000000000000, 0.000000000000000000 ) ) ;
#54322=DIRECTION ( 'NONE',  ( -1.000000000000000000, -0.000000000000000000, -0.000000000000000000 ) ) ;
#54338=CARTESIAN_POINT ( 'NONE',  ( 5.000000000000002665, -3.894527615417340272, -81.90746397400393164 ) ) ;
#54339=DIRECTION ( 'NONE',  ( 0.000000000000000000, 0.7604059656000323741, -0.6494480483301819929 ) ) ;
#54350=DIRECTION ( 'NONE',  ( -1.000000000000000000, -0.000000000000000000, -0.000000000000000000 ) ) ;
#54371=ORIENTED_EDGE ( 'NONE', *, *, #42184, .F. ) ;
#54378=CARTESIAN_POINT ( 'NONE',  ( 10.00000000000000000, -22.90783923731575911, -78.73519480814978522 ) ) ;
#54379=CARTESIAN_POINT ( 'NONE',  ( 10.00000000000000000, 0.000000000000000000, 0.000000000000000000 ) ) ;
#54382=ORIENTED_EDGE ( 'NONE', *, *, #39471, .T. ) ;
#54390=DIRECTION ( 'NONE',  ( -1.000000000000000000, 0.000000000000000000, -0.000000000000000000 ) ) ;
#54392=ADVANCED_FACE ( 'NONE', ( #55950 ), #26628, .T. ) ;
#54394=ORIENTED_EDGE ( 'NONE', *, *, #39408, .F. ) ;
#54395=DIRECTION ( 'NONE',  ( 0.000000000000000000, 0.000000000000000000, 1.000000000000000000 ) ) ;
#54405=EDGE_CURVE ( 'NONE', #19072, #69267, #23714, .T. ) ;
#54411=LINE ( 'NONE', #53670, #73108 ) ;
#54412=DIRECTION ( 'NONE',  ( 1.000000000000000000, 0.000000000000000000, 0.000000000000000000 ) ) ;
#54416=CARTESIAN_POINT ( 'NONE',  ( 10.00000000000000000, 0.000000000000000000, 0.000000000000000000 ) ) ;
#54432=ADVANCED_FACE ( 'NONE', ( #55208 ), #44303, .T. ) ;
#54434=AXIS2_PLACEMENT_3D ( 'NONE', #45318, #27638, #68244 ) ;
#54435=CARTESIAN_POINT ( 'NONE',  ( 10.00000000000000000, -46.21855187248673502, 62.20884554314003623 ) ) ;
#54439=CIRCLE ( 'NONE', #18431, 31.99999999999999289 ) ;
#54440=AXIS2_PLACEMENT_3D ( 'NONE', #19185, #24461, #69942 ) ;
#54460=ORIENTED_EDGE ( 'NONE', *, *, #39826, .T. ) ;
#54462=DIRECTION ( 'NONE',  ( 0.000000000000000000, 0.7071067811865439090, 0.7071067811865512365 ) ) ;
#54472=ORIENTED_EDGE ( 'NONE', *, *, #68671, .F. ) ;
#54474=ORIENTED_EDGE ( 'NONE', *, *, #24802, .F. ) ;
#54484=DIRECTION ( 'NONE',  ( -1.000000000000000000, 0.000000000000000000, 0.000000000000000000 ) ) ;
#54489=CARTESIAN_POINT ( 'NONE',  ( 0.000000000000000000, 0.000000000000000000, 0.000000000000000000 ) ) ;
#54500=AXIS2_PLACEMENT_3D ( 'NONE', #45289, #27970, #73081 ) ;
#54501=AXIS2_PLACEMENT_3D ( 'NONE', #53769, #59055, #13175 ) ;
#54506=ADVANCED_FACE ( 'NONE', ( #10455 ), #29218, .T. ) ;
#54508=EDGE_CURVE ( 'NONE', #60065, #61902, #38088, .T. ) ;
#54525=DIRECTION ( 'NONE',  ( -1.000000000000000000, 0.000000000000000000, 0.000000000000000000 ) ) ;
#54543=ORIENTED_EDGE ( 'NONE', *, *, #45434, .T. ) ;
#54554=DIRECTION ( 'NONE',  ( 0.000000000000000000, -1.000000000000000000, -1.040834085586084730E-14 ) ) ;
#54557=CARTESIAN_POINT ( 'NONE',  ( 10.00000000000000000, 81.90746397400388901, 3.894527615418187150 ) ) ;
#54569=ORIENTED_EDGE ( 'NONE', *, *, #2905, .F. ) ;
#54570=CARTESIAN_POINT ( 'NONE',  ( 10.00000000000000000, -67.80270845531855173, -46.11716303203261447 ) ) ;
#54579=VERTEX_POINT ( 'NONE', #27749 ) ;
#54581=DIRECTION ( 'NONE',  ( 0.000000000000000000, -0.5224985647159559043, 0.8526401643540879594 ) ) ;
#54582=EDGE_CURVE ( 'NONE', #54579, #70, #35024, .T. ) ;
#54585=DIRECTION ( 'NONE',  ( -1.000000000000000000, -0.000000000000000000, 0.000000000000000000 ) ) ;
#54594=DIRECTION ( 'NONE',  ( -1.000000000000000000, 0.000000000000000000, 0.000000000000000000 ) ) ;
#54598=EDGE_CURVE ( 'NONE', #2735, #16527, #66270, .T. ) ;
#54601=CARTESIAN_POINT ( 'NONE',  ( 5.000000000000002665, -71.21200624218825226, 40.65526001592589722 ) ) ;
#54604=VERTEX_POINT ( 'NONE', #56712 ) ;
#54606=DIRECTION ( 'NONE',  ( -1.000000000000000000, 0.000000000000000000, 0.000000000000000000 ) ) ;
#54616=VECTOR ( 'NONE', #41919, 1000.000000000000000 ) ;
#54626=CARTESIAN_POINT ( 'NONE',  ( 10.00000000000000000, -14.66109333815513160, 73.73191006444567108 ) ) ;
#54627=( NAMED_UNIT ( * ) PLANE_ANGLE_UNIT ( ) SI_UNIT ( $, .RADIAN. ) );
#54638=ORIENTED_EDGE ( 'NONE', *, *, #2815, .F. ) ;
#54641=VERTEX_POINT ( 'NONE', #2182 ) ;
#54646=CIRCLE ( 'NONE', #3054, 77.49900000000000944 ) ;
#54648=ORIENTED_EDGE ( 'NONE', *, *, #67246, .F. ) ;
#54651=ORIENTED_EDGE ( 'NONE', *, *, #47294, .T. ) ;
#54654=AXIS2_PLACEMENT_3D ( 'NONE', #5358, #51191, #74125 ) ;
#54657=DIRECTION ( 'NONE',  ( 0.000000000000000000, -0.9876883405951394357, 0.1564344650402205716 ) ) ;
#54665=ORIENTED_EDGE ( 'NONE', *, *, #28509, .F. ) ;
#54669=ORIENTED_EDGE ( 'NONE', *, *, #5947, .T. ) ;
#54677=DIRECTION ( 'NONE',  ( -1.000000000000000000, -0.000000000000000000, 0.000000000000000000 ) ) ;
#54686=DIRECTION ( 'NONE',  ( 0.000000000000000000, 0.000000000000000000, 1.000000000000000000 ) ) ;
#54700=CARTESIAN_POINT ( 'NONE',  ( 0.000000000000000000, -41.19522573413780009, 65.64334221924896440 ) ) ;
#54717=ORIENTED_EDGE ( 'NONE', *, *, #34797, .T. ) ;
#54728=ADVANCED_FACE ( 'NONE', ( #41258 ), #13777, .T. ) ;
#54731=DIRECTION ( 'NONE',  ( 0.000000000000000000, 0.8526401643540936215, -0.5224985647159469115 ) ) ;
#54744=DIRECTION ( 'NONE',  ( -1.000000000000000000, -0.000000000000000000, -0.000000000000000000 ) ) ;
#54747=ORIENTED_EDGE ( 'NONE', *, *, #213, .F. ) ;
#54751=EDGE_CURVE ( 'NONE', #42459, #38362, #33838, .T. ) ;
#54757=CIRCLE ( 'NONE', #7903, 31.99999999999998579 ) ;
#54759=FACE_OUTER_BOUND ( 'NONE', #37642, .T. ) ;
#54769=DIRECTION ( 'NONE',  ( 0.000000000000000000, -0.07845909572783053842, -0.9969173337331290741 ) ) ;
#54770=ADVANCED_FACE ( 'NONE', ( #47631 ), #70539, .T. ) ;
#54775=VECTOR ( 'NONE', #39529, 1000.000000000000000 ) ;
#54776=DIRECTION ( 'NONE',  ( 0.000000000000000000, 0.000000000000000000, 1.000000000000000000 ) ) ;
#54789=LINE ( 'NONE', #73551, #14808 ) ;
#54802=AXIS2_PLACEMENT_3D ( 'NONE', #8259, #37583, #30076 ) ;
#54807=EDGE_CURVE ( 'NONE', #49292, #59685, #15267, .T. ) ;
#54813=ORIENTED_EDGE ( 'NONE', *, *, #52956, .T. ) ;
#54815=CIRCLE ( 'NONE', #36841, 31.99999999999998934 ) ;
#54816=CARTESIAN_POINT ( 'NONE',  ( 0.000000000000000000, 0.000000000000000000, 0.000000000000000000 ) ) ;
#54818=ORIENTED_EDGE ( 'NONE', *, *, #64858, .F. ) ;
#54823=DIRECTION ( 'NONE',  ( -1.000000000000000000, 0.000000000000000000, 0.000000000000000000 ) ) ;
#54829=ORIENTED_EDGE ( 'NONE', *, *, #67416, .T. ) ;
#54853=ADVANCED_FACE ( 'NONE', ( #49477 ), #31442, .T. ) ;
#54854=DIRECTION ( 'NONE',  ( 0.000000000000000000, 0.000000000000000000, 1.000000000000000000 ) ) ;
#54860=DIRECTION ( 'NONE',  ( 0.000000000000000000, -0.8910065241883722287, 0.4539904997395382558 ) ) ;
#54861=AXIS2_PLACEMENT_3D ( 'NONE', #27018, #43604, #10110 ) ;
#54864=DIRECTION ( 'NONE',  ( -1.000000000000000000, -0.000000000000000000, -0.000000000000000000 ) ) ;
#54867=AXIS2_PLACEMENT_3D ( 'NONE', #51247, #63292, #68178 ) ;
#54888=EDGE_LOOP ( 'NONE', ( #20045, #69988, #45701, #67256 ) ) ;
#54891=CYLINDRICAL_SURFACE ( 'NONE', #26222, 77.49899999999999523 ) ;
#54897=VERTEX_POINT ( 'NONE', #26169 ) ;
#54900=CARTESIAN_POINT ( 'NONE',  ( 10.00000000000000000, -65.59268652807237743, 36.72794159290217664 ) ) ;
#54901=ORIENTED_EDGE ( 'NONE', *, *, #44346, .F. ) ;
#54912=ORIENTED_EDGE ( 'NONE', *, *, #18761, .F. ) ;
#54916=AXIS2_PLACEMENT_3D ( 'NONE', #33611, #67458, #45663 ) ;
#54925=DIRECTION ( 'NONE',  ( 0.000000000000000000, 0.000000000000000000, 1.000000000000000000 ) ) ;
#54928=VERTEX_POINT ( 'NONE', #23149 ) ;
#54933=CARTESIAN_POINT ( 'NONE',  ( 5.000000000000002665, -10.30890764327323872, -81.34940948281348483 ) ) ;
#54938=CARTESIAN_POINT ( 'NONE',  ( -10.00000000000000000, 0.000000000000000000, 0.000000000000000000 ) ) ;
#54948=DIRECTION ( 'NONE',  ( 0.000000000000000000, 0.000000000000000000, 1.000000000000000000 ) ) ;
#54949=DIRECTION ( 'NONE',  ( -1.000000000000000000, -0.000000000000000000, 0.000000000000000000 ) ) ;
#54952=DIRECTION ( 'NONE',  ( 0.000000000000000000, 0.000000000000000000, -1.000000000000000000 ) ) ;
#54953=DIRECTION ( 'NONE',  ( 0.000000000000000000, -0.4539904997395350916, -0.8910065241883738940 ) ) ;
#54957=DIRECTION ( 'NONE',  ( -1.000000000000000000, -0.000000000000000000, -0.000000000000000000 ) ) ;
#54968=FACE_OUTER_BOUND ( 'NONE', #52311, .T. ) ;
#54970=DIRECTION ( 'NONE',  ( -1.000000000000000000, 0.000000000000000000, -0.000000000000000000 ) ) ;
#55001=VERTEX_POINT ( 'NONE', #45721 ) ;
#55003=ADVANCED_FACE ( 'NONE', ( #28022 ), #4755, .T. ) ;
#55014=ORIENTED_EDGE ( 'NONE', *, *, #26510, .T. ) ;
#55022=CARTESIAN_POINT ( 'NONE',  ( 10.00000000000000000, -10.30890764327441822, 81.34940948281332851 ) ) ;
#55024=AXIS2_PLACEMENT_3D ( 'NONE', #42877, #65444, #71053 ) ;
#55043=ORIENTED_EDGE ( 'NONE', *, *, #6366, .F. ) ;
#55044=CIRCLE ( 'NONE', #44266, 77.49900000000000944 ) ;
#55055=ORIENTED_EDGE ( 'NONE', *, *, #65911, .T. ) ;
#55061=CARTESIAN_POINT ( 'NONE',  ( 0.000000000000000000, 59.03961581697465277, -46.53671651293886669 ) ) ;
#55078=AXIS2_PLACEMENT_3D ( 'NONE', #15478, #38421, #60974 ) ;
#55081=DIRECTION ( 'NONE',  ( 0.000000000000000000, 0.000000000000000000, -1.000000000000000000 ) ) ;
#55082=EDGE_LOOP ( 'NONE', ( #54317, #73326, #4996, #23335 ) ) ;
#55087=CIRCLE ( 'NONE', #69526, 77.49899999999999523 ) ;
#55089=VECTOR ( 'NONE', #39944, 1000.000000000000000 ) ;
#55092=ADVANCED_FACE ( 'NONE', ( #23880 ), #23506, .T. ) ;
#55105=ORIENTED_EDGE ( 'NONE', *, *, #16225, .F. ) ;
#55106=DIRECTION ( 'NONE',  ( 1.000000000000000000, 0.000000000000000000, -0.000000000000000000 ) ) ;
#55125=FACE_OUTER_BOUND ( 'NONE', #71673, .T. ) ;
#55126=CARTESIAN_POINT ( 'NONE',  ( 10.00000000000000000, -59.46389618801928378, -49.70050353004953791 ) ) ;
#55131=DIRECTION ( 'NONE',  ( -1.000000000000000000, 0.000000000000000000, -0.000000000000000000 ) ) ;
#55134=CIRCLE ( 'NONE', #47944, 32.00000000000000000 ) ;
#55155=CIRCLE ( 'NONE', #59952, 31.99999999999999289 ) ;
#55165=VERTEX_POINT ( 'NONE', #29870 ) ;
#55184=EDGE_CURVE ( 'NONE', #71222, #67983, #8674, .T. ) ;
#55198=AXIS2_PLACEMENT_3D ( 'NONE', #12232, #35533, #64484 ) ;
#55199=LINE ( 'NONE', #66491, #66516 ) ;
#55208=FACE_OUTER_BOUND ( 'NONE', #60045, .T. ) ;
#55210=DIRECTION ( 'NONE',  ( -1.000000000000000000, 0.000000000000000000, 0.000000000000000000 ) ) ;
#55215=ORIENTED_EDGE ( 'NONE', *, *, #25748, .F. ) ;
#55218=ORIENTED_EDGE ( 'NONE', *, *, #15449, .F. ) ;
#55219=DIRECTION ( 'NONE',  ( -1.000000000000000000, -0.000000000000000000, -0.000000000000000000 ) ) ;
#55221=CARTESIAN_POINT ( 'NONE',  ( 5.000000000000000000, -51.29473840253270112, 63.97538442413407012 ) ) ;
#55229=DIRECTION ( 'NONE',  ( 0.000000000000000000, -0.1564344650402170744, -0.9876883405951398798 ) ) ;
#55231=DIRECTION ( 'NONE',  ( 0.000000000000000000, 0.7071067811865436870, 0.7071067811865512365 ) ) ;
#55236=DIRECTION ( 'NONE',  ( -1.000000000000000000, 0.000000000000000000, 0.000000000000000000 ) ) ;
#55242=CARTESIAN_POINT ( 'NONE',  ( 0.000000000000000000, 8.966570791700698706, 81.50828551894228724 ) ) ;
#55245=DIRECTION ( 'NONE',  ( -1.000000000000000000, 0.000000000000000000, 0.000000000000000000 ) ) ;
#55251=ADVANCED_FACE ( 'NONE', ( #66332 ), #38109, .T. ) ;
#55260=AXIS2_PLACEMENT_3D ( 'NONE', #52125, #14022, #59914 ) ;
#55270=EDGE_LOOP ( 'NONE', ( #65597, #59724, #50038, #63271 ) ) ;
#55271=ORIENTED_EDGE ( 'NONE', *, *, #16402, .F. ) ;
#55275=ORIENTED_EDGE ( 'NONE', *, *, #16916, .T. ) ;
#55282=ORIENTED_EDGE ( 'NONE', *, *, #62672, .F. ) ;
#55283=CARTESIAN_POINT ( 'NONE',  ( 5.000000000000000000, -74.74816331893404708, -33.71516098798818462 ) ) ;
#55285=AXIS2_PLACEMENT_3D ( 'NONE', #34824, #28430, #6265 ) ;
#55289=VECTOR ( 'NONE', #17224, 1000.000000000000000 ) ;
#55291=VERTEX_POINT ( 'NONE', #48218 ) ;
#55310=DIRECTION ( 'NONE',  ( -1.000000000000000000, 0.000000000000000000, -0.000000000000000000 ) ) ;
#55319=DIRECTION ( 'NONE',  ( -1.000000000000000000, 0.000000000000000000, 0.000000000000000000 ) ) ;
#55320=CYLINDRICAL_SURFACE ( 'NONE', #26098, 82.00000000000000000 ) ;
#55335=DIRECTION ( 'NONE',  ( 1.000000000000000000, -0.000000000000000000, -0.000000000000000000 ) ) ;
#55338=AXIS2_PLACEMENT_3D ( 'NONE', #56661, #69042, #68677 ) ;
#55340=AXIS2_PLACEMENT_3D ( 'NONE', #43796, #37416, #37028 ) ;
#55341=LINE ( 'NONE', #21117, #31621 ) ;
#55350=CARTESIAN_POINT ( 'NONE',  ( 10.00000000000000000, 44.99326035066052754, 68.55367621811160461 ) ) ;
#55356=CARTESIAN_POINT ( 'NONE',  ( 10.00000000000000000, -30.41916302227060598, -71.27951684758059514 ) ) ;
#55366=LINE ( 'NONE', #31319, #18710 ) ;
#55369=FACE_OUTER_BOUND ( 'NONE', #4528, .T. ) ;
#55388=AXIS2_PLACEMENT_3D ( 'NONE', #14475, #3961, #49428 ) ;
#55392=ORIENTED_EDGE ( 'NONE', *, *, #16187, .F. ) ;
#55395=CIRCLE ( 'NONE', #37384, 31.99999999999999645 ) ;
#55407=ORIENTED_EDGE ( 'NONE', *, *, #14358, .F. ) ;
#55412=DIRECTION ( 'NONE',  ( -1.000000000000000000, 0.000000000000000000, 0.000000000000000000 ) ) ;
#55413=DIRECTION ( 'NONE',  ( -1.000000000000000000, 0.000000000000000000, 0.000000000000000000 ) ) ;
#55438=DIRECTION ( 'NONE',  ( 1.000000000000000000, -0.000000000000000000, -0.000000000000000000 ) ) ;
#55439=CYLINDRICAL_SURFACE ( 'NONE', #4131, 32.00000000000000000 ) ;
#55441=CARTESIAN_POINT ( 'NONE',  ( 10.00000000000000000, 73.95703589264006439, -23.16143007188350822 ) ) ;
#55447=DIRECTION ( 'NONE',  ( -1.000000000000000000, 0.000000000000000000, 0.000000000000000000 ) ) ;
#55448=ORIENTED_EDGE ( 'NONE', *, *, #7966, .F. ) ;
#55453=CARTESIAN_POINT ( 'NONE',  ( 0.000000000000000000, 0.000000000000000000, 0.000000000000000000 ) ) ;
#55456=CIRCLE ( 'NONE', #32624, 82.00000000000000000 ) ;
#55465=ORIENTED_EDGE ( 'NONE', *, *, #69750, .T. ) ;
#55487=EDGE_CURVE ( 'NONE', #35405, #7122, #48334, .T. ) ;
#55488=DIRECTION ( 'NONE',  ( -1.000000000000000000, 0.000000000000000000, 0.000000000000000000 ) ) ;
#55490=DIRECTION ( 'NONE',  ( 0.000000000000000000, 0.000000000000000000, 1.000000000000000000 ) ) ;
#55491=EDGE_CURVE ( 'NONE', #66220, #42336, #51923, .T. ) ;
#55496=EDGE_CURVE ( 'NONE', #58494, #15358, #66379, .T. ) ;
#55497=ORIENTED_EDGE ( 'NONE', *, *, #50860, .T. ) ;
#55505=DIRECTION ( 'NONE',  ( 0.000000000000000000, 0.000000000000000000, 1.000000000000000000 ) ) ;
#55507=AXIS2_PLACEMENT_3D ( 'NONE', #71961, #54321, #65983 ) ;
#55514=VERTEX_POINT ( 'NONE', #37683 ) ;
#55522=EDGE_CURVE ( 'NONE', #73479, #38213, #49506, .T. ) ;
#55533=DIRECTION ( 'NONE',  ( -1.000000000000000000, 0.000000000000000000, 0.000000000000000000 ) ) ;
#55545=DIRECTION ( 'NONE',  ( 0.000000000000000000, 0.000000000000000000, 1.000000000000000000 ) ) ;
#55565=VERTEX_POINT ( 'NONE', #63215 ) ;
#55567=ORIENTED_EDGE ( 'NONE', *, *, #16014, .F. ) ;
#55571=ADVANCED_FACE ( 'NONE', ( #62857 ), #23713, .T. ) ;
#55578=DIRECTION ( 'NONE',  ( 1.000000000000000000, 0.000000000000000000, 0.000000000000000000 ) ) ;
#55581=ORIENTED_EDGE ( 'NONE', *, *, #27463, .T. ) ;
#55585=EDGE_LOOP ( 'NONE', ( #9350, #46229, #37717, #52271, #38354, #21834 ) ) ;
#55589=DIRECTION ( 'NONE',  ( -1.000000000000000000, -0.000000000000000000, -0.000000000000000000 ) ) ;
#55590=ORIENTED_EDGE ( 'NONE', *, *, #46457, .F. ) ;
#55599=ORIENTED_EDGE ( 'NONE', *, *, #60017, .T. ) ;
#55601=DIRECTION ( 'NONE',  ( 0.000000000000000000, -0.9876883405951394357, 0.1564344650402205716 ) ) ;
#55604=CARTESIAN_POINT ( 'NONE',  ( 10.00000000000000000, -30.41916302227164337, 71.27951684758015460 ) ) ;
#55613=CARTESIAN_POINT ( 'NONE',  ( 5.000000000000002665, 21.60688246758586217, 79.10210256391376049 ) ) ;
#55618=DIRECTION ( 'NONE',  ( -1.000000000000000000, 0.000000000000000000, 0.000000000000000000 ) ) ;
#55620=AXIS2_PLACEMENT_3D ( 'NONE', #62234, #67120, #4355 ) ;
#55636=DIRECTION ( 'NONE',  ( -1.000000000000000000, 0.000000000000000000, 0.000000000000000000 ) ) ;
#55643=CIRCLE ( 'NONE', #22063, 82.00000000000000000 ) ;
#55650=ORIENTED_EDGE ( 'NONE', *, *, #63876, .F. ) ;
#55660=CARTESIAN_POINT ( 'NONE',  ( 0.000000000000000000, -81.34940948281344220, 10.30890764327356557 ) ) ;
#55666=VERTEX_POINT ( 'NONE', #62480 ) ;
#55669=ORIENTED_EDGE ( 'NONE', *, *, #44199, .F. ) ;
#55670=EDGE_CURVE ( 'NONE', #66304, #41093, #30344, .T. ) ;
#55680=ORIENTED_EDGE ( 'NONE', *, *, #65869, .T. ) ;
#55696=AXIS2_PLACEMENT_3D ( 'NONE', #63467, #46911, #70181 ) ;
#55709=DIRECTION ( 'NONE',  ( 0.000000000000000000, 0.9238795325112851842, 0.3826834323650937786 ) ) ;
#55711=DIRECTION ( 'NONE',  ( 0.000000000000000000, 0.000000000000000000, -1.000000000000000000 ) ) ;
#55713=DIRECTION ( 'NONE',  ( -1.000000000000000000, -0.000000000000000000, 0.000000000000000000 ) ) ;
#55719=AXIS2_PLACEMENT_3D ( 'NONE', #67967, #39025, #73964 ) ;
#55732=ORIENTED_EDGE ( 'NONE', *, *, #40981, .T. ) ;
#55736=VECTOR ( 'NONE', #14066, 1000.000000000000000 ) ;
#55737=DIRECTION ( 'NONE',  ( -1.000000000000000000, -0.000000000000000000, -0.000000000000000000 ) ) ;
#55747=VERTEX_POINT ( 'NONE', #65063 ) ;
#55777=ORIENTED_EDGE ( 'NONE', *, *, #37770, .T. ) ;
#55783=EDGE_CURVE ( 'NONE', #52606, #63903, #30450, .T. ) ;
#55784=VECTOR ( 'NONE', #64746, 1000.000000000000000 ) ;
#55794=ORIENTED_EDGE ( 'NONE', *, *, #41363, .F. ) ;
#55797=DIRECTION ( 'NONE',  ( 0.000000000000000000, 0.000000000000000000, 1.000000000000000000 ) ) ;
#55812=DIRECTION ( 'NONE',  ( -1.000000000000000000, 0.000000000000000000, 0.000000000000000000 ) ) ;
#55827=ORIENTED_EDGE ( 'NONE', *, *, #32981, .T. ) ;
#55831=VECTOR ( 'NONE', #32556, 1000.000000000000000 ) ;
#55835=EDGE_CURVE ( 'NONE', #57645, #19199, #32691, .T. ) ;
#55838=AXIS2_PLACEMENT_3D ( 'NONE', #65783, #43608, #14641 ) ;
#55851=ORIENTED_EDGE ( 'NONE', *, *, #126, .T. ) ;
#55856=CIRCLE ( 'NONE', #23455, 31.99999999999999289 ) ;
#55858=DIRECTION ( 'NONE',  ( -1.000000000000000000, -0.000000000000000000, -0.000000000000000000 ) ) ;
#55872=DIRECTION ( 'NONE',  ( -1.000000000000000000, 0.000000000000000000, -0.000000000000000000 ) ) ;
#55878=CARTESIAN_POINT ( 'NONE',  ( 0.000000000000000000, 76.69515212746016175, 29.01471420065591289 ) ) ;
#55882=AXIS2_PLACEMENT_3D ( 'NONE', #40801, #57721, #70085 ) ;
#55896=CARTESIAN_POINT ( 'NONE',  ( 10.00000000000000000, 72.35432306680455383, 20.40083707023012494 ) ) ;
#55900=AXIS2_PLACEMENT_3D ( 'NONE', #28053, #21675, #72429 ) ;
#55901=DIRECTION ( 'NONE',  ( 0.000000000000000000, 0.000000000000000000, -1.000000000000000000 ) ) ;
#55913=CYLINDRICAL_SURFACE ( 'NONE', #22217, 82.00000000000000000 ) ;
#55917=CARTESIAN_POINT ( 'NONE',  ( 10.00000000000000000, 0.000000000000000000, 0.000000000000000000 ) ) ;
#55924=EDGE_LOOP ( 'NONE', ( #33937, #49132, #39350, #55055 ) ) ;
#55931=CIRCLE ( 'NONE', #1984, 31.99999999999999645 ) ;
#55946=ORIENTED_EDGE ( 'NONE', *, *, #73560, .T. ) ;
#55950=FACE_OUTER_BOUND ( 'NONE', #24742, .T. ) ;
#55951=CIRCLE ( 'NONE', #42755, 31.99999999999999289 ) ;
#55954=DIRECTION ( 'NONE',  ( 0.000000000000000000, 0.000000000000000000, 1.000000000000000000 ) ) ;
#55957=ORIENTED_EDGE ( 'NONE', *, *, #33078, .F. ) ;
#55960=DIRECTION ( 'NONE',  ( -1.000000000000000000, 0.000000000000000000, 0.000000000000000000 ) ) ;
#55989=AXIS2_PLACEMENT_3D ( 'NONE', #39898, #74088, #6429 ) ;
#55992=CYLINDRICAL_SURFACE ( 'NONE', #58918, 31.99999999999998579 ) ;
#55998=AXIS2_PLACEMENT_3D ( 'NONE', #56754, #16512, #45477 ) ;
#56003=CARTESIAN_POINT ( 'NONE',  ( 10.00000000000000000, -73.44644590900078640, 24.73286445877676343 ) ) ;
#56009=CIRCLE ( 'NONE', #15165, 32.00000000000000000 ) ;
#56013=CYLINDRICAL_SURFACE ( 'NONE', #19994, 31.99999999999999289 ) ;
#56021=DIRECTION ( 'NONE',  ( 0.000000000000000000, 0.5877852522924742473, -0.8090169943749466741 ) ) ;
#56022=ORIENTED_EDGE ( 'NONE', *, *, #58979, .T. ) ;
#56024=CIRCLE ( 'NONE', #23381, 31.99999999999999289 ) ;
#56030=ADVANCED_FACE ( 'NONE', ( #40190 ), #5252, .T. ) ;
#56033=EDGE_CURVE ( 'NONE', #54897, #35415, #14777, .T. ) ;
#56056=CIRCLE ( 'NONE', #18804, 31.99999999999999289 ) ;
#56058=ORIENTED_EDGE ( 'NONE', *, *, #24124, .F. ) ;
#56061=ORIENTED_EDGE ( 'NONE', *, *, #16385, .F. ) ;
#56072=ORIENTED_EDGE ( 'NONE', *, *, #70260, .T. ) ;
#56073=DIRECTION ( 'NONE',  ( 0.000000000000000000, 0.000000000000000000, -1.000000000000000000 ) ) ;
#56083=CARTESIAN_POINT ( 'NONE',  ( 10.00000000000000000, -26.02418014898260878, -70.52718814184285634 ) ) ;
#56085=CYLINDRICAL_SURFACE ( 'NONE', #7040, 32.00000000000000000 ) ;
#56093=VERTEX_POINT ( 'NONE', #17254 ) ;
#56097=CARTESIAN_POINT ( 'NONE',  ( 0.000000000000000000, 70.52718814184260054, 26.02418014898334420 ) ) ;
#56098=CIRCLE ( 'NONE', #12888, 77.49899999999999523 ) ;
#56100=EDGE_CURVE ( 'NONE', #59929, #9910, #8776, .T. ) ;
#56109=ORIENTED_EDGE ( 'NONE', *, *, #63876, .T. ) ;
#56122=EDGE_LOOP ( 'NONE', ( #21135, #36700, #71027, #45353 ) ) ;
#56131=ORIENTED_EDGE ( 'NONE', *, *, #24802, .T. ) ;
#56132=ORIENTED_EDGE ( 'NONE', *, *, #1342, .T. ) ;
#56138=CARTESIAN_POINT ( 'NONE',  ( 10.00000000000000000, -28.89263327155693517, -71.91182617369219088 ) ) ;
#56151=AXIS2_PLACEMENT_3D ( 'NONE', #7115, #60842, #9324 ) ;
#56153=CARTESIAN_POINT ( 'NONE',  ( 10.00000000000000000, 26.01480285779933510, -70.53064760720289428 ) ) ;
#56160=ORIENTED_EDGE ( 'NONE', *, *, #73405, .T. ) ;
#56174=ADVANCED_FACE ( 'NONE', ( #64975 ), #52942, .T. ) ;
#56176=CARTESIAN_POINT ( 'NONE',  ( 5.000000000000000000, 63.97538442413498672, -51.29473840253155714 ) ) ;
#56185=CIRCLE ( 'NONE', #20151, 31.99999999999999289 ) ;
#56191=ORIENTED_EDGE ( 'NONE', *, *, #72700, .F. ) ;
#56203=DIRECTION ( 'NONE',  ( 0.000000000000000000, 0.000000000000000000, 1.000000000000000000 ) ) ;
#56210=AXIS2_PLACEMENT_3D ( 'NONE', #61446, #32848, #72689 ) ;
#56212=ORIENTED_EDGE ( 'NONE', *, *, #37252, .T. ) ;
#56213=VECTOR ( 'NONE', #3873, 1000.000000000000000 ) ;
#56219=CYLINDRICAL_SURFACE ( 'NONE', #32842, 31.99999999999999289 ) ;
#56225=ORIENTED_EDGE ( 'NONE', *, *, #51618, .T. ) ;
#56232=FACE_OUTER_BOUND ( 'NONE', #45159, .T. ) ;
#56233=DIRECTION ( 'NONE',  ( 0.000000000000000000, 0.000000000000000000, 1.000000000000000000 ) ) ;
#56234=CIRCLE ( 'NONE', #9375, 31.99999999999999289 ) ;
#56241=ORIENTED_EDGE ( 'NONE', *, *, #39247, .T. ) ;
#56245=ORIENTED_EDGE ( 'NONE', *, *, #37157, .T. ) ;
#56252=ORIENTED_EDGE ( 'NONE', *, *, #64698, .F. ) ;
#56258=DIRECTION ( 'NONE',  ( 0.000000000000000000, 0.9969173337331282969, -0.07845909572784179331 ) ) ;
#56272=ADVANCED_FACE ( 'NONE', ( #36752 ), #35281, .T. ) ;
#56282=EDGE_CURVE ( 'NONE', #19205, #3369, #38782, .T. ) ;
#56285=DIRECTION ( 'NONE',  ( -1.000000000000000000, 0.000000000000000000, -0.000000000000000000 ) ) ;
#56287=AXIS2_PLACEMENT_3D ( 'NONE', #62596, #11076, #33998 ) ;
#56290=AXIS2_PLACEMENT_3D ( 'NONE', #30044, #6756, #46985 ) ;
#56333=DIRECTION ( 'NONE',  ( -1.000000000000000000, -0.000000000000000000, 0.000000000000000000 ) ) ;
#56337=CARTESIAN_POINT ( 'NONE',  ( 10.00000000000000000, 46.21855187248719687, -62.20884554313968806 ) ) ;
#56348=VERTEX_POINT ( 'NONE', #15299 ) ;
#56350=CARTESIAN_POINT ( 'NONE',  ( 0.000000000000000000, 0.000000000000000000, 0.000000000000000000 ) ) ;
#56355=AXIS2_PLACEMENT_3D ( 'NONE', #63801, #13007, #53606 ) ;
#56359=ORIENTED_EDGE ( 'NONE', *, *, #54807, .T. ) ;
#56364=EDGE_CURVE ( 'NONE', #26612, #1727, #455, .T. ) ;
#56372=CARTESIAN_POINT ( 'NONE',  ( 0.000000000000000000, -59.03961581697432592, 46.53671651293927880 ) ) ;
#56377=EDGE_CURVE ( 'NONE', #33442, #71294, #56871, .T. ) ;
#56383=CIRCLE ( 'NONE', #64807, 82.00000000000000000 ) ;
#56393=CARTESIAN_POINT ( 'NONE',  ( 10.00000000000000000, 12.93880638057314059, 76.41127070299278046 ) ) ;
#56417=CARTESIAN_POINT ( 'NONE',  ( 10.00000000000000000, -63.97538442413389248, -51.29473840253292138 ) ) ;
#56419=DIRECTION ( 'NONE',  ( -1.000000000000000000, -0.000000000000000000, -0.000000000000000000 ) ) ;
#56422=AXIS2_PLACEMENT_3D ( 'NONE', #54489, #60153, #2292 ) ;
#56446=AXIS2_PLACEMENT_3D ( 'NONE', #5173, #51017, #34456 ) ;
#56448=DIRECTION ( 'NONE',  ( 0.000000000000000000, 0.7071067811865487940, -0.7071067811865463515 ) ) ;
#56477=EDGE_CURVE ( 'NONE', #38312, #70074, #41247, .T. ) ;
#56480=ORIENTED_EDGE ( 'NONE', *, *, #30466, .T. ) ;
#56489=DIRECTION ( 'NONE',  ( 1.000000000000000000, 0.000000000000000000, 0.000000000000000000 ) ) ;
#56491=CARTESIAN_POINT ( 'NONE',  ( 10.00000000000000000, 30.41916302227216562, -71.27951684757994144 ) ) ;
#56493=VERTEX_POINT ( 'NONE', #38987 ) ;
#56496=DIRECTION ( 'NONE',  ( 0.000000000000000000, -0.9969173337331271867, -0.07845909572785568498 ) ) ;
#56500=VERTEX_POINT ( 'NONE', #63405 ) ;
#56501=CARTESIAN_POINT ( 'NONE',  ( 0.000000000000000000, 30.41916302227113178, 71.27951684758036777 ) ) ;
#56502=VERTEX_POINT ( 'NONE', #45756 ) ;
#56504=FACE_OUTER_BOUND ( 'NONE', #1910, .T. ) ;
#56512=EDGE_LOOP ( 'NONE', ( #25532, #24416, #48414, #68658 ) ) ;
#56514=DIRECTION ( 'NONE',  ( 0.000000000000000000, 0.000000000000000000, 1.000000000000000000 ) ) ;
#56523=DIRECTION ( 'NONE',  ( 0.000000000000000000, 0.000000000000000000, 1.000000000000000000 ) ) ;
#56529=LINE ( 'NONE', #38852, #13199 ) ;
#56536=ORIENTED_EDGE ( 'NONE', *, *, #23006, .F. ) ;
#56537=LINE ( 'NONE', #15927, #4704 ) ;
#56550=ORIENTED_EDGE ( 'NONE', *, *, #8000, .F. ) ;
#56558=CARTESIAN_POINT ( 'NONE',  ( 10.00000000000000000, -23.16143007188376757, -73.95703589263997912 ) ) ;
#56562=ORIENTED_EDGE ( 'NONE', *, *, #61728, .F. ) ;
#56564=AXIS2_PLACEMENT_3D ( 'NONE', #37223, #35716, #36101 ) ;
#56573=CIRCLE ( 'NONE', #68592, 31.99999999999999289 ) ;
#56578=DIRECTION ( 'NONE',  ( -1.000000000000000000, 0.000000000000000000, 0.000000000000000000 ) ) ;
#56582=DIRECTION ( 'NONE',  ( -1.000000000000000000, 0.000000000000000000, 0.000000000000000000 ) ) ;
#56587=ORIENTED_EDGE ( 'NONE', *, *, #64946, .T. ) ;
#56590=CIRCLE ( 'NONE', #48208, 31.99999999999999289 ) ;
#56595=ORIENTED_EDGE ( 'NONE', *, *, #6083, .F. ) ;
#56607=ORIENTED_EDGE ( 'NONE', *, *, #71806, .F. ) ;
#56609=LINE ( 'NONE', #73875, #14213 ) ;
#56615=CIRCLE ( 'NONE', #15764, 82.00000000000000000 ) ;
#56616=DIRECTION ( 'NONE',  ( 0.000000000000000000, 0.000000000000000000, 1.000000000000000000 ) ) ;
#56617=ADVANCED_FACE ( 'NONE', ( #69396 ), #1760, .T. ) ;
#56628=ORIENTED_EDGE ( 'NONE', *, *, #36471, .F. ) ;
#56637=DIRECTION ( 'NONE',  ( 1.000000000000000000, 0.000000000000000000, 0.000000000000000000 ) ) ;
#56644=EDGE_CURVE ( 'NONE', #71305, #32419, #29207, .T. ) ;
#56652=( GEOMETRIC_REPRESENTATION_CONTEXT ( 3 ) GLOBAL_UNCERTAINTY_ASSIGNED_CONTEXT ( ( #10600 ) ) GLOBAL_UNIT_ASSIGNED_CONTEXT ( ( #795, #36071, #40988 ) ) REPRESENTATION_CONTEXT ( 'NONE', 'WORKASPACE' ) );
#56654=EDGE_CURVE ( 'NONE', #57624, #47069, #66268, .T. ) ;
#56661=CARTESIAN_POINT ( 'NONE',  ( 10.00000000000000000, -73.73191006444561424, -14.66109333815538918 ) ) ;
#56663=DIRECTION ( 'NONE',  ( -1.000000000000000000, -0.000000000000000000, -0.000000000000000000 ) ) ;
#56664=CARTESIAN_POINT ( 'NONE',  ( 10.00000000000000000, -65.58780272294048075, -36.73666225445966660 ) ) ;
#56683=VERTEX_POINT ( 'NONE', #58122 ) ;
#56684=DIRECTION ( 'NONE',  ( -1.000000000000000000, -0.000000000000000000, -0.000000000000000000 ) ) ;
#56686=LINE ( 'NONE', #33741, #24427 ) ;
#56699=ADVANCED_FACE ( 'NONE', ( #45188 ), #44812, .T. ) ;
#56702=DIRECTION ( 'NONE',  ( 0.000000000000000000, 0.000000000000000000, 1.000000000000000000 ) ) ;
#56708=ORIENTED_EDGE ( 'NONE', *, *, #58886, .F. ) ;
#56712=CARTESIAN_POINT ( 'NONE',  ( 0.000000000000000000, 71.27951684758068041, -30.41916302227035018 ) ) ;
#56716=EDGE_CURVE ( 'NONE', #46506, #58494, #73361, .T. ) ;
#56723=DIRECTION ( 'NONE',  ( -1.000000000000000000, 0.000000000000000000, 0.000000000000000000 ) ) ;
#56727=AXIS2_PLACEMENT_3D ( 'NONE', #60389, #25427, #48349 ) ;
#56742=DIRECTION ( 'NONE',  ( 0.000000000000000000, 0.000000000000000000, 1.000000000000000000 ) ) ;
#56743=CARTESIAN_POINT ( 'NONE',  ( -10.00000000000000000, 0.000000000000000000, 0.000000000000000000 ) ) ;
#56745=EDGE_CURVE ( 'NONE', #53342, #18595, #27878, .T. ) ;
#56748=CARTESIAN_POINT ( 'NONE',  ( 10.00000000000000000, 31.47745569255237896, -68.26794271651228030 ) ) ;
#56751=DIRECTION ( 'NONE',  ( 0.000000000000000000, -0.1564344650402381687, 0.9876883405951365491 ) ) ;
#56753=EDGE_CURVE ( 'NONE', #5465, #38312, #32397, .T. ) ;
#56754=CARTESIAN_POINT ( 'NONE',  ( 10.00000000000000000, 0.000000000000000000, 0.000000000000000000 ) ) ;
#56757=DIRECTION ( 'NONE',  ( -1.000000000000000000, 0.000000000000000000, 0.000000000000000000 ) ) ;
#56772=ORIENTED_EDGE ( 'NONE', *, *, #21288, .T. ) ;
#56785=DIRECTION ( 'NONE',  ( 0.000000000000000000, 0.000000000000000000, 1.000000000000000000 ) ) ;
#56789=EDGE_CURVE ( 'NONE', #60775, #17276, #55341, .T. ) ;
#56800=CARTESIAN_POINT ( 'NONE',  ( 0.000000000000000000, 0.000000000000000000, 0.000000000000000000 ) ) ;
#56804=ORIENTED_EDGE ( 'NONE', *, *, #21105, .F. ) ;
#56810=VERTEX_POINT ( 'NONE', #72981 ) ;
#56813=ORIENTED_EDGE ( 'NONE', *, *, #34273, .F. ) ;
#56820=LINE ( 'NONE', #33874, #40483 ) ;
#56824=AXIS2_PLACEMENT_3D ( 'NONE', #69486, #17984, #63866 ) ;
#56836=CARTESIAN_POINT ( 'NONE',  ( 0.000000000000000000, 58.39081064771751528, 50.95692526931350841 ) ) ;
#56837=DIRECTION ( 'NONE',  ( 0.000000000000000000, 0.000000000000000000, 1.000000000000000000 ) ) ;
#56846=CARTESIAN_POINT ( 'NONE',  ( 0.000000000000000000, -67.80270845531855173, -46.11716303203261447 ) ) ;
#56854=FACE_OUTER_BOUND ( 'NONE', #68904, .T. ) ;
#56867=CIRCLE ( 'NONE', #41243, 31.99999999999998934 ) ;
#56871=CIRCLE ( 'NONE', #48427, 77.49900000000000944 ) ;
#56873=EDGE_CURVE ( 'NONE', #73588, #21230, #27121, .T. ) ;
#56874=ORIENTED_EDGE ( 'NONE', *, *, #4066, .F. ) ;
#56876=CARTESIAN_POINT ( 'NONE',  ( 0.000000000000000000, 51.02545421589402252, -55.20638768913705263 ) ) ;
#56879=ORIENTED_EDGE ( 'NONE', *, *, #16519, .F. ) ;
#56881=DIRECTION ( 'NONE',  ( 1.000000000000000000, -0.000000000000000000, -0.000000000000000000 ) ) ;
#56883=CARTESIAN_POINT ( 'NONE',  ( 0.000000000000000000, -81.34940948281328588, -10.30890764327469711 ) ) ;
#56896=DIRECTION ( 'NONE',  ( -1.000000000000000000, -0.000000000000000000, -0.000000000000000000 ) ) ;
#56916=VERTEX_POINT ( 'NONE', #56836 ) ;
#56925=AXIS2_PLACEMENT_3D ( 'NONE', #34956, #34210, #6393 ) ;
#56928=AXIS2_PLACEMENT_3D ( 'NONE', #50917, #67471, #74218 ) ;
#56954=EDGE_LOOP ( 'NONE', ( #10020, #18651, #49444, #11885 ) ) ;
#56967=CARTESIAN_POINT ( 'NONE',  ( 0.000000000000000000, 16.00000000000000000, 2.500000000000000000 ) ) ;
#56974=ORIENTED_EDGE ( 'NONE', *, *, #61650, .T. ) ;
#56975=AXIS2_PLACEMENT_3D ( 'NONE', #71514, #53867, #37332 ) ;
#56979=CARTESIAN_POINT ( 'NONE',  ( 10.00000000000000000, 67.80270845531889279, 46.11716303203210998 ) ) ;
#56981=DIRECTION ( 'NONE',  ( 0.000000000000000000, 0.07845909572783793529, 0.9969173337331285190 ) ) ;
#56988=ORIENTED_EDGE ( 'NONE', *, *, #71030, .F. ) ;
#56995=ADVANCED_FACE ( 'NONE', ( #45565 ), #57580, .T. ) ;
#56998=CARTESIAN_POINT ( 'NONE',  ( 0.000000000000000000, 0.000000000000000000, 0.000000000000000000 ) ) ;
#57005=CARTESIAN_POINT ( 'NONE',  ( 10.00000000000000000, 5.256550761632864166, 77.32052557432842832 ) ) ;
#57016=AXIS2_PLACEMENT_3D ( 'NONE', #29212, #13407, #29952 ) ;
#57019=CARTESIAN_POINT ( 'NONE',  ( 10.00000000000000000, 22.90783923731741112, -78.73519480814930205 ) ) ;
#57024=DIRECTION ( 'NONE',  ( 0.000000000000000000, 0.000000000000000000, 1.000000000000000000 ) ) ;
#57025=DIRECTION ( 'NONE',  ( 0.000000000000000000, 0.000000000000000000, 1.000000000000000000 ) ) ;
#57031=ORIENTED_EDGE ( 'NONE', *, *, #74193, .T. ) ;
#57038=ADVANCED_FACE ( 'NONE', ( #41385 ), #19187, .T. ) ;
#57057=EDGE_CURVE ( 'NONE', #55291, #50178, #7705, .T. ) ;
#57060=ORIENTED_EDGE ( 'NONE', *, *, #27160, .T. ) ;
#57066=CIRCLE ( 'NONE', #45041, 31.99999999999999289 ) ;
#57073=CYLINDRICAL_SURFACE ( 'NONE', #28740, 31.99999999999998579 ) ;
#57084=DIRECTION ( 'NONE',  ( -1.000000000000000000, 0.000000000000000000, 0.000000000000000000 ) ) ;
#57102=VERTEX_POINT ( 'NONE', #7177 ) ;
#57106=DIRECTION ( 'NONE',  ( 0.000000000000000000, 0.000000000000000000, 1.000000000000000000 ) ) ;
#57112=DIRECTION ( 'NONE',  ( -1.000000000000000000, 0.000000000000000000, 0.000000000000000000 ) ) ;
#57113=CYLINDRICAL_SURFACE ( 'NONE', #70990, 31.99999999999999289 ) ;
#57115=DIRECTION ( 'NONE',  ( 0.000000000000000000, 0.000000000000000000, 1.000000000000000000 ) ) ;
#57118=CARTESIAN_POINT ( 'NONE',  ( -10.00000000000000000, 0.000000000000000000, 0.000000000000000000 ) ) ;
#57121=CYLINDRICAL_SURFACE ( 'NONE', #64989, 82.00000000000000000 ) ;
#57123=CARTESIAN_POINT ( 'NONE',  ( 10.00000000000000000, -34.94270380257586339, -74.18225833017926618 ) ) ;
#57128=ORIENTED_EDGE ( 'NONE', *, *, #7966, .T. ) ;
#57129=DIRECTION ( 'NONE',  ( -1.000000000000000000, 0.000000000000000000, 0.000000000000000000 ) ) ;
#57135=VECTOR ( 'NONE', #39225, 1000.000000000000000 ) ;
#57140=CARTESIAN_POINT ( 'NONE',  ( 10.00000000000000000, -74.65491531819124305, 8.830959090342128448 ) ) ;
#57166=CARTESIAN_POINT ( 'NONE',  ( 5.000000000000000000, 44.99326035066149387, -68.55367621811095091 ) ) ;
#57170=VERTEX_POINT ( 'NONE', #66901 ) ;
#57173=ORIENTED_EDGE ( 'NONE', *, *, #38648, .T. ) ;
#57190=DIRECTION ( 'NONE',  ( 0.000000000000000000, 0.8910065241883690090, -0.4539904997395446395 ) ) ;
#57198=LINE ( 'NONE', #52656, #41034 ) ;
#57205=DIRECTION ( 'NONE',  ( 1.000000000000000000, -0.000000000000000000, -0.000000000000000000 ) ) ;
#57208=DIRECTION ( 'NONE',  ( 0.000000000000000000, 0.000000000000000000, 1.000000000000000000 ) ) ;
#57222=VERTEX_POINT ( 'NONE', #43259 ) ;
#57224=CARTESIAN_POINT ( 'NONE',  ( 10.00000000000000000, -2.543863470248951320, 81.96053171279901051 ) ) ;
#57228=AXIS2_PLACEMENT_3D ( 'NONE', #1557, #8640, #42848 ) ;
#57238=CIRCLE ( 'NONE', #68073, 77.49899999999999523 ) ;
#57240=ORIENTED_EDGE ( 'NONE', *, *, #16311, .F. ) ;
#57248=DIRECTION ( 'NONE',  ( 0.000000000000000000, 0.9238795325112878487, -0.3826834323650874503 ) ) ;
#57251=ORIENTED_EDGE ( 'NONE', *, *, #39885, .T. ) ;
#57272=CARTESIAN_POINT ( 'NONE',  ( 5.000000000000002665, 80.28980883073781172, -16.65972982744850839 ) ) ;
#57279=ORIENTED_EDGE ( 'NONE', *, *, #11347, .F. ) ;
#57284=CYLINDRICAL_SURFACE ( 'NONE', #20515, 31.99999999999999289 ) ;
#57314=VECTOR ( 'NONE', #48089, 1000.000000000000000 ) ;
#57325=VERTEX_POINT ( 'NONE', #40199 ) ;
#57346=ORIENTED_EDGE ( 'NONE', *, *, #42219, .F. ) ;
#57358=EDGE_CURVE ( 'NONE', #23124, #15280, #34542, .T. ) ;
#57360=CARTESIAN_POINT ( 'NONE',  ( 10.00000000000000000, -20.40083707022935400, 72.35432306680478121 ) ) ;
#57365=ORIENTED_EDGE ( 'NONE', *, *, #10343, .F. ) ;
#57367=ORIENTED_EDGE ( 'NONE', *, *, #19229, .T. ) ;
#57369=VECTOR ( 'NONE', #38796, 1000.000000000000000 ) ;
#57379=DIRECTION ( 'NONE',  ( -1.000000000000000000, -0.000000000000000000, 0.000000000000000000 ) ) ;
#57382=DIRECTION ( 'NONE',  ( 0.000000000000000000, 0.6494480483301793283, 0.7604059656000345946 ) ) ;
#57384=DIRECTION ( 'NONE',  ( -1.000000000000000000, -0.000000000000000000, -0.000000000000000000 ) ) ;
#57394=EDGE_LOOP ( 'NONE', ( #5652, #62123, #41690, #47045 ) ) ;
#57397=CIRCLE ( 'NONE', #56210, 82.00000000000000000 ) ;
#57414=CIRCLE ( 'NONE', #63435, 82.00000000000000000 ) ;
#57417=CARTESIAN_POINT ( 'NONE',  ( 10.00000000000000000, 74.74816331893477184, -33.71516098798658589 ) ) ;
#57430=CYLINDRICAL_SURFACE ( 'NONE', #49691, 82.00000000000000000 ) ;
#57431=CARTESIAN_POINT ( 'NONE',  ( 0.000000000000000000, 0.000000000000000000, 0.000000000000000000 ) ) ;
#57434=EDGE_LOOP ( 'NONE', ( #35396, #35128, #12766, #34807 ) ) ;
#57442=AXIS2_PLACEMENT_3D ( 'NONE', #70909, #43107, #14130 ) ;
#57450=CARTESIAN_POINT ( 'NONE',  ( 10.00000000000000000, 73.73191006444572793, -14.66109333815486515 ) ) ;
#57456=AXIS2_PLACEMENT_3D ( 'NONE', #32036, #49696, #26408 ) ;
#57460=VERTEX_POINT ( 'NONE', #3239 ) ;
#57462=DIRECTION ( 'NONE',  ( 0.000000000000000000, 0.5224985647159441360, 0.8526401643540952868 ) ) ;
#57466=CARTESIAN_POINT ( 'NONE',  ( 5.000000000000002665, -81.50828551894220197, -8.966570791701590437 ) ) ;
#57470=EDGE_CURVE ( 'NONE', #36758, #1076, #14944, .T. ) ;
#57472=EDGE_CURVE ( 'NONE', #16471, #32358, #43785, .T. ) ;
#57482=CYLINDRICAL_SURFACE ( 'NONE', #51220, 31.99999999999999289 ) ;
#57483=FACE_OUTER_BOUND ( 'NONE', #61162, .T. ) ;
#57485=EDGE_CURVE ( 'NONE', #31772, #59828, #20863, .T. ) ;
#57494=EDGE_CURVE ( 'NONE', #17127, #13140, #12527, .T. ) ;
#57496=ADVANCED_FACE ( 'NONE', ( #48696 ), #71620, .T. ) ;
#57503=CARTESIAN_POINT ( 'NONE',  ( 10.00000000000000000, 0.000000000000000000, 0.000000000000000000 ) ) ;
#57512=CARTESIAN_POINT ( 'NONE',  ( 0.000000000000000000, 0.8261519478431083030, 77.49459641780886443 ) ) ;
#57521=CIRCLE ( 'NONE', #22750, 77.49899999999999523 ) ;
#57522=CIRCLE ( 'NONE', #19080, 31.99999999999999645 ) ;
#57532=EDGE_LOOP ( 'NONE', ( #24166, #27905, #15934, #26727 ) ) ;
#57538=EDGE_LOOP ( 'NONE', ( #48255, #43229, #14625, #59481 ) ) ;
#57548=AXIS2_PLACEMENT_3D ( 'NONE', #44785, #73329, #33474 ) ;
#57556=VECTOR ( 'NONE', #10944, 1000.000000000000000 ) ;
#57559=DIRECTION ( 'NONE',  ( 0.000000000000000000, 0.000000000000000000, -1.000000000000000000 ) ) ;
#57561=CIRCLE ( 'NONE', #16708, 77.49900000000000944 ) ;
#57564=AXIS2_PLACEMENT_3D ( 'NONE', #37417, #59981, #49039 ) ;
#57575=ORIENTED_EDGE ( 'NONE', *, *, #17563, .T. ) ;
#57580=CYLINDRICAL_SURFACE ( 'NONE', #44910, 82.00000000000000000 ) ;
#57590=CARTESIAN_POINT ( 'NONE',  ( 10.00000000000000000, 0.000000000000000000, 0.000000000000000000 ) ) ;
#57593=ORIENTED_EDGE ( 'NONE', *, *, #15187, .F. ) ;
#57597=EDGE_CURVE ( 'NONE', #25432, #64863, #25734, .T. ) ;
#57608=AXIS2_PLACEMENT_3D ( 'NONE', #43728, #56489, #66648 ) ;
#57609=DIRECTION ( 'NONE',  ( -1.000000000000000000, 0.000000000000000000, 0.000000000000000000 ) ) ;
#57613=VERTEX_POINT ( 'NONE', #74220 ) ;
#57617=ORIENTED_EDGE ( 'NONE', *, *, #12947, .F. ) ;
#57622=VERTEX_POINT ( 'NONE', #16339 ) ;
#57624=VERTEX_POINT ( 'NONE', #62212 ) ;
#57626=ORIENTED_EDGE ( 'NONE', *, *, #68184, .T. ) ;
#57637=CARTESIAN_POINT ( 'NONE',  ( 10.00000000000000000, -51.03279382321125723, 55.19960302592048862 ) ) ;
#57639=CYLINDRICAL_SURFACE ( 'NONE', #21602, 82.00000000000000000 ) ;
#57645=VERTEX_POINT ( 'NONE', #51665 ) ;
#57657=ORIENTED_EDGE ( 'NONE', *, *, #13428, .T. ) ;
#57666=AXIS2_PLACEMENT_3D ( 'NONE', #1789, #32798, #24672 ) ;
#57667=ORIENTED_EDGE ( 'NONE', *, *, #5936, .T. ) ;
#57677=CARTESIAN_POINT ( 'NONE',  ( 10.00000000000000000, 34.44570377933695227, -69.42325613327405165 ) ) ;
#57695=DIRECTION ( 'NONE',  ( 0.000000000000000000, 0.000000000000000000, 1.000000000000000000 ) ) ;
#57709=ORIENTED_EDGE ( 'NONE', *, *, #56364, .F. ) ;
#57710=CIRCLE ( 'NONE', #13269, 77.49899999999999523 ) ;
#57713=ORIENTED_EDGE ( 'NONE', *, *, #42771, .T. ) ;
#57714=CARTESIAN_POINT ( 'NONE',  ( 10.00000000000000178, 12.24744871391589029, 2.499999999999999556 ) ) ;
#57717=CARTESIAN_POINT ( 'NONE',  ( 10.00000000000000000, 76.41127070299273782, 12.93880638057342836 ) ) ;
#57719=CARTESIAN_POINT ( 'NONE',  ( 0.000000000000000000, 17.28742895386190526, -75.54627589209924565 ) ) ;
#57721=DIRECTION ( 'NONE',  ( -1.000000000000000000, 0.000000000000000000, -0.000000000000000000 ) ) ;
#57723=DIRECTION ( 'NONE',  ( 1.000000000000000000, 0.000000000000000000, 0.000000000000000000 ) ) ;
#57732=EDGE_CURVE ( 'NONE', #57170, #46225, #29365, .T. ) ;
#57736=CARTESIAN_POINT ( 'NONE',  ( 10.00000000000000000, -70.53064760720297954, -26.01480285779911839 ) ) ;
#57737=CARTESIAN_POINT ( 'NONE',  ( 10.00000000000000000, -73.44644590900043113, -24.73286445877782924 ) ) ;
#57745=AXIS2_PLACEMENT_3D ( 'NONE', #10497, #2413, #26026 ) ;
#57748=CARTESIAN_POINT ( 'NONE',  ( 0.000000000000000000, -77.49459641780886443, -0.8261519478439277586 ) ) ;
#57752=ORIENTED_EDGE ( 'NONE', *, *, #662, .T. ) ;
#57754=EDGE_CURVE ( 'NONE', #5647, #30680, #71381, .T. ) ;
#57760=CYLINDRICAL_SURFACE ( 'NONE', #55285, 82.00000000000000000 ) ;
#57776=FACE_OUTER_BOUND ( 'NONE', #58560, .T. ) ;
#57781=DIRECTION ( 'NONE',  ( 0.000000000000000000, 0.000000000000000000, 1.000000000000000000 ) ) ;
#57793=CARTESIAN_POINT ( 'NONE',  ( 0.000000000000000000, -71.21200624218768382, -40.65526001592689909 ) ) ;
#57797=EDGE_CURVE ( 'NONE', #18834, #1870, #58043, .T. ) ;
#57804=EDGE_CURVE ( 'NONE', #32364, #49560, #23833, .T. ) ;
#57813=ORIENTED_EDGE ( 'NONE', *, *, #25484, .F. ) ;
#57824=CARTESIAN_POINT ( 'NONE',  ( 5.000000000000000000, -33.71516098798792171, 74.74816331893418919 ) ) ;
#57826=LINE ( 'NONE', #45443, #43522 ) ;
#57827=VECTOR ( 'NONE', #53124, 1000.000000000000000 ) ;
#57829=ORIENTED_EDGE ( 'NONE', *, *, #65449, .T. ) ;
#57832=DIRECTION ( 'NONE',  ( -1.000000000000000000, 0.000000000000000000, 0.000000000000000000 ) ) ;
#57833=EDGE_CURVE ( 'NONE', #56093, #45747, #25678, .T. ) ;
#57845=VERTEX_POINT ( 'NONE', #15128 ) ;
#57850=DIRECTION ( 'NONE',  ( -1.000000000000000000, 0.000000000000000000, -0.000000000000000000 ) ) ;
#57851=AXIS2_PLACEMENT_3D ( 'NONE', #68596, #17083, #5815 ) ;
#57854=CARTESIAN_POINT ( 'NONE',  ( 10.00000000000000000, 70.52718814184294160, -26.02418014898236720 ) ) ;
#57858=CARTESIAN_POINT ( 'NONE',  ( 10.00000000000000000, 51.02545421589402252, -55.20638768913705263 ) ) ;
#57873=AXIS2_PLACEMENT_3D ( 'NONE', #32758, #50435, #55709 ) ;
#57876=ORIENTED_EDGE ( 'NONE', *, *, #15871, .F. ) ;
#57891=VECTOR ( 'NONE', #32615, 1000.000000000000000 ) ;
#57903=DIRECTION ( 'NONE',  ( 0.000000000000000000, -0.7604059656000368150, 0.6494480483301767748 ) ) ;
#57907=FILL_AREA_STYLE_COLOUR ( '', #25448 ) ;
#57911=VERTEX_POINT ( 'NONE', #61381 ) ;
#57915=CARTESIAN_POINT ( 'NONE',  ( 0.000000000000000000, -76.69515212746036070, 29.01471420065537643 ) ) ;
#57923=ORIENTED_EDGE ( 'NONE', *, *, #2588, .F. ) ;
#57924=ADVANCED_FACE ( 'NONE', ( #36959 ), #59908, .T. ) ;
#57929=DIRECTION ( 'NONE',  ( 0.000000000000000000, 0.3090169943749411785, 0.9510565162951556406 ) ) ;
#57932=CARTESIAN_POINT ( 'NONE',  ( 0.000000000000000000, 0.000000000000000000, 0.000000000000000000 ) ) ;
#57937=DIRECTION ( 'NONE',  ( -1.000000000000000000, 0.000000000000000000, 0.000000000000000000 ) ) ;
#57942=CIRCLE ( 'NONE', #61585, 32.00000000000000000 ) ;
#57947=CARTESIAN_POINT ( 'NONE',  ( 0.000000000000000000, -55.20638768913724448, -51.02545421589383068 ) ) ;
#57954=DIRECTION ( 'NONE',  ( 1.000000000000000000, 0.000000000000000000, -0.000000000000000000 ) ) ;
#57967=EDGE_CURVE ( 'NONE', #54604, #37783, #23437, .T. ) ;
#57973=CIRCLE ( 'NONE', #48359, 77.49899999999999523 ) ;
#57978=VERTEX_POINT ( 'NONE', #44830 ) ;
#57980=EDGE_CURVE ( 'NONE', #68833, #32793, #68123, .T. ) ;
#57984=EDGE_CURVE ( 'NONE', #2989, #68435, #38999, .T. ) ;
#57987=AXIS2_PLACEMENT_3D ( 'NONE', #7715, #65239, #13713 ) ;
#57988=VERTEX_POINT ( 'NONE', #68505 ) ;
#58003=ORIENTED_EDGE ( 'NONE', *, *, #30950, .T. ) ;
#58022=DIRECTION ( 'NONE',  ( 0.000000000000000000, -0.9238795325112822976, -0.3826834323651008285 ) ) ;
#58028=CARTESIAN_POINT ( 'NONE',  ( 0.000000000000000000, 30.41916302227216562, -71.27951684757994144 ) ) ;
#58029=DIRECTION ( 'NONE',  ( -1.000000000000000000, 0.000000000000000000, 0.000000000000000000 ) ) ;
#58039=DIRECTION ( 'NONE',  ( 0.000000000000000000, 0.000000000000000000, 1.000000000000000000 ) ) ;
#58040=ORIENTED_EDGE ( 'NONE', *, *, #35725, .F. ) ;
#58043=LINE ( 'NONE', #52394, #30597 ) ;
#58045=AXIS2_PLACEMENT_3D ( 'NONE', #8275, #1211, #23720 ) ;
#58046=AXIS2_PLACEMENT_3D ( 'NONE', #11156, #4799, #33707 ) ;
#58047=EDGE_CURVE ( 'NONE', #10469, #17740, #4228, .T. ) ;
#58056=CARTESIAN_POINT ( 'NONE',  ( 5.000000000000002665, 81.90746397400393164, -3.894527615416986333 ) ) ;
#58063=FACE_OUTER_BOUND ( 'NONE', #62808, .T. ) ;
#58065=CIRCLE ( 'NONE', #4099, 31.99999999999998934 ) ;
#58078=EDGE_CURVE ( 'NONE', #28208, #65655, #60627, .T. ) ;
#58079=CIRCLE ( 'NONE', #30423, 31.99999999999998934 ) ;
#58086=DIRECTION ( 'NONE',  ( 0.000000000000000000, 0.000000000000000000, 1.000000000000000000 ) ) ;
#58087=ORIENTED_EDGE ( 'NONE', *, *, #61211, .F. ) ;
#58092=ORIENTED_EDGE ( 'NONE', *, *, #27744, .T. ) ;
#58112=DIRECTION ( 'NONE',  ( 1.000000000000000000, 0.000000000000000000, 0.000000000000000000 ) ) ;
#58122=CARTESIAN_POINT ( 'NONE',  ( 0.000000000000000000, 15.33399622253481986, 80.55351364060595643 ) ) ;
#58134=ADVANCED_FACE ( 'NONE', ( #48786 ), #47682, .T. ) ;
#58135=EDGE_CURVE ( 'NONE', #7305, #2169, #25127, .T. ) ;
#58140=VECTOR ( 'NONE', #57954, 1000.000000000000000 ) ;
#58142=ORIENTED_EDGE ( 'NONE', *, *, #14072, .F. ) ;
#58143=CARTESIAN_POINT ( 'NONE',  ( 0.000000000000000000, -51.02545421589363883, 55.20638768913742922 ) ) ;
#58145=CARTESIAN_POINT ( 'NONE',  ( 10.00000000000000000, 71.87247863392413194, 39.47590169984869135 ) ) ;
#58154=DIRECTION ( 'NONE',  ( 0.000000000000000000, 0.000000000000000000, -1.000000000000000000 ) ) ;
#58170=VERTEX_POINT ( 'NONE', #31492 ) ;
#58172=VERTEX_POINT ( 'NONE', #54435 ) ;
#58173=DIRECTION ( 'NONE',  ( -1.000000000000000000, 0.000000000000000000, 0.000000000000000000 ) ) ;
#58196=CYLINDRICAL_SURFACE ( 'NONE', #23104, 31.99999999999998579 ) ;
#58211=LINE ( 'NONE', #380, #38714 ) ;
#58216=FACE_OUTER_BOUND ( 'NONE', #39697, .T. ) ;
#58232=AXIS2_PLACEMENT_3D ( 'NONE', #61134, #9625, #56616 ) ;
#58234=EDGE_LOOP ( 'NONE', ( #49153, #36502, #73237, #32648 ) ) ;
#58239=ORIENTED_EDGE ( 'NONE', *, *, #56654, .T. ) ;
#58244=VECTOR ( 'NONE', #20551, 1000.000000000000000 ) ;
#58255=ORIENTED_EDGE ( 'NONE', *, *, #63338, .F. ) ;
#58264=AXIS2_PLACEMENT_3D ( 'NONE', #57360, #22406, #28782 ) ;
#58272=VERTEX_POINT ( 'NONE', #67197 ) ;
#58273=ORIENTED_EDGE ( 'NONE', *, *, #1342, .F. ) ;
#58281=CARTESIAN_POINT ( 'NONE',  ( 0.000000000000000000, 0.000000000000000000, 0.000000000000000000 ) ) ;
#58285=ORIENTED_EDGE ( 'NONE', *, *, #25206, .T. ) ;
#58286=CARTESIAN_POINT ( 'NONE',  ( 0.000000000000000000, 0.000000000000000000, 0.000000000000000000 ) ) ;
#58292=AXIS2_PLACEMENT_3D ( 'NONE', #44503, #62158, #32820 ) ;
#58300=DIRECTION ( 'NONE',  ( -1.000000000000000000, -0.000000000000000000, -0.000000000000000000 ) ) ;
#58305=EDGE_CURVE ( 'NONE', #32358, #52599, #32969, .T. ) ;
#58313=CYLINDRICAL_SURFACE ( 'NONE', #2610, 31.99999999999999289 ) ;
#58328=ORIENTED_EDGE ( 'NONE', *, *, #16720, .T. ) ;
#58332=ORIENTED_EDGE ( 'NONE', *, *, #26142, .F. ) ;
#58341=ORIENTED_EDGE ( 'NONE', *, *, #53378, .F. ) ;
#58343=DIRECTION ( 'NONE',  ( 0.000000000000000000, -0.8090169943749402348, -0.5877852522924830181 ) ) ;
#58369=CYLINDRICAL_SURFACE ( 'NONE', #15517, 82.00000000000000000 ) ;
#58398=CARTESIAN_POINT ( 'NONE',  ( 10.00000000000000000, 0.000000000000000000, 0.000000000000000000 ) ) ;
#58414=EDGE_LOOP ( 'NONE', ( #28928, #25387, #52248, #40823 ) ) ;
#58428=ORIENTED_EDGE ( 'NONE', *, *, #72713, .T. ) ;
#58439=DIRECTION ( 'NONE',  ( 0.000000000000000000, 0.000000000000000000, 1.000000000000000000 ) ) ;
#58460=CYLINDRICAL_SURFACE ( 'NONE', #70215, 31.99999999999999289 ) ;
#58463=LINE ( 'NONE', #30994, #15603 ) ;
#58480=DIRECTION ( 'NONE',  ( 1.000000000000000000, 0.000000000000000000, 0.000000000000000000 ) ) ;
#58485=CYLINDRICAL_SURFACE ( 'NONE', #4917, 77.49899999999999523 ) ;
#58493=FACE_OUTER_BOUND ( 'NONE', #25736, .T. ) ;
#58494=VERTEX_POINT ( 'NONE', #17543 ) ;
#58498=ADVANCED_FACE ( 'NONE', ( #57776 ), #5176, .T. ) ;
#58503=VERTEX_POINT ( 'NONE', #34841 ) ;
#58511=ORIENTED_EDGE ( 'NONE', *, *, #45139, .T. ) ;
#58512=VECTOR ( 'NONE', #55438, 1000.000000000000000 ) ;
#58513=ORIENTED_EDGE ( 'NONE', *, *, #64352, .T. ) ;
#58522=ORIENTED_EDGE ( 'NONE', *, *, #25151, .T. ) ;
#58537=DIRECTION ( 'NONE',  ( 0.000000000000000000, 0.000000000000000000, 1.000000000000000000 ) ) ;
#58550=EDGE_LOOP ( 'NONE', ( #5606, #57617, #47443, #25314 ) ) ;
#58560=EDGE_LOOP ( 'NONE', ( #70231, #42804, #22550, #22204 ) ) ;
#58567=AXIS2_PLACEMENT_3D ( 'NONE', #24998, #41928, #14077 ) ;
#58569=EDGE_CURVE ( 'NONE', #19761, #11722, #1884, .T. ) ;
#58586=VECTOR ( 'NONE', #34111, 1000.000000000000000 ) ;
#58587=AXIS2_PLACEMENT_3D ( 'NONE', #51763, #311, #62356 ) ;
#58588=CIRCLE ( 'NONE', #1005, 32.00000000000000711 ) ;
#58589=VECTOR ( 'NONE', #63689, 1000.000000000000000 ) ;
#58594=DIRECTION ( 'NONE',  ( -1.000000000000000000, 0.000000000000000000, -0.000000000000000000 ) ) ;
#58600=FACE_OUTER_BOUND ( 'NONE', #40396, .T. ) ;
#58601=ORIENTED_EDGE ( 'NONE', *, *, #4932, .F. ) ;
#58608=CIRCLE ( 'NONE', #14175, 31.99999999999999289 ) ;
#58609=ORIENTED_EDGE ( 'NONE', *, *, #18248, .T. ) ;
#58610=DIRECTION ( 'NONE',  ( 0.000000000000000000, 0.000000000000000000, 1.000000000000000000 ) ) ;
#58612=VERTEX_POINT ( 'NONE', #56979 ) ;
#58616=CIRCLE ( 'NONE', #55024, 31.99999999999999645 ) ;
#58631=ORIENTED_EDGE ( 'NONE', *, *, #62785, .T. ) ;
#58634=CARTESIAN_POINT ( 'NONE',  ( 10.00000000000000000, -78.73519480814971416, 22.90783923731600069 ) ) ;
#58637=ORIENTED_EDGE ( 'NONE', *, *, #42465, .F. ) ;
#58655=ORIENTED_EDGE ( 'NONE', *, *, #53060, .F. ) ;
#58656=DIRECTION ( 'NONE',  ( -1.000000000000000000, -0.000000000000000000, 0.000000000000000000 ) ) ;
#58663=DIRECTION ( 'NONE',  ( -1.000000000000000000, -0.000000000000000000, -0.000000000000000000 ) ) ;
#58677=EDGE_CURVE ( 'NONE', #42699, #24045, #10326, .T. ) ;
#58679=CARTESIAN_POINT ( 'NONE',  ( 0.000000000000000000, -17.28742895386031719, -75.54627589209962935 ) ) ;
#58680=CIRCLE ( 'NONE', #26244, 82.00000000000000000 ) ;
#58687=CARTESIAN_POINT ( 'NONE',  ( 10.00000000000000000, 0.000000000000000000, 0.000000000000000000 ) ) ;
#58693=AXIS2_PLACEMENT_3D ( 'NONE', #48166, #71075, #42904 ) ;
#58700=AXIS2_PLACEMENT_3D ( 'NONE', #15972, #43085, #55081 ) ;
#58715=CYLINDRICAL_SURFACE ( 'NONE', #34415, 31.99999999999998579 ) ;
#58719=DIRECTION ( 'NONE',  ( 0.000000000000000000, 0.000000000000000000, 1.000000000000000000 ) ) ;
#58734=AXIS2_PLACEMENT_3D ( 'NONE', #24373, #7452, #29619 ) ;
#58737=ADVANCED_FACE ( 'NONE', ( #34778 ), #46428, .T. ) ;
#58738=CIRCLE ( 'NONE', #14293, 77.49900000000002365 ) ;
#58739=CARTESIAN_POINT ( 'NONE',  ( 0.000000000000000000, 0.000000000000000000, 0.000000000000000000 ) ) ;
#58749=EDGE_CURVE ( 'NONE', #21235, #2959, #47171, .T. ) ;
#58751=LINE ( 'NONE', #24172, #36718 ) ;
#58772=CARTESIAN_POINT ( 'NONE',  ( 0.000000000000000000, 72.35160999960817207, 20.41045688087850607 ) ) ;
#58776=DIRECTION ( 'NONE',  ( -1.000000000000000000, -0.000000000000000000, 0.000000000000000000 ) ) ;
#58778=DIRECTION ( 'NONE',  ( 0.000000000000000000, 0.000000000000000000, 1.000000000000000000 ) ) ;
#58788=DIRECTION ( 'NONE',  ( -1.000000000000000000, -0.000000000000000000, -0.000000000000000000 ) ) ;
#58789=VECTOR ( 'NONE', #59123, 1000.000000000000000 ) ;
#58794=ORIENTED_EDGE ( 'NONE', *, *, #43975, .F. ) ;
#58807=ORIENTED_EDGE ( 'NONE', *, *, #61781, .F. ) ;
#58814=CARTESIAN_POINT ( 'NONE',  ( 0.000000000000000000, -66.50666863321971789, -39.78640506895676054 ) ) ;
#58817=EDGE_CURVE ( 'NONE', #2983, #23472, #27105, .T. ) ;
#58821=CARTESIAN_POINT ( 'NONE',  ( 0.000000000000000000, 46.21855187248719687, -62.20884554313968806 ) ) ;
#58825=CARTESIAN_POINT ( 'NONE',  ( 10.00000000000000000, -55.16347631942997509, -60.67117009219195722 ) ) ;
#58841=CARTESIAN_POINT ( 'NONE',  ( 5.000000000000000000, 50.23322058963348979, 64.81221759200361987 ) ) ;
#58844=AXIS2_PLACEMENT_3D ( 'NONE', #11413, #26850, #62189 ) ;
#58847=FACE_OUTER_BOUND ( 'NONE', #3707, .T. ) ;
#58848=CYLINDRICAL_SURFACE ( 'NONE', #55198, 82.00000000000000000 ) ;
#58849=ORIENTED_EDGE ( 'NONE', *, *, #42612, .F. ) ;
#58852=EDGE_CURVE ( 'NONE', #14528, #37162, #30708, .T. ) ;
#58853=CARTESIAN_POINT ( 'NONE',  ( 10.00000000000000000, 65.58780272294076497, 36.73666225445916211 ) ) ;
#58854=DIRECTION ( 'NONE',  ( -1.000000000000000000, 0.000000000000000000, -0.000000000000000000 ) ) ;
#58859=ORIENTED_EDGE ( 'NONE', *, *, #13347, .T. ) ;
#58860=AXIS2_PLACEMENT_3D ( 'NONE', #27867, #73719, #38785 ) ;
#58861=LINE ( 'NONE', #26110, #29468 ) ;
#58862=AXIS2_PLACEMENT_3D ( 'NONE', #49517, #48776, #4052 ) ;
#58868=DIRECTION ( 'NONE',  ( 1.000000000000000000, 0.000000000000000000, 0.000000000000000000 ) ) ;
#58871=AXIS2_PLACEMENT_3D ( 'NONE', #70721, #19227, #48546 ) ;
#58883=AXIS2_PLACEMENT_3D ( 'NONE', #26593, #65720, #25852 ) ;
#58886=EDGE_CURVE ( 'NONE', #38466, #15320, #12682, .T. ) ;
#58890=FACE_OUTER_BOUND ( 'NONE', #35097, .T. ) ;
#58892=ADVANCED_FACE ( 'NONE', ( #8794 ), #8434, .T. ) ;
#58895=ORIENTED_EDGE ( 'NONE', *, *, #66475, .T. ) ;
#58908=ORIENTED_EDGE ( 'NONE', *, *, #69370, .T. ) ;
#58910=VERTEX_POINT ( 'NONE', #25351 ) ;
#58914=AXIS2_PLACEMENT_3D ( 'NONE', #39886, #45153, #35351 ) ;
#58918=AXIS2_PLACEMENT_3D ( 'NONE', #67652, #30923, #65905 ) ;
#58926=EDGE_CURVE ( 'NONE', #5866, #10267, #40324, .T. ) ;
#58937=CARTESIAN_POINT ( 'NONE',  ( 10.00000000000000000, 0.000000000000000000, 0.000000000000000000 ) ) ;
#58943=EDGE_CURVE ( 'NONE', #24336, #19951, #63154, .T. ) ;
#58945=LINE ( 'NONE', #53294, #32877 ) ;
#58953=DIRECTION ( 'NONE',  ( 1.000000000000000000, 0.000000000000000000, -0.000000000000000000 ) ) ;
#58960=CARTESIAN_POINT ( 'NONE',  ( 10.00000000000000000, -41.76937507738831812, 62.50329211542423025 ) ) ;
#58963=FACE_OUTER_BOUND ( 'NONE', #42735, .T. ) ;
#58971=AXIS2_PLACEMENT_3D ( 'NONE', #34895, #57832, #6337 ) ;
#58973=DIRECTION ( 'NONE',  ( 0.000000000000000000, 0.000000000000000000, -1.000000000000000000 ) ) ;
#58979=EDGE_CURVE ( 'NONE', #29678, #66220, #71187, .T. ) ;
#58983=ORIENTED_EDGE ( 'NONE', *, *, #39505, .T. ) ;
#58993=CIRCLE ( 'NONE', #25404, 31.99999999999999645 ) ;
#58995=DIRECTION ( 'NONE',  ( -1.000000000000000000, 0.000000000000000000, 0.000000000000000000 ) ) ;
#58998=ORIENTED_EDGE ( 'NONE', *, *, #23330, .T. ) ;
#59002=CARTESIAN_POINT ( 'NONE',  ( 10.00000000000000000, 68.67312586195046720, -35.91791733033402068 ) ) ;
#59005=ORIENTED_EDGE ( 'NONE', *, *, #24929, .T. ) ;
#59010=VERTEX_POINT ( 'NONE', #30599 ) ;
#59023=ORIENTED_EDGE ( 'NONE', *, *, #213, .T. ) ;
#59028=CIRCLE ( 'NONE', #26592, 82.00000000000000000 ) ;
#59032=EDGE_CURVE ( 'NONE', #61902, #38392, #44500, .T. ) ;
#59051=DIRECTION ( 'NONE',  ( 0.000000000000000000, -0.8910065241883627918, -0.4539904997395567965 ) ) ;
#59052=FACE_OUTER_BOUND ( 'NONE', #18872, .T. ) ;
#59054=AXIS2_PLACEMENT_3D ( 'NONE', #24810, #53024, #30802 ) ;
#59055=DIRECTION ( 'NONE',  ( -1.000000000000000000, 0.000000000000000000, 0.000000000000000000 ) ) ;
#59065=ORIENTED_EDGE ( 'NONE', *, *, #20456, .F. ) ;
#59073=CIRCLE ( 'NONE', #57851, 31.99999999999999289 ) ;
#59074=DIRECTION ( 'NONE',  ( -1.000000000000000000, 0.000000000000000000, 0.000000000000000000 ) ) ;
#59077=DIRECTION ( 'NONE',  ( 0.000000000000000000, 0.000000000000000000, 1.000000000000000000 ) ) ;
#59091=ORIENTED_EDGE ( 'NONE', *, *, #66041, .F. ) ;
#59093=ADVANCED_FACE ( 'NONE', ( #16658 ), #9536, .T. ) ;
#59114=DIRECTION ( 'NONE',  ( 0.000000000000000000, 0.000000000000000000, -1.000000000000000000 ) ) ;
#59123=DIRECTION ( 'NONE',  ( -1.000000000000000000, 0.000000000000000000, 0.000000000000000000 ) ) ;
#59126=CARTESIAN_POINT ( 'NONE',  ( 10.00000000000000000, -66.50666863322028632, 39.78640506895582973 ) ) ;
#59131=ORIENTED_EDGE ( 'NONE', *, *, #47218, .T. ) ;
#59141=ORIENTED_EDGE ( 'NONE', *, *, #27425, .F. ) ;
#59142=CARTESIAN_POINT ( 'NONE',  ( 10.00000000000000000, 72.35160999960817207, 20.41045688087850607 ) ) ;
#59148=CARTESIAN_POINT ( 'NONE',  ( -10.00000000000000000, 0.000000000000000000, 0.000000000000000000 ) ) ;
#59149=EDGE_CURVE ( 'NONE', #12767, #16822, #62155, .T. ) ;
#59157=CARTESIAN_POINT ( 'NONE',  ( 10.00000000000000000, 0.000000000000000000, 0.000000000000000000 ) ) ;
#59163=ORIENTED_EDGE ( 'NONE', *, *, #16402, .T. ) ;
#59173=DIRECTION ( 'NONE',  ( -1.000000000000000000, 0.000000000000000000, 0.000000000000000000 ) ) ;
#59180=EDGE_CURVE ( 'NONE', #35421, #61359, #29523, .T. ) ;
#59186=ORIENTED_EDGE ( 'NONE', *, *, #30950, .F. ) ;
#59190=ORIENTED_EDGE ( 'NONE', *, *, #70110, .T. ) ;
#59195=CARTESIAN_POINT ( 'NONE',  ( 10.00000000000000000, 0.000000000000000000, 0.000000000000000000 ) ) ;
#59208=LINE ( 'NONE', #70844, #64240 ) ;
#59210=VERTEX_POINT ( 'NONE', #61418 ) ;
#59216=CARTESIAN_POINT ( 'NONE',  ( 0.000000000000000000, -70.52718814184240159, -26.02418014898383802 ) ) ;
#59217=DIRECTION ( 'NONE',  ( -1.000000000000000000, 0.000000000000000000, 0.000000000000000000 ) ) ;
#59225=AXIS2_PLACEMENT_3D ( 'NONE', #62249, #44590, #67509 ) ;
#59229=FACE_OUTER_BOUND ( 'NONE', #21811, .T. ) ;
#59239=DIRECTION ( 'NONE',  ( 1.000000000000000000, 0.000000000000000000, 0.000000000000000000 ) ) ;
#59249=ORIENTED_EDGE ( 'NONE', *, *, #6145, .F. ) ;
#59257=EDGE_LOOP ( 'NONE', ( #11373, #15823, #53919, #6211 ) ) ;
#59264=DIRECTION ( 'NONE',  ( -1.000000000000000000, 0.000000000000000000, 0.000000000000000000 ) ) ;
#59267=DIRECTION ( 'NONE',  ( -1.000000000000000000, -0.000000000000000000, -0.000000000000000000 ) ) ;
#59269=AXIS2_PLACEMENT_3D ( 'NONE', #39368, #5911, #66548 ) ;
#59270=CARTESIAN_POINT ( 'NONE',  ( 0.000000000000000000, 0.000000000000000000, 0.000000000000000000 ) ) ;
#59272=VERTEX_POINT ( 'NONE', #69639 ) ;
#59277=CYLINDRICAL_SURFACE ( 'NONE', #57442, 77.49899999999999523 ) ;
#59284=ORIENTED_EDGE ( 'NONE', *, *, #72887, .T. ) ;
#59293=CARTESIAN_POINT ( 'NONE',  ( 10.00000000000000000, 59.03342792756263435, 46.54456581323825048 ) ) ;
#59300=ORIENTED_EDGE ( 'NONE', *, *, #57984, .F. ) ;
#59308=ORIENTED_EDGE ( 'NONE', *, *, #55496, .T. ) ;
#59309=VECTOR ( 'NONE', #41852, 1000.000000000000000 ) ;
#59310=ADVANCED_FACE ( 'NONE', ( #64377 ), #17396, .T. ) ;
#59312=FACE_OUTER_BOUND ( 'NONE', #24863, .T. ) ;
#59313=AXIS2_PLACEMENT_3D ( 'NONE', #56967, #18126, #25249 ) ;
#59329=CARTESIAN_POINT ( 'NONE',  ( 10.00000000000000000, -63.97538442413463855, 51.29473840253199768 ) ) ;
#59333=AXIS2_PLACEMENT_3D ( 'NONE', #5897, #58868, #7362 ) ;
#59341=DIRECTION ( 'NONE',  ( 0.000000000000000000, 0.000000000000000000, 1.000000000000000000 ) ) ;
#59350=EDGE_CURVE ( 'NONE', #71222, #47809, #5401, .T. ) ;
#59351=FACE_OUTER_BOUND ( 'NONE', #45069, .T. ) ;
#59353=EDGE_CURVE ( 'NONE', #51767, #1192, #17030, .T. ) ;
#59379=ORIENTED_EDGE ( 'NONE', *, *, #3699, .F. ) ;
#59385=ORIENTED_EDGE ( 'NONE', *, *, #29089, .T. ) ;
#59397=CARTESIAN_POINT ( 'NONE',  ( 10.00000000000000000, -65.59268652807183742, -36.72794159290312166 ) ) ;
#59419=CARTESIAN_POINT ( 'NONE',  ( 0.000000000000000000, 0.000000000000000000, 0.000000000000000000 ) ) ;
#59427=ORIENTED_EDGE ( 'NONE', *, *, #50339, .F. ) ;
#59434=CARTESIAN_POINT ( 'NONE',  ( 10.00000000000000000, -63.18004540533059554, 44.88180994100355292 ) ) ;
#59437=EDGE_CURVE ( 'NONE', #63900, #39587, #19237, .T. ) ;
#59438=CIRCLE ( 'NONE', #55838, 77.49899999999999523 ) ;
#59458=ORIENTED_EDGE ( 'NONE', *, *, #28596, .T. ) ;
#59478=LINE ( 'NONE', #2743, #13088 ) ;
#59481=ORIENTED_EDGE ( 'NONE', *, *, #27061, .T. ) ;
#59483=VERTEX_POINT ( 'NONE', #7956 ) ;
#59485=CIRCLE ( 'NONE', #9026, 77.49899999999999523 ) ;
#59491=EDGE_CURVE ( 'NONE', #71738, #14718, #60228, .T. ) ;
#59497=EDGE_CURVE ( 'NONE', #18411, #56810, #71373, .T. ) ;
#59508=DIRECTION ( 'NONE',  ( -1.000000000000000000, -0.000000000000000000, -0.000000000000000000 ) ) ;
#59516=FACE_OUTER_BOUND ( 'NONE', #61316, .T. ) ;
#59525=CARTESIAN_POINT ( 'NONE',  ( 10.00000000000000000, 60.67117009219136037, 55.16347631943062879 ) ) ;
#59543=ORIENTED_EDGE ( 'NONE', *, *, #34376, .T. ) ;
#59550=ORIENTED_EDGE ( 'NONE', *, *, #25125, .T. ) ;
#59557=DIRECTION ( 'NONE',  ( 0.000000000000000000, -0.9510565162951499785, -0.3090169943749582204 ) ) ;
#59559=VERTEX_POINT ( 'NONE', #44779 ) ;
#59580=EDGE_CURVE ( 'NONE', #71482, #16336, #4939, .T. ) ;
#59595=DIRECTION ( 'NONE',  ( 1.000000000000000000, 0.000000000000000000, 0.000000000000000000 ) ) ;
#59601=DIRECTION ( 'NONE',  ( 0.000000000000000000, 0.000000000000000000, 1.000000000000000000 ) ) ;
#59610=EDGE_CURVE ( 'NONE', #26168, #29955, #66593, .T. ) ;
#59617=DIRECTION ( 'NONE',  ( -1.000000000000000000, 0.000000000000000000, 0.000000000000000000 ) ) ;
#59622=ADVANCED_FACE ( 'NONE', ( #10544 ), #37657, .T. ) ;
#59626=ORIENTED_EDGE ( 'NONE', *, *, #14957, .T. ) ;
#59634=DIRECTION ( 'NONE',  ( 0.000000000000000000, 0.3090169943749410120, 0.9510565162951556406 ) ) ;
#59637=CARTESIAN_POINT ( 'NONE',  ( 10.00000000000000000, 49.70050353004889132, 59.46389618801982380 ) ) ;
#59638=AXIS2_PLACEMENT_3D ( 'NONE', #21091, #15088, #10562 ) ;
#59645=ORIENTED_EDGE ( 'NONE', *, *, #48239, .T. ) ;
#59667=LINE ( 'NONE', #43864, #72181 ) ;
#59669=CYLINDRICAL_SURFACE ( 'NONE', #36079, 77.49899999999999523 ) ;
#59671=DIRECTION ( 'NONE',  ( 0.000000000000000000, 0.000000000000000000, 1.000000000000000000 ) ) ;
#59675=ADVANCED_FACE ( 'NONE', ( #74069 ), #68455, .T. ) ;
#59684=LINE ( 'NONE', #48762, #42898 ) ;
#59685=VERTEX_POINT ( 'NONE', #29314 ) ;
#59686=ORIENTED_EDGE ( 'NONE', *, *, #2905, .T. ) ;
#59704=VECTOR ( 'NONE', #16484, 1000.000000000000000 ) ;
#59705=DIRECTION ( 'NONE',  ( -1.000000000000000000, 0.000000000000000000, 0.000000000000000000 ) ) ;
#59709=AXIS2_PLACEMENT_3D ( 'NONE', #19533, #59775, #19900 ) ;
#59722=EDGE_CURVE ( 'NONE', #26087, #57460, #11443, .T. ) ;
#59724=ORIENTED_EDGE ( 'NONE', *, *, #41117, .T. ) ;
#59732=ORIENTED_EDGE ( 'NONE', *, *, #8913, .F. ) ;
#59741=EDGE_CURVE ( 'NONE', #59210, #14718, #23428, .T. ) ;
#59746=ORIENTED_EDGE ( 'NONE', *, *, #67726, .F. ) ;
#59751=CIRCLE ( 'NONE', #22558, 31.99999999999998579 ) ;
#59754=ADVANCED_FACE ( 'NONE', ( #5314 ), #45530, .T. ) ;
#59755=LINE ( 'NONE', #42828, #69681 ) ;
#59756=ORIENTED_EDGE ( 'NONE', *, *, #50432, .T. ) ;
#59761=DIRECTION ( 'NONE',  ( 0.000000000000000000, 0.8090169943749487835, -0.5877852522924712497 ) ) ;
#59774=LINE ( 'NONE', #31184, #24811 ) ;
#59775=DIRECTION ( 'NONE',  ( -1.000000000000000000, -0.000000000000000000, 0.000000000000000000 ) ) ;
#59786=DIRECTION ( 'NONE',  ( -1.000000000000000000, 0.000000000000000000, 0.000000000000000000 ) ) ;
#59787=ADVANCED_FACE ( 'NONE', ( #54759 ), #3287, .T. ) ;
#59792=VECTOR ( 'NONE', #67751, 1000.000000000000000 ) ;
#59809=AXIS2_PLACEMENT_3D ( 'NONE', #56664, #73926, #39740 ) ;
#59814=DIRECTION ( 'NONE',  ( -1.000000000000000000, 0.000000000000000000, 0.000000000000000000 ) ) ;
#59815=VERTEX_POINT ( 'NONE', #31812 ) ;
#59819=ORIENTED_EDGE ( 'NONE', *, *, #74282, .T. ) ;
#59827=VERTEX_POINT ( 'NONE', #58634 ) ;
#59828=VERTEX_POINT ( 'NONE', #37847 ) ;
#59832=AXIS2_PLACEMENT_3D ( 'NONE', #53524, #70805, #25332 ) ;
#59837=DIRECTION ( 'NONE',  ( 1.000000000000000000, -0.000000000000000000, 0.000000000000000000 ) ) ;
#59841=ORIENTED_EDGE ( 'NONE', *, *, #48448, .T. ) ;
#59858=ADVANCED_FACE ( 'NONE', ( #55125 ), #3650, .T. ) ;
#59864=CARTESIAN_POINT ( 'NONE',  ( 0.000000000000000000, 0.000000000000000000, 0.000000000000000000 ) ) ;
#59866=CYLINDRICAL_SURFACE ( 'NONE', #49906, 31.99999999999999289 ) ;
#59873=EDGE_CURVE ( 'NONE', #45145, #70724, #53368, .T. ) ;
#59874=CARTESIAN_POINT ( 'NONE',  ( 0.000000000000000000, 80.55351364060611274, -15.33399622253396544 ) ) ;
#59877=ORIENTED_EDGE ( 'NONE', *, *, #26924, .F. ) ;
#59885=DIRECTION ( 'NONE',  ( -1.000000000000000000, 0.000000000000000000, 0.000000000000000000 ) ) ;
#59886=ORIENTED_EDGE ( 'NONE', *, *, #65347, .F. ) ;
#59887=EDGE_CURVE ( 'NONE', #62914, #26721, #7141, .T. ) ;
#59890=LINE ( 'NONE', #53500, #21323 ) ;
#59892=CARTESIAN_POINT ( 'NONE',  ( 0.000000000000000000, 2.543863470249527303, -81.96053171279901051 ) ) ;
#59898=AXIS2_PLACEMENT_3D ( 'NONE', #34661, #40683, #35406 ) ;
#59899=VECTOR ( 'NONE', #21126, 1000.000000000000000 ) ;
#59905=ORIENTED_EDGE ( 'NONE', *, *, #29692, .T. ) ;
#59908=CYLINDRICAL_SURFACE ( 'NONE', #1840, 32.00000000000000000 ) ;
#59914=DIRECTION ( 'NONE',  ( 0.000000000000000000, 0.000000000000000000, 1.000000000000000000 ) ) ;
#59917=AXIS2_PLACEMENT_3D ( 'NONE', #60314, #48644, #70439 ) ;
#59918=CARTESIAN_POINT ( 'NONE',  ( 10.00000000000000000, 76.66974797899837313, 11.30684508768368524 ) ) ;
#59929=VERTEX_POINT ( 'NONE', #72765 ) ;
#59933=EDGE_CURVE ( 'NONE', #73763, #1655, #54646, .T. ) ;
#59937=CIRCLE ( 'NONE', #67108, 77.49900000000000944 ) ;
#59947=DIRECTION ( 'NONE',  ( 0.000000000000000000, 0.4539904997395413089, 0.8910065241883705633 ) ) ;
#59949=CYLINDRICAL_SURFACE ( 'NONE', #12483, 82.00000000000000000 ) ;
#59950=CYLINDRICAL_SURFACE ( 'NONE', #64312, 77.49899999999999523 ) ;
#59952=AXIS2_PLACEMENT_3D ( 'NONE', #70612, #58995, #42075 ) ;
#59953=CARTESIAN_POINT ( 'NONE',  ( 10.00000000000000000, 74.74816331893428867, 33.71516098798765881 ) ) ;
#59954=CIRCLE ( 'NONE', #45573, 31.99999999999998579 ) ;
#59963=DIRECTION ( 'NONE',  ( 0.000000000000000000, 0.000000000000000000, -1.000000000000000000 ) ) ;
#59970=EDGE_CURVE ( 'NONE', #31543, #71294, #44972, .T. ) ;
#59972=CARTESIAN_POINT ( 'NONE',  ( 10.00000000000000000, 0.000000000000000000, 0.000000000000000000 ) ) ;
#59978=FACE_OUTER_BOUND ( 'NONE', #71086, .T. ) ;
#59981=DIRECTION ( 'NONE',  ( 1.000000000000000000, 0.000000000000000000, 0.000000000000000000 ) ) ;
#59987=DIRECTION ( 'NONE',  ( 0.000000000000000000, -0.8526401643540861830, -0.5224985647159590130 ) ) ;
#60017=EDGE_CURVE ( 'NONE', #25521, #71862, #27045, .T. ) ;
#60024=AXIS2_PLACEMENT_3D ( 'NONE', #59397, #25543, #53748 ) ;
#60025=CARTESIAN_POINT ( 'NONE',  ( 0.000000000000000000, 24.73286445877808148, -73.44644590900034586 ) ) ;
#60032=ORIENTED_EDGE ( 'NONE', *, *, #73939, .F. ) ;
#60039=DIRECTION ( 'NONE',  ( 0.000000000000000000, 0.3826834323650907810, -0.9238795325112864054 ) ) ;
#60043=VERTEX_POINT ( 'NONE', #67151 ) ;
#60045=EDGE_LOOP ( 'NONE', ( #33084, #876, #62702, #21113 ) ) ;
#60047=CARTESIAN_POINT ( 'NONE',  ( 10.00000000000000000, -23.16143007188376757, -73.95703589263997912 ) ) ;
#60054=AXIS2_PLACEMENT_3D ( 'NONE', #3669, #72055, #25824 ) ;
#60065=VERTEX_POINT ( 'NONE', #45729 ) ;
#60073=VERTEX_POINT ( 'NONE', #68651 ) ;
#60080=LINE ( 'NONE', #25475, #38889 ) ;
#60082=LINE ( 'NONE', #37875, #32520 ) ;
#60085=CYLINDRICAL_SURFACE ( 'NONE', #58734, 82.00000000000000000 ) ;
#60087=CARTESIAN_POINT ( 'NONE',  ( 0.000000000000000000, -75.11725578898466438, -2.956366410621452001 ) ) ;
#60089=AXIS2_PLACEMENT_3D ( 'NONE', #42582, #48943, #8742 ) ;
#60093=EDGE_CURVE ( 'NONE', #61657, #65189, #37904, .T. ) ;
#60094=CARTESIAN_POINT ( 'NONE',  ( -10.00000000000000000, 0.000000000000000000, 0.000000000000000000 ) ) ;
#60110=CARTESIAN_POINT ( 'NONE',  ( 10.00000000000000000, -24.73286445877653961, -73.44644590900085745 ) ) ;
#60119=ORIENTED_EDGE ( 'NONE', *, *, #21213, .T. ) ;
#60128=ORIENTED_EDGE ( 'NONE', *, *, #41665, .F. ) ;
#60132=ORIENTED_EDGE ( 'NONE', *, *, #1808, .T. ) ;
#60138=AXIS2_PLACEMENT_3D ( 'NONE', #54416, #15298, #4414 ) ;
#60153=DIRECTION ( 'NONE',  ( -1.000000000000000000, 0.000000000000000000, -0.000000000000000000 ) ) ;
#60176=CARTESIAN_POINT ( 'NONE',  ( 5.000000000000002665, -71.87247863392443037, 39.47590169984818687 ) ) ;
#60199=EDGE_CURVE ( 'NONE', #70437, #36744, #29462, .T. ) ;
#60202=ORIENTED_EDGE ( 'NONE', *, *, #18935, .F. ) ;
#60207=CIRCLE ( 'NONE', #68587, 77.49900000000000944 ) ;
#60228=LINE ( 'NONE', #65490, #52183 ) ;
#60242=CARTESIAN_POINT ( 'NONE',  ( 0.000000000000000000, 0.000000000000000000, 0.000000000000000000 ) ) ;
#60249=CARTESIAN_POINT ( 'NONE',  ( 10.00000000000000000, 77.32052557432849937, -5.256550761632002633 ) ) ;
#60252=CIRCLE ( 'NONE', #29041, 31.99999999999999289 ) ;
#60259=DIRECTION ( 'NONE',  ( 0.000000000000000000, -0.1564344650402172687, -0.9876883405951399908 ) ) ;
#60268=LINE ( 'NONE', #13999, #22567 ) ;
#60281=DIRECTION ( 'NONE',  ( 0.000000000000000000, 0.000000000000000000, 1.000000000000000000 ) ) ;
#60287=SURFACE_SIDE_STYLE ('',( #3516 ) ) ;
#60307=ORIENTED_EDGE ( 'NONE', *, *, #35712, .F. ) ;
#60314=CARTESIAN_POINT ( 'NONE',  ( 0.000000000000000000, 41.76937507738788469, 62.50329211542452157 ) ) ;
#60331=CARTESIAN_POINT ( 'NONE',  ( 10.00000000000000000, -75.54627589209931671, -17.28742895386164591 ) ) ;
#60335=DIRECTION ( 'NONE',  ( -1.000000000000000000, -0.000000000000000000, -0.000000000000000000 ) ) ;
#60341=CARTESIAN_POINT ( 'NONE',  ( 10.00000000000000000, -68.26794271651286294, 31.47745569255117104 ) ) ;
#60346=ADVANCED_FACE ( 'NONE', ( #49020 ), #71202, .T. ) ;
#60351=AXIS2_PLACEMENT_3D ( 'NONE', #14431, #8795, #30600 ) ;
#60359=DIRECTION ( 'NONE',  ( -1.000000000000000000, 0.000000000000000000, -0.000000000000000000 ) ) ;
#60367=CYLINDRICAL_SURFACE ( 'NONE', #61685, 31.99999999999999289 ) ;
#60373=VERTEX_POINT ( 'NONE', #8448 ) ;
#60377=EDGE_CURVE ( 'NONE', #18834, #33464, #31874, .T. ) ;
#60378=ORIENTED_EDGE ( 'NONE', *, *, #73929, .T. ) ;
#60389=CARTESIAN_POINT ( 'NONE',  ( 0.000000000000000000, 0.000000000000000000, 0.000000000000000000 ) ) ;
#60396=ORIENTED_EDGE ( 'NONE', *, *, #21202, .F. ) ;
#60398=CARTESIAN_POINT ( 'NONE',  ( 5.000000000000002665, 40.65526001592612459, 71.21200624218811015 ) ) ;
#60399=AXIS2_PLACEMENT_3D ( 'NONE', #9502, #55737, #27144 ) ;
#60420=CARTESIAN_POINT ( 'NONE',  ( 10.00000000000000000, 0.000000000000000000, 0.000000000000000000 ) ) ;
#60426=DIRECTION ( 'NONE',  ( -1.000000000000000000, -0.000000000000000000, 0.000000000000000000 ) ) ;
#60448=CIRCLE ( 'NONE', #18395, 31.99999999999999289 ) ;
#60451=CARTESIAN_POINT ( 'NONE',  ( 0.000000000000000000, 62.50329211542435104, 41.76937507738811917 ) ) ;
#60456=EDGE_CURVE ( 'NONE', #25971, #33774, #29519, .T. ) ;
#60468=VECTOR ( 'NONE', #39169, 1000.000000000000000 ) ;
#60471=ORIENTED_EDGE ( 'NONE', *, *, #26968, .T. ) ;
#60474=DIRECTION ( 'NONE',  ( -1.000000000000000000, -0.000000000000000000, -0.000000000000000000 ) ) ;
#60481=DIRECTION ( 'NONE',  ( -1.000000000000000000, -0.000000000000000000, -0.000000000000000000 ) ) ;
#60486=ORIENTED_EDGE ( 'NONE', *, *, #57967, .T. ) ;
#60487=DIRECTION ( 'NONE',  ( -1.000000000000000000, -0.000000000000000000, 0.000000000000000000 ) ) ;
#60490=VERTEX_POINT ( 'NONE', #62171 ) ;
#60493=AXIS2_PLACEMENT_3D ( 'NONE', #71837, #53453, #1990 ) ;
#60494=EDGE_LOOP ( 'NONE', ( #38806, #41346, #32886, #69067 ) ) ;
#60502=VERTEX_POINT ( 'NONE', #45258 ) ;
#60508=DIRECTION ( 'NONE',  ( 0.000000000000000000, 0.000000000000000000, 1.000000000000000000 ) ) ;
#60509=VERTEX_POINT ( 'NONE', #4671 ) ;
#60510=DIRECTION ( 'NONE',  ( -1.000000000000000000, -0.000000000000000000, -0.000000000000000000 ) ) ;
#60511=AXIS2_PLACEMENT_3D ( 'NONE', #72559, #44015, #66930 ) ;
#60513=ORIENTED_EDGE ( 'NONE', *, *, #66, .T. ) ;
#60520=DIRECTION ( 'NONE',  ( -1.000000000000000000, 0.000000000000000000, 0.000000000000000000 ) ) ;
#60527=CARTESIAN_POINT ( 'NONE',  ( 10.00000000000000178, 0.000000000000000000, 0.000000000000000000 ) ) ;
#60534=CARTESIAN_POINT ( 'NONE',  ( 10.00000000000000000, 0.000000000000000000, 0.000000000000000000 ) ) ;
#60536=EDGE_CURVE ( 'NONE', #70328, #13032, #55931, .T. ) ;
#60549=DIRECTION ( 'NONE',  ( -1.000000000000000000, 0.000000000000000000, 0.000000000000000000 ) ) ;
#60551=DIRECTION ( 'NONE',  ( 0.000000000000000000, 0.000000000000000000, 1.000000000000000000 ) ) ;
#60557=VERTEX_POINT ( 'NONE', #23791 ) ;
#60559=DIRECTION ( 'NONE',  ( -1.000000000000000000, 0.000000000000000000, 0.000000000000000000 ) ) ;
#60565=VERTEX_POINT ( 'NONE', #17774 ) ;
#60575=AXIS2_PLACEMENT_3D ( 'NONE', #68488, #16976, #28609 ) ;
#60591=DIRECTION ( 'NONE',  ( 1.000000000000000000, 0.000000000000000000, -0.000000000000000000 ) ) ;
#60600=VERTEX_POINT ( 'NONE', #35796 ) ;
#60603=CARTESIAN_POINT ( 'NONE',  ( 10.00000000000000000, 0.000000000000000000, 0.000000000000000000 ) ) ;
#60606=DIRECTION ( 'NONE',  ( -1.000000000000000000, -0.000000000000000000, 0.000000000000000000 ) ) ;
#60618=CARTESIAN_POINT ( 'NONE',  ( 0.000000000000000000, -39.78640506895559525, -66.50666863322042843 ) ) ;
#60623=EDGE_CURVE ( 'NONE', #16652, #70598, #58751, .T. ) ;
#60626=LINE ( 'NONE', #67358, #41643 ) ;
#60627=CIRCLE ( 'NONE', #54654, 82.00000000000000000 ) ;
#60630=CARTESIAN_POINT ( 'NONE',  ( 10.00000000000000000, 0.000000000000000000, 0.000000000000000000 ) ) ;
#60656=ORIENTED_EDGE ( 'NONE', *, *, #63822, .T. ) ;
#60664=ORIENTED_EDGE ( 'NONE', *, *, #57358, .T. ) ;
#60689=ORIENTED_EDGE ( 'NONE', *, *, #41662, .F. ) ;
#60697=CIRCLE ( 'NONE', #24665, 12.50000000000000000 ) ;
#60698=CYLINDRICAL_SURFACE ( 'NONE', #72244, 82.00000000000000000 ) ;
#60699=CARTESIAN_POINT ( 'NONE',  ( 5.000000000000000000, -74.74816331893454446, 33.71516098798714722 ) ) ;
#60709=DIRECTION ( 'NONE',  ( 0.000000000000000000, 0.000000000000000000, 1.000000000000000000 ) ) ;
#60712=DIRECTION ( 'NONE',  ( -1.000000000000000000, 0.000000000000000000, 0.000000000000000000 ) ) ;
#60722=DIRECTION ( 'NONE',  ( 0.000000000000000000, 0.8526401643540897357, 0.5224985647159531288 ) ) ;
#60727=EDGE_CURVE ( 'NONE', #62260, #29988, #54757, .T. ) ;
#60731=CARTESIAN_POINT ( 'NONE',  ( 10.00000000000000000, 0.000000000000000000, 0.000000000000000000 ) ) ;
#60737=CIRCLE ( 'NONE', #70306, 77.49899999999998101 ) ;
#60738=CIRCLE ( 'NONE', #24661, 31.99999999999999289 ) ;
#60740=ORIENTED_EDGE ( 'NONE', *, *, #22089, .F. ) ;
#60750=LINE ( 'NONE', #66395, #32787 ) ;
#60765=FACE_OUTER_BOUND ( 'NONE', #23390, .T. ) ;
#60766=ADVANCED_FACE ( 'NONE', ( #66246 ), #14722, .T. ) ;
#60771=ORIENTED_EDGE ( 'NONE', *, *, #40556, .T. ) ;
#60775=VERTEX_POINT ( 'NONE', #70373 ) ;
#60790=DIRECTION ( 'NONE',  ( 0.000000000000000000, -6.938893903907228378E-15, 1.000000000000000000 ) ) ;
#60811=ADVANCED_FACE ( 'NONE', ( #8724 ), #59866, .T. ) ;
#60819=CARTESIAN_POINT ( 'NONE',  ( 0.000000000000000000, -63.97538442413390669, -51.29473840253292849 ) ) ;
#60825=CARTESIAN_POINT ( 'NONE',  ( 10.00000000000000000, 0.000000000000000000, 0.000000000000000000 ) ) ;
#60830=ORIENTED_EDGE ( 'NONE', *, *, #12478, .T. ) ;
#60834=CYLINDRICAL_SURFACE ( 'NONE', #66408, 77.49899999999999523 ) ;
#60840=ORIENTED_EDGE ( 'NONE', *, *, #13977, .T. ) ;
#60842=DIRECTION ( 'NONE',  ( -1.000000000000000000, 0.000000000000000000, -0.000000000000000000 ) ) ;
#60843=ADVANCED_FACE ( 'NONE', ( #8353 ), #30526, .T. ) ;
#60845=LINE ( 'NONE', #3721, #53314 ) ;
#60847=DIRECTION ( 'NONE',  ( -1.000000000000000000, 0.000000000000000000, -0.000000000000000000 ) ) ;
#60851=EDGE_CURVE ( 'NONE', #71294, #29955, #36768, .T. ) ;
#60861=DIRECTION ( 'NONE',  ( -1.000000000000000000, 0.000000000000000000, 0.000000000000000000 ) ) ;
#60869=CYLINDRICAL_SURFACE ( 'NONE', #30082, 82.00000000000000000 ) ;
#60880=DIRECTION ( 'NONE',  ( -1.000000000000000000, 0.000000000000000000, 0.000000000000000000 ) ) ;
#60885=EDGE_CURVE ( 'NONE', #63017, #57622, #11596, .T. ) ;
#60886=EDGE_CURVE ( 'NONE', #38196, #63089, #16388, .T. ) ;
#60900=DIRECTION ( 'NONE',  ( -1.000000000000000000, 0.000000000000000000, -0.000000000000000000 ) ) ;
#60906=FACE_OUTER_BOUND ( 'NONE', #11302, .T. ) ;
#60908=CARTESIAN_POINT ( 'NONE',  ( 10.00000000000000000, 0.000000000000000000, 0.000000000000000000 ) ) ;
#60911=ORIENTED_EDGE ( 'NONE', *, *, #6028, .F. ) ;
#60921=VERTEX_POINT ( 'NONE', #66607 ) ;
#60929=ORIENTED_EDGE ( 'NONE', *, *, #69530, .F. ) ;
#60938=CARTESIAN_POINT ( 'NONE',  ( 0.000000000000000000, 56.15606465354959198, 59.75363087400094741 ) ) ;
#60942=ORIENTED_EDGE ( 'NONE', *, *, #14862, .F. ) ;
#60954=ORIENTED_EDGE ( 'NONE', *, *, #43068, .F. ) ;
#60957=CARTESIAN_POINT ( 'NONE',  ( 10.00000000000000000, 54.21277698773752718, -55.38113227695725271 ) ) ;
#60958=CARTESIAN_POINT ( 'NONE',  ( 0.000000000000000000, 79.10210256391398786, -21.60688246758503084 ) ) ;
#60961=DIRECTION ( 'NONE',  ( -1.000000000000000000, 0.000000000000000000, -0.000000000000000000 ) ) ;
#60967=EDGE_CURVE ( 'NONE', #8405, #24336, #46388, .T. ) ;
#60974=DIRECTION ( 'NONE',  ( 0.000000000000000000, 0.8910065241883690090, -0.4539904997395446395 ) ) ;
#60976=AXIS2_PLACEMENT_3D ( 'NONE', #63174, #40596, #51873 ) ;
#60979=AXIS2_PLACEMENT_3D ( 'NONE', #72789, #26198, #31839 ) ;
#60980=AXIS2_PLACEMENT_3D ( 'NONE', #35923, #59239, #13729 ) ;
#60986=VECTOR ( 'NONE', #32030, 1000.000000000000000 ) ;
#60989=CARTESIAN_POINT ( 'NONE',  ( 10.00000000000000000, 39.78640506895700213, -66.50666863321957578 ) ) ;
#60995=AXIS2_PLACEMENT_3D ( 'NONE', #64915, #25050, #69433 ) ;
#61006=ADVANCED_FACE ( 'NONE', ( #9452 ), #72229, .T. ) ;
#61007=CYLINDRICAL_SURFACE ( 'NONE', #60399, 82.00000000000000000 ) ;
#61012=ORIENTED_EDGE ( 'NONE', *, *, #29973, .F. ) ;
#61014=ORIENTED_EDGE ( 'NONE', *, *, #43079, .F. ) ;
#61017=ORIENTED_EDGE ( 'NONE', *, *, #4721, .F. ) ;
#61026=DIRECTION ( 'NONE',  ( 0.000000000000000000, -0.07845909572783053842, -0.9969173337331290741 ) ) ;
#61029=CIRCLE ( 'NONE', #2251, 77.49899999999998101 ) ;
#61037=AXIS2_PLACEMENT_3D ( 'NONE', #48941, #49316, #15104 ) ;
#61043=LINE ( 'NONE', #42647, #2304 ) ;
#61045=EDGE_CURVE ( 'NONE', #52606, #36080, #72811, .T. ) ;
#61047=ADVANCED_FACE ( 'NONE', ( #23703 ), #69567, .T. ) ;
#61048=EDGE_LOOP ( 'NONE', ( #6212, #45495, #25657, #28869 ) ) ;
#61053=CARTESIAN_POINT ( 'NONE',  ( 0.000000000000000000, -74.18225833017864090, -34.94270380257719211 ) ) ;
#61058=DIRECTION ( 'NONE',  ( 0.000000000000000000, -0.7604059656000227152, -0.6494480483301933171 ) ) ;
#61060=DIRECTION ( 'NONE',  ( 1.000000000000000000, -0.000000000000000000, 0.000000000000000000 ) ) ;
#61061=FACE_OUTER_BOUND ( 'NONE', #61688, .T. ) ;
#61068=DIRECTION ( 'NONE',  ( -1.000000000000000000, 0.000000000000000000, 0.000000000000000000 ) ) ;
#61070=DIRECTION ( 'NONE',  ( -1.000000000000000000, 0.000000000000000000, 0.000000000000000000 ) ) ;
#61072=CYLINDRICAL_SURFACE ( 'NONE', #25132, 82.00000000000000000 ) ;
#61079=CARTESIAN_POINT ( 'NONE',  ( 5.000000000000002665, -76.69515212746036070, 29.01471420065537643 ) ) ;
#61083=CYLINDRICAL_SURFACE ( 'NONE', #50871, 31.99999999999999289 ) ;
#61086=VECTOR ( 'NONE', #44514, 1000.000000000000000 ) ;
#61088=AXIS2_PLACEMENT_3D ( 'NONE', #63690, #64790, #13272 ) ;
#61091=DIRECTION ( 'NONE',  ( 1.000000000000000000, 0.000000000000000000, -0.000000000000000000 ) ) ;
#61097=VECTOR ( 'NONE', #11697, 1000.000000000000000 ) ;
#61098=ADVANCED_FACE ( 'NONE', ( #34608 ), #69925, .T. ) ;
#61102=EDGE_CURVE ( 'NONE', #40399, #40236, #42789, .T. ) ;
#61104=ORIENTED_EDGE ( 'NONE', *, *, #29756, .F. ) ;
#61108=ADVANCED_FACE ( 'NONE', ( #40632 ), #12781, .T. ) ;
#61113=CIRCLE ( 'NONE', #26265, 82.00000000000000000 ) ;
#61115=ORIENTED_EDGE ( 'NONE', *, *, #1604, .F. ) ;
#61116=CIRCLE ( 'NONE', #43158, 31.99999999999999645 ) ;
#61129=ORIENTED_EDGE ( 'NONE', *, *, #36379, .T. ) ;
#61134=CARTESIAN_POINT ( 'NONE',  ( -10.00000000000000000, 0.000000000000000000, 0.000000000000000000 ) ) ;
#61141=ORIENTED_EDGE ( 'NONE', *, *, #69258, .T. ) ;
#61143=ORIENTED_EDGE ( 'NONE', *, *, #32418, .F. ) ;
#61151=CARTESIAN_POINT ( 'NONE',  ( 10.00000000000000000, -75.16055320797016748, -18.89407956138335365 ) ) ;
#61153=LINE ( 'NONE', #55126, #27810 ) ;
#61157=ORIENTED_EDGE ( 'NONE', *, *, #4803, .T. ) ;
#61162=EDGE_LOOP ( 'NONE', ( #64284, #35460, #48903, #41707 ) ) ;
#61163=AXIS2_PLACEMENT_3D ( 'NONE', #14579, #42058, #67948 ) ;
#61171=CIRCLE ( 'NONE', #23978, 82.00000000000000000 ) ;
#61179=CARTESIAN_POINT ( 'NONE',  ( 5.000000000000002665, 80.55351364060611274, -15.33399622253396544 ) ) ;
#61181=CYLINDRICAL_SURFACE ( 'NONE', #49617, 77.49899999999999523 ) ;
#61188=EDGE_CURVE ( 'NONE', #1192, #57624, #62017, .T. ) ;
#61192=CIRCLE ( 'NONE', #3583, 82.00000000000000000 ) ;
#61198=AXIS2_PLACEMENT_3D ( 'NONE', #4577, #26002, #38402 ) ;
#61205=ADVANCED_FACE ( 'NONE', ( #34991 ), #64670, .T. ) ;
#61209=EDGE_CURVE ( 'NONE', #15320, #36881, #15201, .T. ) ;
#61211=EDGE_CURVE ( 'NONE', #21621, #4375, #59774, .T. ) ;
#61215=CARTESIAN_POINT ( 'NONE',  ( 10.00000000000000000, 15.33399622253481276, 80.55351364060595643 ) ) ;
#61219=ORIENTED_EDGE ( 'NONE', *, *, #971, .F. ) ;
#61227=LINE ( 'NONE', #8968, #29351 ) ;
#61231=ORIENTED_EDGE ( 'NONE', *, *, #20175, .F. ) ;
#61241=DIRECTION ( 'NONE',  ( -1.000000000000000000, -0.000000000000000000, -0.000000000000000000 ) ) ;
#61276=DIRECTION ( 'NONE',  ( -1.000000000000000000, -0.000000000000000000, 0.000000000000000000 ) ) ;
#61287=DIRECTION ( 'NONE',  ( 0.000000000000000000, -0.5224985647159379187, -0.8526401643540989506 ) ) ;
#61294=CYLINDRICAL_SURFACE ( 'NONE', #16353, 77.49899999999999523 ) ;
#61299=ORIENTED_EDGE ( 'NONE', *, *, #32759, .T. ) ;
#61311=VECTOR ( 'NONE', #51338, 1000.000000000000000 ) ;
#61314=CARTESIAN_POINT ( 'NONE',  ( 0.000000000000000000, 12.24744871391589207, -2.500000000000000000 ) ) ;
#61316=EDGE_LOOP ( 'NONE', ( #15146, #2601, #21444, #6701 ) ) ;
#61319=ORIENTED_EDGE ( 'NONE', *, *, #10003, .F. ) ;
#61334=DIRECTION ( 'NONE',  ( 0.000000000000000000, 0.000000000000000000, 1.000000000000000000 ) ) ;
#61335=AXIS2_PLACEMENT_3D ( 'NONE', #52247, #789, #29666 ) ;
#61338=ORIENTED_EDGE ( 'NONE', *, *, #40380, .F. ) ;
#61346=DIRECTION ( 'NONE',  ( 0.000000000000000000, 0.000000000000000000, 1.000000000000000000 ) ) ;
#61348=LINE ( 'NONE', #10565, #31412 ) ;
#61353=CARTESIAN_POINT ( 'NONE',  ( 0.000000000000000000, -33.71516098798792171, 74.74816331893418919 ) ) ;
#61359=VERTEX_POINT ( 'NONE', #71033 ) ;
#61365=CARTESIAN_POINT ( 'NONE',  ( 10.00000000000000000, -69.42325613327466272, 34.44570377933573724 ) ) ;
#61367=CARTESIAN_POINT ( 'NONE',  ( 0.000000000000000000, -79.10210256391383155, 21.60688246758557796 ) ) ;
#61371=EDGE_CURVE ( 'NONE', #33591, #15290, #20018, .T. ) ;
#61379=ORIENTED_EDGE ( 'NONE', *, *, #20573, .F. ) ;
#61381=CARTESIAN_POINT ( 'NONE',  ( 10.00000000000000000, -80.55351364060578589, -15.33399622253569028 ) ) ;
#61385=EDGE_CURVE ( 'NONE', #43844, #55291, #65650, .T. ) ;
#61389=ORIENTED_EDGE ( 'NONE', *, *, #33113, .F. ) ;
#61392=ORIENTED_EDGE ( 'NONE', *, *, #2194, .T. ) ;
#61396=EDGE_CURVE ( 'NONE', #35405, #34710, #66524, .T. ) ;
#61400=ORIENTED_EDGE ( 'NONE', *, *, #11520, .F. ) ;
#61410=VECTOR ( 'NONE', #3597, 1000.000000000000000 ) ;
#61418=CARTESIAN_POINT ( 'NONE',  ( 0.000000000000000000, 6.903761155838878061, -77.19088730480517313 ) ) ;
#61421=CARTESIAN_POINT ( 'NONE',  ( 10.00000000000000000, -75.11764819372149304, 2.946379043146075905 ) ) ;
#61423=DIRECTION ( 'NONE',  ( -1.000000000000000000, -0.000000000000000000, -0.000000000000000000 ) ) ;
#61433=CARTESIAN_POINT ( 'NONE',  ( 0.000000000000000000, -59.46389618801928378, -49.70050353004953791 ) ) ;
#61438=DIRECTION ( 'NONE',  ( 0.000000000000000000, 0.4539904997395478592, -0.8910065241883673437 ) ) ;
#61446=CARTESIAN_POINT ( 'NONE',  ( 0.000000000000000000, 0.000000000000000000, 0.000000000000000000 ) ) ;
#61471=CYLINDRICAL_SURFACE ( 'NONE', #28080, 77.49899999999999523 ) ;
#61477=EDGE_CURVE ( 'NONE', #15522, #31227, #68063, .T. ) ;
#61480=EDGE_CURVE ( 'NONE', #33774, #44570, #17669, .T. ) ;
#61490=ORIENTED_EDGE ( 'NONE', *, *, #25299, .T. ) ;
#61506=FACE_OUTER_BOUND ( 'NONE', #2079, .T. ) ;
#61523=ORIENTED_EDGE ( 'NONE', *, *, #9221, .T. ) ;
#61525=CARTESIAN_POINT ( 'NONE',  ( 10.00000000000000000, 0.000000000000000000, 0.000000000000000000 ) ) ;
#61528=AXIS2_PLACEMENT_3D ( 'NONE', #52423, #63734, #23497 ) ;
#61540=DIRECTION ( 'NONE',  ( 0.000000000000000000, -6.938893903907229955E-15, 1.000000000000000000 ) ) ;
#61549=DIRECTION ( 'NONE',  ( 1.000000000000000000, 0.000000000000000000, -0.000000000000000000 ) ) ;
#61551=DIRECTION ( 'NONE',  ( -1.000000000000000000, 0.000000000000000000, 0.000000000000000000 ) ) ;
#61558=DIRECTION ( 'NONE',  ( 0.000000000000000000, 0.8526401643540935105, -0.5224985647159468005 ) ) ;
#61562=CARTESIAN_POINT ( 'NONE',  ( -10.00000000000000000, 0.000000000000000000, 0.000000000000000000 ) ) ;
#61577=AXIS2_PLACEMENT_3D ( 'NONE', #28037, #67905, #74277 ) ;
#61585=AXIS2_PLACEMENT_3D ( 'NONE', #67449, #44530, #9564 ) ;
#61611=ORIENTED_EDGE ( 'NONE', *, *, #67572, .T. ) ;
#61632=CARTESIAN_POINT ( 'NONE',  ( 0.000000000000000000, -71.27951684758005513, -30.41916302227188851 ) ) ;
#61639=DIRECTION ( 'NONE',  ( -1.000000000000000000, -0.000000000000000000, 0.000000000000000000 ) ) ;
#61642=CARTESIAN_POINT ( 'NONE',  ( 0.000000000000000000, 55.16347631943131802, -60.67117009219075641 ) ) ;
#61650=EDGE_CURVE ( 'NONE', #39929, #52914, #11583, .T. ) ;
#61653=LINE ( 'NONE', #21788, #33436 ) ;
#61657=VERTEX_POINT ( 'NONE', #74001 ) ;
#61658=ORIENTED_EDGE ( 'NONE', *, *, #28562, .T. ) ;
#61667=AXIS2_PLACEMENT_3D ( 'NONE', #59148, #65535, #54256 ) ;
#61671=VERTEX_POINT ( 'NONE', #68390 ) ;
#61672=DIRECTION ( 'NONE',  ( 0.000000000000000000, 0.8090169943749488946, -0.5877852522924712497 ) ) ;
#61683=ORIENTED_EDGE ( 'NONE', *, *, #73560, .F. ) ;
#61685=AXIS2_PLACEMENT_3D ( 'NONE', #8851, #67096, #50544 ) ;
#61688=EDGE_LOOP ( 'NONE', ( #58908, #55567, #58087, #14392 ) ) ;
#61697=ORIENTED_EDGE ( 'NONE', *, *, #7295, .F. ) ;
#61703=ORIENTED_EDGE ( 'NONE', *, *, #30146, .F. ) ;
#61712=AXIS2_PLACEMENT_3D ( 'NONE', #28486, #67242, #33380 ) ;
#61728=EDGE_CURVE ( 'NONE', #13032, #50832, #59684, .T. ) ;
#61735=CIRCLE ( 'NONE', #542, 31.99999999999998934 ) ;
#61743=VECTOR ( 'NONE', #39557, 1000.000000000000000 ) ;
#61750=DIRECTION ( 'NONE',  ( -1.000000000000000000, 0.000000000000000000, -0.000000000000000000 ) ) ;
#61767=ORIENTED_EDGE ( 'NONE', *, *, #25380, .F. ) ;
#61774=VECTOR ( 'NONE', #12240, 1000.000000000000000 ) ;
#61778=DIRECTION ( 'NONE',  ( 0.000000000000000000, 0.000000000000000000, 1.000000000000000000 ) ) ;
#61779=ORIENTED_EDGE ( 'NONE', *, *, #29001, .T. ) ;
#61781=EDGE_CURVE ( 'NONE', #39383, #74142, #47295, .T. ) ;
#61791=DIRECTION ( 'NONE',  ( 0.000000000000000000, -0.3826834323650969427, 0.9238795325112838519 ) ) ;
#61812=CARTESIAN_POINT ( 'NONE',  ( 10.00000000000000000, -40.65526001592664329, 71.21200624218782593 ) ) ;
#61831=CYLINDRICAL_SURFACE ( 'NONE', #19000, 31.99999999999999289 ) ;
#61852=ORIENTED_EDGE ( 'NONE', *, *, #61477, .T. ) ;
#61858=ORIENTED_EDGE ( 'NONE', *, *, #51088, .T. ) ;
#61860=EDGE_LOOP ( 'NONE', ( #44930, #14346, #45427, #71389 ) ) ;
#61867=EDGE_CURVE ( 'NONE', #8597, #4038, #63351, .T. ) ;
#61869=ORIENTED_EDGE ( 'NONE', *, *, #32981, .F. ) ;
#61876=EDGE_CURVE ( 'NONE', #63903, #28680, #72912, .T. ) ;
#61880=DIRECTION ( 'NONE',  ( -1.000000000000000000, -0.000000000000000000, -0.000000000000000000 ) ) ;
#61900=CARTESIAN_POINT ( 'NONE',  ( 0.000000000000000000, -15.33399622253540961, 80.55351364060584274 ) ) ;
#61901=ORIENTED_EDGE ( 'NONE', *, *, #25121, .T. ) ;
#61902=VERTEX_POINT ( 'NONE', #49131 ) ;
#61906=CARTESIAN_POINT ( 'NONE',  ( 10.00000000000000000, 0.000000000000000000, 0.000000000000000000 ) ) ;
#61909=EDGE_LOOP ( 'NONE', ( #19036, #71630, #18399, #14239 ) ) ;
#61916=EDGE_CURVE ( 'NONE', #7122, #55565, #34519, .T. ) ;
#61919=DIRECTION ( 'NONE',  ( 0.000000000000000000, 0.9723699203976773342, -0.2334453638559025601 ) ) ;
#61920=LINE ( 'NONE', #72791, #42488 ) ;
#61921=FACE_OUTER_BOUND ( 'NONE', #27062, .T. ) ;
#61926=FACE_OUTER_BOUND ( 'NONE', #43591, .T. ) ;
#61932=EDGE_LOOP ( 'NONE', ( #65540, #50847, #16185, #54651 ) ) ;
#61936=VERTEX_POINT ( 'NONE', #28050 ) ;
#61950=CARTESIAN_POINT ( 'NONE',  ( 10.00000000000000000, 65.58780272294129077, -36.73666225445822420 ) ) ;
#61965=VERTEX_POINT ( 'NONE', #16173 ) ;
#61978=EDGE_CURVE ( 'NONE', #6059, #16594, #28196, .T. ) ;
#61984=CYLINDRICAL_SURFACE ( 'NONE', #30005, 31.99999999999999289 ) ;
#61990=ORIENTED_EDGE ( 'NONE', *, *, #13660, .F. ) ;
#61992=EDGE_CURVE ( 'NONE', #60373, #71222, #36869, .T. ) ;
#62007=CARTESIAN_POINT ( 'NONE',  ( 10.00000000000000000, -12.93880638057369659, 76.41127070299266677 ) ) ;
#62008=DIRECTION ( 'NONE',  ( 0.000000000000000000, 0.000000000000000000, -1.000000000000000000 ) ) ;
#62010=CARTESIAN_POINT ( 'NONE',  ( 10.00000000000000000, -68.67312586194971402, -35.91791733033549860 ) ) ;
#62013=FACE_OUTER_BOUND ( 'NONE', #65384, .T. ) ;
#62017=CIRCLE ( 'NONE', #17559, 31.99999999999999289 ) ;
#62018=DIRECTION ( 'NONE',  ( -1.000000000000000000, 0.000000000000000000, -0.000000000000000000 ) ) ;
#62021=CYLINDRICAL_SURFACE ( 'NONE', #63520, 77.49899999999999523 ) ;
#62022=CIRCLE ( 'NONE', #23581, 31.99999999999999645 ) ;
#62028=VECTOR ( 'NONE', #7991, 1000.000000000000000 ) ;
#62030=DIRECTION ( 'NONE',  ( 0.000000000000000000, -0.4539904997395542430, 0.8910065241883641241 ) ) ;
#62048=DIRECTION ( 'NONE',  ( 1.000000000000000000, 0.000000000000000000, -0.000000000000000000 ) ) ;
#62049=EDGE_LOOP ( 'NONE', ( #3941, #53700, #67752, #21331 ) ) ;
#62051=CARTESIAN_POINT ( 'NONE',  ( 10.00000000000000000, 63.18004540533029001, 44.88180994100400767 ) ) ;
#62054=DIRECTION ( 'NONE',  ( 0.000000000000000000, 0.000000000000000000, 1.000000000000000000 ) ) ;
#62062=CIRCLE ( 'NONE', #66831, 77.49899999999999523 ) ;
#62063=ORIENTED_EDGE ( 'NONE', *, *, #72382, .F. ) ;
#62079=ORIENTED_EDGE ( 'NONE', *, *, #73226, .F. ) ;
#62099=ORIENTED_EDGE ( 'NONE', *, *, #10580, .F. ) ;
#62123=ORIENTED_EDGE ( 'NONE', *, *, #35476, .F. ) ;
#62124=CARTESIAN_POINT ( 'NONE',  ( 10.00000000000000000, -75.16055320797016748, -18.89407956138335365 ) ) ;
#62125=DIRECTION ( 'NONE',  ( 0.000000000000000000, 0.000000000000000000, 1.000000000000000000 ) ) ;
#62129=VERTEX_POINT ( 'NONE', #52236 ) ;
#62131=ADVANCED_FACE ( 'NONE', ( #6033 ), #19131, .T. ) ;
#62146=DIRECTION ( 'NONE',  ( 0.000000000000000000, 0.000000000000000000, 1.000000000000000000 ) ) ;
#62155=LINE ( 'NONE', #11018, #3003 ) ;
#62158=DIRECTION ( 'NONE',  ( -1.000000000000000000, 0.000000000000000000, -0.000000000000000000 ) ) ;
#62163=ADVANCED_FACE ( 'NONE', ( #6749 ), #24053, .T. ) ;
#62169=CIRCLE ( 'NONE', #22555, 82.00000000000000000 ) ;
#62170=CARTESIAN_POINT ( 'NONE',  ( 10.00000000000000000, 0.000000000000000000, 0.000000000000000000 ) ) ;
#62171=CARTESIAN_POINT ( 'NONE',  ( 10.00000000000000000, 74.18225833017889670, 34.94270380257666631 ) ) ;
#62178=DIRECTION ( 'NONE',  ( -1.000000000000000000, 0.000000000000000000, -0.000000000000000000 ) ) ;
#62189=DIRECTION ( 'NONE',  ( 0.000000000000000000, -0.9876883405951393247, 0.1564344650402207382 ) ) ;
#62194=AXIS2_PLACEMENT_3D ( 'NONE', #59270, #7764, #29939 ) ;
#62202=AXIS2_PLACEMENT_3D ( 'NONE', #30930, #53878, #43720 ) ;
#62212=CARTESIAN_POINT ( 'NONE',  ( 10.00000000000000000, -59.46389618801999433, 49.70050353004867816 ) ) ;
#62218=CARTESIAN_POINT ( 'NONE',  ( 5.000000000000000000, -63.97538442413390669, -51.29473840253292849 ) ) ;
#62223=ORIENTED_EDGE ( 'NONE', *, *, #71700, .F. ) ;
#62233=ORIENTED_EDGE ( 'NONE', *, *, #4703, .T. ) ;
#62234=CARTESIAN_POINT ( 'NONE',  ( 0.000000000000000000, -2.956366410621191765, 75.11725578898467859 ) ) ;
#62235=FACE_OUTER_BOUND ( 'NONE', #51400, .T. ) ;
#62242=ORIENTED_EDGE ( 'NONE', *, *, #44509, .F. ) ;
#62245=EDGE_CURVE ( 'NONE', #72136, #11546, #62169, .T. ) ;
#62247=CIRCLE ( 'NONE', #53801, 82.00000000000000000 ) ;
#62249=CARTESIAN_POINT ( 'NONE',  ( 0.000000000000000000, 0.000000000000000000, 0.000000000000000000 ) ) ;
#62251=DIRECTION ( 'NONE',  ( -1.000000000000000000, 0.000000000000000000, 0.000000000000000000 ) ) ;
#62255=ORIENTED_EDGE ( 'NONE', *, *, #23636, .T. ) ;
#62259=EDGE_CURVE ( 'NONE', #4552, #961, #48944, .T. ) ;
#62260=VERTEX_POINT ( 'NONE', #19863 ) ;
#62273=DIRECTION ( 'NONE',  ( -1.000000000000000000, -0.000000000000000000, -0.000000000000000000 ) ) ;
#62275=ORIENTED_EDGE ( 'NONE', *, *, #15956, .F. ) ;
#62281=ORIENTED_EDGE ( 'NONE', *, *, #68768, .F. ) ;
#62289=AXIS2_PLACEMENT_3D ( 'NONE', #9101, #50434, #38790 ) ;
#62290=DIRECTION ( 'NONE',  ( -1.000000000000000000, 0.000000000000000000, -0.000000000000000000 ) ) ;
#62294=DIRECTION ( 'NONE',  ( -1.000000000000000000, 0.000000000000000000, -0.000000000000000000 ) ) ;
#62304=CIRCLE ( 'NONE', #17905, 31.99999999999998934 ) ;
#62326=AXIS2_PLACEMENT_3D ( 'NONE', #63281, #27180, #62546 ) ;
#62328=DIRECTION ( 'NONE',  ( -1.000000000000000000, 0.000000000000000000, 0.000000000000000000 ) ) ;
#62336=AXIS2_PLACEMENT_3D ( 'NONE', #50353, #4145, #72166 ) ;
#62348=DIRECTION ( 'NONE',  ( 1.000000000000000000, 0.000000000000000000, -0.000000000000000000 ) ) ;
#62356=DIRECTION ( 'NONE',  ( 0.000000000000000000, 0.9876883405951371042, 0.1564344650402346437 ) ) ;
#62359=ORIENTED_EDGE ( 'NONE', *, *, #3828, .F. ) ;
#62365=CARTESIAN_POINT ( 'NONE',  ( 10.00000000000000000, -59.03342792756231461, -46.54456581323868392 ) ) ;
#62392=CARTESIAN_POINT ( 'NONE',  ( 0.000000000000000000, 0.000000000000000000, 0.000000000000000000 ) ) ;
#62394=CARTESIAN_POINT ( 'NONE',  ( 0.000000000000000000, 68.26794271651307611, -31.47745569255064169 ) ) ;
#62398=CARTESIAN_POINT ( 'NONE',  ( 10.00000000000000000, -0.8261519478436571973, 77.49459641780886443 ) ) ;
#62404=CIRCLE ( 'NONE', #40763, 77.49900000000000944 ) ;
#62407=ADVANCED_FACE ( 'NONE', ( #44677 ), #38277, .T. ) ;
#62433=CARTESIAN_POINT ( 'NONE',  ( 10.00000000000000000, 35.91791733033475253, 68.67312586195009771 ) ) ;
#62434=VERTEX_POINT ( 'NONE', #16087 ) ;
#62441=ORIENTED_EDGE ( 'NONE', *, *, #58926, .T. ) ;
#62450=ORIENTED_EDGE ( 'NONE', *, *, #47022, .T. ) ;
#62455=AXIS2_PLACEMENT_3D ( 'NONE', #32643, #55589, #8620 ) ;
#62460=ORIENTED_EDGE ( 'NONE', *, *, #43896, .F. ) ;
#62468=DIRECTION ( 'NONE',  ( 1.000000000000000000, -0.000000000000000000, -0.000000000000000000 ) ) ;
#62474=CIRCLE ( 'NONE', #52849, 77.49900000000002365 ) ;
#62478=AXIS2_PLACEMENT_3D ( 'NONE', #24874, #15065, #54925 ) ;
#62480=CARTESIAN_POINT ( 'NONE',  ( 0.000000000000000000, -76.41127070299262414, -12.93880638057396304 ) ) ;
#62484=CARTESIAN_POINT ( 'NONE',  ( 0.000000000000000000, -67.80270845531921964, 46.11716303203163392 ) ) ;
#62491=DIRECTION ( 'NONE',  ( -1.000000000000000000, 0.000000000000000000, 0.000000000000000000 ) ) ;
#62495=FACE_OUTER_BOUND ( 'NONE', #38951, .T. ) ;
#62497=ADVANCED_FACE ( 'NONE', ( #73962 ), #9706, .T. ) ;
#62502=AXIS2_PLACEMENT_3D ( 'NONE', #44722, #2030, #2770 ) ;
#62503=DIRECTION ( 'NONE',  ( -1.000000000000000000, 0.000000000000000000, 0.000000000000000000 ) ) ;
#62505=VECTOR ( 'NONE', #29970, 1000.000000000000000 ) ;
#62507=ORIENTED_EDGE ( 'NONE', *, *, #19229, .F. ) ;
#62510=EDGE_CURVE ( 'NONE', #58494, #40236, #38162, .T. ) ;
#62512=VERTEX_POINT ( 'NONE', #1440 ) ;
#62518=AXIS2_PLACEMENT_3D ( 'NONE', #15099, #49674, #21101 ) ;
#62522=AXIS2_PLACEMENT_3D ( 'NONE', #32729, #55310, #61334 ) ;
#62527=VERTEX_POINT ( 'NONE', #6304 ) ;
#62542=LINE ( 'NONE', #6855, #43690 ) ;
#62546=DIRECTION ( 'NONE',  ( 0.000000000000000000, 0.000000000000000000, 1.000000000000000000 ) ) ;
#62555=CARTESIAN_POINT ( 'NONE',  ( 10.00000000000000000, 8.840884882376133902, -74.65374052328640175 ) ) ;
#62586=FACE_OUTER_BOUND ( 'NONE', #3381, .T. ) ;
#62596=CARTESIAN_POINT ( 'NONE',  ( 0.000000000000000000, 72.35432306680485226, -20.40083707022909110 ) ) ;
#62606=VERTEX_POINT ( 'NONE', #41605 ) ;
#62618=CARTESIAN_POINT ( 'NONE',  ( 10.00000000000000000, -44.88180994100421373, 63.18004540533011948 ) ) ;
#62640=ORIENTED_EDGE ( 'NONE', *, *, #10073, .T. ) ;
#62658=EDGE_LOOP ( 'NONE', ( #6836, #32091, #49985, #69058 ) ) ;
#62662=DIRECTION ( 'NONE',  ( -1.000000000000000000, 0.000000000000000000, 0.000000000000000000 ) ) ;
#62668=ORIENTED_EDGE ( 'NONE', *, *, #15776, .T. ) ;
#62672=EDGE_CURVE ( 'NONE', #65467, #29404, #20143, .T. ) ;
#62681=LINE ( 'NONE', #11155, #52933 ) ;
#62696=EDGE_CURVE ( 'NONE', #28018, #39348, #15398, .T. ) ;
#62697=EDGE_CURVE ( 'NONE', #16594, #43494, #65811, .T. ) ;
#62699=CIRCLE ( 'NONE', #36254, 82.00000000000000000 ) ;
#62702=ORIENTED_EDGE ( 'NONE', *, *, #43376, .T. ) ;
#62703=CARTESIAN_POINT ( 'NONE',  ( 10.00000000000000000, 0.000000000000000000, 0.000000000000000000 ) ) ;
#62712=DIRECTION ( 'NONE',  ( -1.000000000000000000, 0.000000000000000000, 0.000000000000000000 ) ) ;
#62715=CARTESIAN_POINT ( 'NONE',  ( 5.000000000000002665, 10.30890764327382847, 81.34940948281339956 ) ) ;
#62726=DIRECTION ( 'NONE',  ( 0.000000000000000000, 0.000000000000000000, 1.000000000000000000 ) ) ;
#62727=CARTESIAN_POINT ( 'NONE',  ( 0.000000000000000000, 75.54627589209970040, -17.28742895386005785 ) ) ;
#62732=AXIS2_PLACEMENT_3D ( 'NONE', #67263, #15756, #56742 ) ;
#62737=AXIS2_PLACEMENT_3D ( 'NONE', #50219, #20919, #50599 ) ;
#62744=ADVANCED_FACE ( 'NONE', ( #9240 ), #59277, .T. ) ;
#62760=ORIENTED_EDGE ( 'NONE', *, *, #40011, .T. ) ;
#62780=CARTESIAN_POINT ( 'NONE',  ( 10.00000000000000000, 0.000000000000000000, 0.000000000000000000 ) ) ;
#62785=EDGE_CURVE ( 'NONE', #52790, #3338, #56609, .T. ) ;
#62797=VECTOR ( 'NONE', #44149, 1000.000000000000000 ) ;
#62808=EDGE_LOOP ( 'NONE', ( #69559, #23690, #10363, #5051 ) ) ;
#62809=DIRECTION ( 'NONE',  ( 0.000000000000000000, 0.000000000000000000, 1.000000000000000000 ) ) ;
#62810=ORIENTED_EDGE ( 'NONE', *, *, #24929, .F. ) ;
#62822=EDGE_CURVE ( 'NONE', #35621, #2136, #27648, .T. ) ;
#62836=LINE ( 'NONE', #27465, #5926 ) ;
#62843=DIRECTION ( 'NONE',  ( -1.000000000000000000, 0.000000000000000000, 0.000000000000000000 ) ) ;
#62847=AXIS2_PLACEMENT_3D ( 'NONE', #33142, #27883, #72613 ) ;
#62853=CARTESIAN_POINT ( 'NONE',  ( 10.00000000000000000, 29.01471420065674423, -76.69515212745983490 ) ) ;
#62857=FACE_OUTER_BOUND ( 'NONE', #67772, .T. ) ;
#62877=VERTEX_POINT ( 'NONE', #66763 ) ;
#62880=CARTESIAN_POINT ( 'NONE',  ( 10.00000000000000000, 0.000000000000000000, 0.000000000000000000 ) ) ;
#62893=AXIS2_PLACEMENT_3D ( 'NONE', #37967, #10794, #28820 ) ;
#62901=VECTOR ( 'NONE', #32764, 1000.000000000000000 ) ;
#62903=EDGE_LOOP ( 'NONE', ( #30995, #4822, #8683, #39935 ) ) ;
#62907=ORIENTED_EDGE ( 'NONE', *, *, #61371, .T. ) ;
#62912=DIRECTION ( 'NONE',  ( -1.000000000000000000, -0.000000000000000000, -0.000000000000000000 ) ) ;
#62914=VERTEX_POINT ( 'NONE', #52809 ) ;
#62915=CIRCLE ( 'NONE', #47277, 82.00000000000000000 ) ;
#62916=EDGE_CURVE ( 'NONE', #61359, #70648, #35846, .T. ) ;
#62926=CARTESIAN_POINT ( 'NONE',  ( 10.00000000000000000, -21.60688246758529019, -79.10210256391388839 ) ) ;
#62934=ORIENTED_EDGE ( 'NONE', *, *, #27334, .F. ) ;
#62963=VECTOR ( 'NONE', #2126, 1000.000000000000000 ) ;
#62979=ORIENTED_EDGE ( 'NONE', *, *, #9579, .F. ) ;
#62981=CIRCLE ( 'NONE', #5339, 31.99999999999999289 ) ;
#62982=DIRECTION ( 'NONE',  ( 0.000000000000000000, 0.000000000000000000, 1.000000000000000000 ) ) ;
#62987=AXIS2_PLACEMENT_3D ( 'NONE', #14228, #25884, #43575 ) ;
#62996=ORIENTED_EDGE ( 'NONE', *, *, #19114, .T. ) ;
#63002=VERTEX_POINT ( 'NONE', #22769 ) ;
#63006=ORIENTED_EDGE ( 'NONE', *, *, #69258, .F. ) ;
#63011=CARTESIAN_POINT ( 'NONE',  ( 0.000000000000000000, 71.91182617369230456, -28.89263327155667938 ) ) ;
#63017=VERTEX_POINT ( 'NONE', #57714 ) ;
#63020=ORIENTED_EDGE ( 'NONE', *, *, #3828, .T. ) ;
#63026=DIRECTION ( 'NONE',  ( -1.000000000000000000, -0.000000000000000000, -0.000000000000000000 ) ) ;
#63027=CIRCLE ( 'NONE', #34179, 82.00000000000000000 ) ;
#63030=DIRECTION ( 'NONE',  ( 0.000000000000000000, 0.000000000000000000, -1.000000000000000000 ) ) ;
#63033=VERTEX_POINT ( 'NONE', #58821 ) ;
#63034=EDGE_LOOP ( 'NONE', ( #40590, #16394, #53298, #45077 ) ) ;
#63050=DIRECTION ( 'NONE',  ( -1.000000000000000000, 0.000000000000000000, -0.000000000000000000 ) ) ;
#63051=CARTESIAN_POINT ( 'NONE',  ( 0.000000000000000000, 46.53671651293948486, 59.03961581697416250 ) ) ;
#63063=AXIS2_PLACEMENT_3D ( 'NONE', #52579, #16614, #45203 ) ;
#63064=VECTOR ( 'NONE', #6348, 1000.000000000000000 ) ;
#63066=EDGE_CURVE ( 'NONE', #27978, #39783, #5888, .T. ) ;
#63089=VERTEX_POINT ( 'NONE', #47901 ) ;
#63094=CARTESIAN_POINT ( 'NONE',  ( -10.00000000000000000, 0.000000000000000000, 0.000000000000000000 ) ) ;
#63099=DIRECTION ( 'NONE',  ( 0.000000000000000000, -0.6494480483301903195, 0.7604059656000252687 ) ) ;
#63101=DIRECTION ( 'NONE',  ( 0.000000000000000000, 0.000000000000000000, 1.000000000000000000 ) ) ;
#63108=VECTOR ( 'NONE', #27086, 1000.000000000000000 ) ;
#63114=DIRECTION ( 'NONE',  ( -1.000000000000000000, 0.000000000000000000, 0.000000000000000000 ) ) ;
#63120=VECTOR ( 'NONE', #29522, 1000.000000000000000 ) ;
#63129=LINE ( 'NONE', #57466, #13424 ) ;
#63133=CIRCLE ( 'NONE', #30663, 77.49899999999999523 ) ;
#63149=CARTESIAN_POINT ( 'NONE',  ( 10.00000000000000000, 0.000000000000000000, 0.000000000000000000 ) ) ;
#63154=CIRCLE ( 'NONE', #22295, 77.49900000000000944 ) ;
#63161=ORIENTED_EDGE ( 'NONE', *, *, #46415, .F. ) ;
#63162=DIRECTION ( 'NONE',  ( 0.000000000000000000, 0.000000000000000000, 1.000000000000000000 ) ) ;
#63163=ORIENTED_EDGE ( 'NONE', *, *, #11347, .T. ) ;
#63174=CARTESIAN_POINT ( 'NONE',  ( -10.00000000000000000, 0.000000000000000000, 0.000000000000000000 ) ) ;
#63182=DIRECTION ( 'NONE',  ( 0.000000000000000000, 0.000000000000000000, -1.000000000000000000 ) ) ;
#63186=ORIENTED_EDGE ( 'NONE', *, *, #38465, .F. ) ;
#63188=CARTESIAN_POINT ( 'NONE',  ( 10.00000000000000000, 71.27951684758069462, -30.41916302227035729 ) ) ;
#63195=DIRECTION ( 'NONE',  ( -1.000000000000000000, -0.000000000000000000, -0.000000000000000000 ) ) ;
#63204=VERTEX_POINT ( 'NONE', #61053 ) ;
#63207=CARTESIAN_POINT ( 'NONE',  ( 10.00000000000000000, 0.000000000000000000, 0.000000000000000000 ) ) ;
#63214=CIRCLE ( 'NONE', #46397, 32.00000000000000000 ) ;
#63215=CARTESIAN_POINT ( 'NONE',  ( 10.00000000000000000, -77.49459641780886443, -0.8261519478439277586 ) ) ;
#63226=LINE ( 'NONE', #28990, #38226 ) ;
#63241=EDGE_CURVE ( 'NONE', #48030, #70758, #56537, .T. ) ;
#63253=FACE_OUTER_BOUND ( 'NONE', #49576, .T. ) ;
#63255=CYLINDRICAL_SURFACE ( 'NONE', #21625, 77.49899999999999523 ) ;
#63257=CARTESIAN_POINT ( 'NONE',  ( 10.00000000000000000, -36.72794159290197769, -65.59268652807249111 ) ) ;
#63259=AXIS2_PLACEMENT_3D ( 'NONE', #39732, #27695, #11152 ) ;
#63262=EDGE_CURVE ( 'NONE', #55165, #15320, #21557, .T. ) ;
#63268=ORIENTED_EDGE ( 'NONE', *, *, #330, .F. ) ;
#63269=ORIENTED_EDGE ( 'NONE', *, *, #65470, .T. ) ;
#63271=ORIENTED_EDGE ( 'NONE', *, *, #12214, .T. ) ;
#63281=CARTESIAN_POINT ( 'NONE',  ( 10.00000000000000000, 74.65491531819118620, -8.830959090342659579 ) ) ;
#63292=DIRECTION ( 'NONE',  ( -1.000000000000000000, -0.000000000000000000, -0.000000000000000000 ) ) ;
#63313=CARTESIAN_POINT ( 'NONE',  ( 5.000000000000002665, -81.50828551894234408, 8.966570791700407383 ) ) ;
#63316=DIRECTION ( 'NONE',  ( -1.000000000000000000, -0.000000000000000000, -0.000000000000000000 ) ) ;
#63324=EDGE_CURVE ( 'NONE', #60073, #59929, #45486, .T. ) ;
#63332=EDGE_CURVE ( 'NONE', #64894, #36430, #51531, .T. ) ;
#63336=FACE_OUTER_BOUND ( 'NONE', #58550, .T. ) ;
#63338=EDGE_CURVE ( 'NONE', #16918, #39783, #27528, .T. ) ;
#63343=VERTEX_POINT ( 'NONE', #45639 ) ;
#63346=EDGE_CURVE ( 'NONE', #33464, #66997, #34328, .T. ) ;
#63351=CIRCLE ( 'NONE', #44130, 82.00000000000000000 ) ;
#63360=CARTESIAN_POINT ( 'NONE',  ( 10.00000000000000000, 0.000000000000000000, 0.000000000000000000 ) ) ;
#63363=CIRCLE ( 'NONE', #21309, 31.99999999999999289 ) ;
#63367=ORIENTED_EDGE ( 'NONE', *, *, #14072, .T. ) ;
#63389=AXIS2_PLACEMENT_3D ( 'NONE', #24196, #48229, #47849 ) ;
#63405=CARTESIAN_POINT ( 'NONE',  ( 10.00000000000000000, 75.54627589209943039, 17.28742895386112721 ) ) ;
#63407=ADVANCED_FACE ( 'NONE', ( #64393 ), #46728, .T. ) ;
#63414=FACE_OUTER_BOUND ( 'NONE', #49629, .T. ) ;
#63425=DIRECTION ( 'NONE',  ( -1.000000000000000000, 0.000000000000000000, 0.000000000000000000 ) ) ;
#63429=CARTESIAN_POINT ( 'NONE',  ( 0.000000000000000000, 0.000000000000000000, 0.000000000000000000 ) ) ;
#63435=AXIS2_PLACEMENT_3D ( 'NONE', #59419, #41386, #64691 ) ;
#63450=DIRECTION ( 'NONE',  ( 0.000000000000000000, 0.000000000000000000, 1.000000000000000000 ) ) ;
#63466=AXIS2_PLACEMENT_3D ( 'NONE', #31390, #2864, #25760 ) ;
#63467=CARTESIAN_POINT ( 'NONE',  ( 0.000000000000000000, 0.000000000000000000, 0.000000000000000000 ) ) ;
#63474=ORIENTED_EDGE ( 'NONE', *, *, #64795, .F. ) ;
#63483=CARTESIAN_POINT ( 'NONE',  ( 10.00000000000000000, 72.35432306680485226, -20.40083707022909110 ) ) ;
#63487=VECTOR ( 'NONE', #6549, 1000.000000000000000 ) ;
#63507=LINE ( 'NONE', #5628, #204 ) ;
#63508=CARTESIAN_POINT ( 'NONE',  ( 10.00000000000000000, 0.000000000000000000, 0.000000000000000000 ) ) ;
#63510=PLANE ( 'NONE',  #29636 ) ;
#63519=AXIS2_PLACEMENT_3D ( 'NONE', #23127, #69711, #64450 ) ;
#63520=AXIS2_PLACEMENT_3D ( 'NONE', #10499, #49603, #67282 ) ;
#63539=CIRCLE ( 'NONE', #11889, 31.99999999999998224 ) ;
#63547=DIRECTION ( 'NONE',  ( 1.000000000000000000, 0.000000000000000000, 0.000000000000000000 ) ) ;
#63548=ORIENTED_EDGE ( 'NONE', *, *, #47599, .F. ) ;
#63550=FACE_OUTER_BOUND ( 'NONE', #23137, .T. ) ;
#63553=EDGE_LOOP ( 'NONE', ( #41462, #7743, #4259, #61523 ) ) ;
#63556=DIRECTION ( 'NONE',  ( -1.000000000000000000, -0.000000000000000000, -0.000000000000000000 ) ) ;
#63559=EDGE_LOOP ( 'NONE', ( #73191, #33757, #53604, #69541 ) ) ;
#63571=DIRECTION ( 'NONE',  ( -1.000000000000000000, -0.000000000000000000, 0.000000000000000000 ) ) ;
#63572=DIRECTION ( 'NONE',  ( -1.000000000000000000, -0.000000000000000000, -0.000000000000000000 ) ) ;
#63587=CARTESIAN_POINT ( 'NONE',  ( 10.00000000000000000, -74.65491531819111515, -8.830959090343204920 ) ) ;
#63590=CARTESIAN_POINT ( 'NONE',  ( 10.00000000000000000, 68.26794271651307611, -31.47745569255064169 ) ) ;
#63602=CARTESIAN_POINT ( 'NONE',  ( 10.00000000000000000, 0.000000000000000000, 0.000000000000000000 ) ) ;
#63605=VECTOR ( 'NONE', #41671, 1000.000000000000000 ) ;
#63606=CARTESIAN_POINT ( 'NONE',  ( 10.00000000000000000, 74.65374052328648702, 8.840884882375350529 ) ) ;
#63607=ORIENTED_EDGE ( 'NONE', *, *, #40080, .F. ) ;
#63614=EDGE_CURVE ( 'NONE', #4987, #5465, #46765, .T. ) ;
#63621=AXIS2_PLACEMENT_3D ( 'NONE', #37942, #62662, #55601 ) ;
#63630=CARTESIAN_POINT ( 'NONE',  ( 10.00000000000000000, -24.73286445877653961, -73.44644590900085745 ) ) ;
#63636=DIRECTION ( 'NONE',  ( -1.000000000000000000, -0.000000000000000000, 0.000000000000000000 ) ) ;
#63638=ORIENTED_EDGE ( 'NONE', *, *, #46042, .T. ) ;
#63649=DIRECTION ( 'NONE',  ( -1.000000000000000000, -0.000000000000000000, -0.000000000000000000 ) ) ;
#63661=CARTESIAN_POINT ( 'NONE',  ( 10.00000000000000000, -14.66109333815410487, -73.73191006444587003 ) ) ;
#63667=CARTESIAN_POINT ( 'NONE',  ( 0.000000000000000000, 16.65972982745046238, -80.28980883073738539 ) ) ;
#63674=ORIENTED_EDGE ( 'NONE', *, *, #19272, .F. ) ;
#63680=CARTESIAN_POINT ( 'NONE',  ( -10.00000000000000000, 0.000000000000000000, 0.000000000000000000 ) ) ;
#63682=CARTESIAN_POINT ( 'NONE',  ( 10.00000000000000000, 0.000000000000000000, 0.000000000000000000 ) ) ;
#63684=VERTEX_POINT ( 'NONE', #60957 ) ;
#63688=AXIS2_PLACEMENT_3D ( 'NONE', #40844, #13360, #70125 ) ;
#63689=DIRECTION ( 'NONE',  ( -1.000000000000000000, 0.000000000000000000, 0.000000000000000000 ) ) ;
#63690=CARTESIAN_POINT ( 'NONE',  ( 0.000000000000000000, 41.76106447765489094, 62.50884508063442269 ) ) ;
#63713=ORIENTED_EDGE ( 'NONE', *, *, #72299, .F. ) ;
#63729=VECTOR ( 'NONE', #73819, 1000.000000000000000 ) ;
#63734=DIRECTION ( 'NONE',  ( -1.000000000000000000, 0.000000000000000000, -0.000000000000000000 ) ) ;
#63763=EDGE_CURVE ( 'NONE', #16380, #28262, #45909, .T. ) ;
#63767=DIRECTION ( 'NONE',  ( 0.000000000000000000, 0.000000000000000000, 1.000000000000000000 ) ) ;
#63772=ORIENTED_EDGE ( 'NONE', *, *, #8569, .T. ) ;
#63784=ADVANCED_FACE ( 'NONE', ( #6062 ), #51901, .T. ) ;
#63786=CARTESIAN_POINT ( 'NONE',  ( 10.00000000000000000, 0.000000000000000000, 0.000000000000000000 ) ) ;
#63791=CIRCLE ( 'NONE', #46971, 31.99999999999999289 ) ;
#63801=CARTESIAN_POINT ( 'NONE',  ( 10.00000000000000000, 0.000000000000000000, 0.000000000000000000 ) ) ;
#63811=DIRECTION ( 'NONE',  ( 0.000000000000000000, 0.000000000000000000, 1.000000000000000000 ) ) ;
#63822=EDGE_CURVE ( 'NONE', #70403, #4935, #61192, .T. ) ;
#63829=ORIENTED_EDGE ( 'NONE', *, *, #71563, .T. ) ;
#63835=ORIENTED_EDGE ( 'NONE', *, *, #68531, .F. ) ;
#63840=VECTOR ( 'NONE', #68558, 1000.000000000000000 ) ;
#63847=AXIS2_PLACEMENT_3D ( 'NONE', #50798, #44443, #16221 ) ;
#63850=ORIENTED_EDGE ( 'NONE', *, *, #18163, .F. ) ;
#63853=ORIENTED_EDGE ( 'NONE', *, *, #28185, .F. ) ;
#63857=ADVANCED_FACE ( 'NONE', ( #39894 ), #54131, .T. ) ;
#63866=DIRECTION ( 'NONE',  ( 0.000000000000000000, 0.000000000000000000, 1.000000000000000000 ) ) ;
#63869=DIRECTION ( 'NONE',  ( 0.000000000000000000, 0.5224985647159441360, 0.8526401643540952868 ) ) ;
#63876=EDGE_CURVE ( 'NONE', #66429, #31341, #14387, .T. ) ;
#63877=CARTESIAN_POINT ( 'NONE',  ( 0.000000000000000000, 39.47590169984944453, -71.87247863392373404 ) ) ;
#63889=DIRECTION ( 'NONE',  ( -1.000000000000000000, 0.000000000000000000, -0.000000000000000000 ) ) ;
#63896=ORIENTED_EDGE ( 'NONE', *, *, #73133, .F. ) ;
#63900=VERTEX_POINT ( 'NONE', #8254 ) ;
#63903=VERTEX_POINT ( 'NONE', #13149 ) ;
#63906=CIRCLE ( 'NONE', #56727, 82.00000000000000000 ) ;
#63912=DIRECTION ( 'NONE',  ( 0.000000000000000000, 0.000000000000000000, 1.000000000000000000 ) ) ;
#63920=ORIENTED_EDGE ( 'NONE', *, *, #73737, .T. ) ;
#63936=VERTEX_POINT ( 'NONE', #69921 ) ;
#63940=FACE_OUTER_BOUND ( 'NONE', #22194, .T. ) ;
#63942=DIRECTION ( 'NONE',  ( 0.000000000000000000, 0.000000000000000000, -1.000000000000000000 ) ) ;
#63947=DIRECTION ( 'NONE',  ( -1.000000000000000000, 0.000000000000000000, 0.000000000000000000 ) ) ;
#63948=CIRCLE ( 'NONE', #36287, 32.00000000000000000 ) ;
#63964=DIRECTION ( 'NONE',  ( -1.000000000000000000, -0.000000000000000000, 0.000000000000000000 ) ) ;
#63987=ORIENTED_EDGE ( 'NONE', *, *, #34047, .T. ) ;
#63998=CARTESIAN_POINT ( 'NONE',  ( 10.00000000000000000, 20.41045688087824317, 72.35160999960824313 ) ) ;
#63999=CARTESIAN_POINT ( 'NONE',  ( 0.000000000000000000, 0.000000000000000000, 0.000000000000000000 ) ) ;
#64003=EDGE_LOOP ( 'NONE', ( #1743, #29357, #42273, #16536 ) ) ;
#64005=ORIENTED_EDGE ( 'NONE', *, *, #23352, .T. ) ;
#64006=EDGE_CURVE ( 'NONE', #36499, #44699, #11977, .T. ) ;
#64008=CIRCLE ( 'NONE', #73587, 77.49899999999999523 ) ;
#64037=ORIENTED_EDGE ( 'NONE', *, *, #5001, .T. ) ;
#64054=AXIS2_PLACEMENT_3D ( 'NONE', #26051, #15511, #14770 ) ;
#64067=DIRECTION ( 'NONE',  ( 0.000000000000000000, 0.9969173337331276308, 0.07845909572784873220 ) ) ;
#64069=AXIS2_PLACEMENT_3D ( 'NONE', #73178, #21679, #12252 ) ;
#64075=CARTESIAN_POINT ( 'NONE',  ( 0.000000000000000000, 67.80270845531956070, -46.11716303203112943 ) ) ;
#64077=CARTESIAN_POINT ( 'NONE',  ( 10.00000000000000000, -33.71516098798792171, 74.74816331893418919 ) ) ;
#64081=CARTESIAN_POINT ( 'NONE',  ( 0.000000000000000000, 16.65972982744934683, 80.28980883073764119 ) ) ;
#64089=EDGE_LOOP ( 'NONE', ( #32831, #54460, #44179, #57128 ) ) ;
#64108=ORIENTED_EDGE ( 'NONE', *, *, #47430, .T. ) ;
#64141=CARTESIAN_POINT ( 'NONE',  ( 10.00000000000000000, 56.15606465354958488, 59.75363087400094031 ) ) ;
#64143=DIRECTION ( 'NONE',  ( -1.000000000000000000, 0.000000000000000000, 0.000000000000000000 ) ) ;
#64144=DIRECTION ( 'NONE',  ( 0.000000000000000000, 0.000000000000000000, 1.000000000000000000 ) ) ;
#64160=VECTOR ( 'NONE', #65817, 1000.000000000000000 ) ;
#64171=EDGE_CURVE ( 'NONE', #59929, #19226, #25781, .T. ) ;
#64175=FACE_OUTER_BOUND ( 'NONE', #14343, .T. ) ;
#64178=CYLINDRICAL_SURFACE ( 'NONE', #15910, 31.99999999999999289 ) ;
#64180=CARTESIAN_POINT ( 'NONE',  ( 10.00000000000000000, -27.74655509720723501, 77.16300072079651784 ) ) ;
#64193=EDGE_CURVE ( 'NONE', #17740, #40404, #25232, .T. ) ;
#64198=CARTESIAN_POINT ( 'NONE',  ( 10.00000000000000000, 73.72996012237440766, 14.67089635893739619 ) ) ;
#64203=DIRECTION ( 'NONE',  ( 0.000000000000000000, 0.5877852522924742473, -0.8090169943749466741 ) ) ;
#64210=ADVANCED_FACE ( 'NONE', ( #15520 ), #38458, .T. ) ;
#64212=CIRCLE ( 'NONE', #62987, 31.99999999999999289 ) ;
#64222=DIRECTION ( 'NONE',  ( -1.000000000000000000, 0.000000000000000000, -0.000000000000000000 ) ) ;
#64224=ORIENTED_EDGE ( 'NONE', *, *, #54508, .F. ) ;
#64234=DIRECTION ( 'NONE',  ( 0.000000000000000000, 0.000000000000000000, 1.000000000000000000 ) ) ;
#64240=VECTOR ( 'NONE', #70464, 1000.000000000000000 ) ;
#64248=ORIENTED_EDGE ( 'NONE', *, *, #20611, .F. ) ;
#64259=DIRECTION ( 'NONE',  ( 0.000000000000000000, 0.000000000000000000, 1.000000000000000000 ) ) ;
#64284=ORIENTED_EDGE ( 'NONE', *, *, #49695, .F. ) ;
#64287=ORIENTED_EDGE ( 'NONE', *, *, #19019, .T. ) ;
#64288=AXIS2_PLACEMENT_3D ( 'NONE', #11755, #35800, #47108 ) ;
#64292=DIRECTION ( 'NONE',  ( -1.000000000000000000, 0.000000000000000000, 0.000000000000000000 ) ) ;
#64293=CARTESIAN_POINT ( 'NONE',  ( 10.00000000000000000, 0.000000000000000000, 0.000000000000000000 ) ) ;
#64296=VECTOR ( 'NONE', #70863, 1000.000000000000000 ) ;
#64312=AXIS2_PLACEMENT_3D ( 'NONE', #59195, #7686, #24974 ) ;
#64314=CARTESIAN_POINT ( 'NONE',  ( 10.00000000000000000, -59.75363087400034345, -56.15606465355021015 ) ) ;
#64322=AXIS2_PLACEMENT_3D ( 'NONE', #2836, #25727, #48664 ) ;
#64341=ADVANCED_FACE ( 'NONE', ( #56504 ), #63255, .T. ) ;
#64344=AXIS2_PLACEMENT_3D ( 'NONE', #29010, #22269, #62125 ) ;
#64349=ORIENTED_EDGE ( 'NONE', *, *, #44199, .T. ) ;
#64352=EDGE_CURVE ( 'NONE', #69125, #41920, #6044, .T. ) ;
#64362=VERTEX_POINT ( 'NONE', #68138 ) ;
#64364=CARTESIAN_POINT ( 'NONE',  ( -10.00000000000000000, 0.000000000000000000, 0.000000000000000000 ) ) ;
#64373=EDGE_LOOP ( 'NONE', ( #68087, #56879, #23830, #53126 ) ) ;
#64377=FACE_OUTER_BOUND ( 'NONE', #2703, .T. ) ;
#64384=DIRECTION ( 'NONE',  ( 1.000000000000000000, 0.000000000000000000, 0.000000000000000000 ) ) ;
#64387=VERTEX_POINT ( 'NONE', #20455 ) ;
#64393=FACE_OUTER_BOUND ( 'NONE', #64003, .T. ) ;
#64400=CARTESIAN_POINT ( 'NONE',  ( 10.00000000000000000, -39.47590169984896136, 71.87247863392398983 ) ) ;
#64403=ORIENTED_EDGE ( 'NONE', *, *, #67667, .F. ) ;
#64404=ORIENTED_EDGE ( 'NONE', *, *, #8133, .F. ) ;
#64410=EDGE_CURVE ( 'NONE', #70238, #22507, #25356, .T. ) ;
#64416=ADVANCED_FACE ( 'NONE', ( #26455 ), #66330, .T. ) ;
#64418=CARTESIAN_POINT ( 'NONE',  ( 10.00000000000000000, 0.000000000000000000, 0.000000000000000000 ) ) ;
#64432=CIRCLE ( 'NONE', #52395, 82.00000000000000000 ) ;
#64438=FACE_OUTER_BOUND ( 'NONE', #30142, .T. ) ;
#64439=EDGE_CURVE ( 'NONE', #56500, #1655, #61043, .T. ) ;
#64448=VERTEX_POINT ( 'NONE', #71571 ) ;
#64450=DIRECTION ( 'NONE',  ( 0.000000000000000000, 0.000000000000000000, 1.000000000000000000 ) ) ;
#64462=AXIS2_PLACEMENT_3D ( 'NONE', #59142, #30549, #24918 ) ;
#64484=DIRECTION ( 'NONE',  ( 0.000000000000000000, 0.000000000000000000, 1.000000000000000000 ) ) ;
#64486=AXIS2_PLACEMENT_3D ( 'NONE', #72372, #13471, #38915 ) ;
#64496=ADVANCED_FACE ( 'NONE', ( #32086 ), #38107, .T. ) ;
#64499=EDGE_CURVE ( 'NONE', #68371, #73400, #26406, .T. ) ;
#64504=DIRECTION ( 'NONE',  ( -1.000000000000000000, -0.000000000000000000, -0.000000000000000000 ) ) ;
#64508=CYLINDRICAL_SURFACE ( 'NONE', #48454, 31.99999999999999289 ) ;
#64515=VERTEX_POINT ( 'NONE', #59953 ) ;
#64521=ORIENTED_EDGE ( 'NONE', *, *, #17726, .T. ) ;
#64528=LINE ( 'NONE', #41973, #7843 ) ;
#64531=AXIS2_PLACEMENT_3D ( 'NONE', #50147, #15953, #22341 ) ;
#64532=ORIENTED_EDGE ( 'NONE', *, *, #29005, .F. ) ;
#64535=CARTESIAN_POINT ( 'NONE',  ( 10.00000000000000000, 0.8261519478441983200, -77.49459641780885022 ) ) ;
#64563=CARTESIAN_POINT ( 'NONE',  ( 10.00000000000000000, 39.78640506895604290, 66.50666863322015843 ) ) ;
#64575=ORIENTED_EDGE ( 'NONE', *, *, #15651, .T. ) ;
#64578=EDGE_LOOP ( 'NONE', ( #17320, #8303, #66603, #17225 ) ) ;
#64586=DIRECTION ( 'NONE',  ( 0.000000000000000000, 0.000000000000000000, 1.000000000000000000 ) ) ;
#64589=DIRECTION ( 'NONE',  ( -1.000000000000000000, 0.000000000000000000, 0.000000000000000000 ) ) ;
#64595=DIRECTION ( 'NONE',  ( -1.000000000000000000, 0.000000000000000000, -0.000000000000000000 ) ) ;
#64611=CARTESIAN_POINT ( 'NONE',  ( 10.00000000000000000, 18.89407956138362010, -75.16055320797013906 ) ) ;
#64612=DIRECTION ( 'NONE',  ( 0.000000000000000000, -0.4539904997395542430, 0.8910065241883641241 ) ) ;
#64614=EDGE_CURVE ( 'NONE', #19224, #11648, #56529, .T. ) ;
#64617=ORIENTED_EDGE ( 'NONE', *, *, #25121, .F. ) ;
#64627=DIRECTION ( 'NONE',  ( 0.000000000000000000, 0.000000000000000000, 1.000000000000000000 ) ) ;
#64647=AXIS2_PLACEMENT_3D ( 'NONE', #15589, #8473, #32865 ) ;
#64657=CARTESIAN_POINT ( 'NONE',  ( 10.00000000000000000, -81.50828551894220197, -8.966570791701579779 ) ) ;
#64659=VECTOR ( 'NONE', #63964, 1000.000000000000000 ) ;
#64662=DIRECTION ( 'NONE',  ( -1.000000000000000000, -0.000000000000000000, 0.000000000000000000 ) ) ;
#64668=VERTEX_POINT ( 'NONE', #5767 ) ;
#64670=CYLINDRICAL_SURFACE ( 'NONE', #54802, 31.99999999999999289 ) ;
#64676=ADVANCED_FACE ( 'NONE', ( #33198 ), #45630, .T. ) ;
#64678=CYLINDRICAL_SURFACE ( 'NONE', #12035, 82.00000000000000000 ) ;
#64689=CIRCLE ( 'NONE', #74293, 77.49900000000000944 ) ;
#64691=DIRECTION ( 'NONE',  ( 0.000000000000000000, 0.000000000000000000, 1.000000000000000000 ) ) ;
#64697=AXIS2_PLACEMENT_3D ( 'NONE', #43633, #71061, #36859 ) ;
#64698=EDGE_CURVE ( 'NONE', #23222, #19226, #50273, .T. ) ;
#64701=ORIENTED_EDGE ( 'NONE', *, *, #59580, .T. ) ;
#64706=DIRECTION ( 'NONE',  ( 1.000000000000000000, -0.000000000000000000, -0.000000000000000000 ) ) ;
#64715=ORIENTED_EDGE ( 'NONE', *, *, #57494, .T. ) ;
#64730=DIRECTION ( 'NONE',  ( -1.000000000000000000, -0.000000000000000000, -0.000000000000000000 ) ) ;
#64734=CARTESIAN_POINT ( 'NONE',  ( 10.00000000000000000, -65.58780272294100655, 36.73666225445870737 ) ) ;
#64737=AXIS2_PLACEMENT_3D ( 'NONE', #902, #12131, #12502 ) ;
#64746=DIRECTION ( 'NONE',  ( -1.000000000000000000, 0.000000000000000000, -0.000000000000000000 ) ) ;
#64747=CARTESIAN_POINT ( 'NONE',  ( 10.00000000000000000, 0.000000000000000000, 0.000000000000000000 ) ) ;
#64750=DIRECTION ( 'NONE',  ( 0.000000000000000000, 0.000000000000000000, 1.000000000000000000 ) ) ;
#64752=CARTESIAN_POINT ( 'NONE',  ( 10.00000000000000000, -39.78640506895559525, -66.50666863322042843 ) ) ;
#64761=DIRECTION ( 'NONE',  ( 0.000000000000000000, 0.9876883405951371042, 0.1564344650402346437 ) ) ;
#64766=DIRECTION ( 'NONE',  ( 0.000000000000000000, 0.000000000000000000, 1.000000000000000000 ) ) ;
#64774=AXIS2_PLACEMENT_3D ( 'NONE', #65682, #14161, #49490 ) ;
#64779=CARTESIAN_POINT ( 'NONE',  ( 0.000000000000000000, -22.90783923731575911, -78.73519480814978522 ) ) ;
#64785=DIRECTION ( 'NONE',  ( 0.000000000000000000, 0.6494480483301849905, -0.7604059656000299317 ) ) ;
#64787=EDGE_LOOP ( 'NONE', ( #29020, #67532, #47701, #20268 ) ) ;
#64790=DIRECTION ( 'NONE',  ( -1.000000000000000000, 0.000000000000000000, -0.000000000000000000 ) ) ;
#64795=EDGE_CURVE ( 'NONE', #9779, #34381, #69503, .T. ) ;
#64804=VERTEX_POINT ( 'NONE', #40711 ) ;
#64807=AXIS2_PLACEMENT_3D ( 'NONE', #13972, #36539, #2385 ) ;
#64812=VERTEX_POINT ( 'NONE', #47818 ) ;
#64814=CARTESIAN_POINT ( 'NONE',  ( 0.000000000000000000, 0.000000000000000000, 0.000000000000000000 ) ) ;
#64822=CIRCLE ( 'NONE', #35993, 82.00000000000000000 ) ;
#64833=ORIENTED_EDGE ( 'NONE', *, *, #8897, .F. ) ;
#64837=ORIENTED_EDGE ( 'NONE', *, *, #14862, .T. ) ;
#64858=EDGE_CURVE ( 'NONE', #4038, #17670, #32368, .T. ) ;
#64859=AXIS2_PLACEMENT_3D ( 'NONE', #46014, #23447, #6528 ) ;
#64861=DIRECTION ( 'NONE',  ( 0.000000000000000000, 0.000000000000000000, 1.000000000000000000 ) ) ;
#64863=VERTEX_POINT ( 'NONE', #26365 ) ;
#64864=ORIENTED_EDGE ( 'NONE', *, *, #71287, .F. ) ;
#64866=CARTESIAN_POINT ( 'NONE',  ( 0.000000000000000000, 65.64334221924909230, 41.19522573413756561 ) ) ;
#64869=CARTESIAN_POINT ( 'NONE',  ( 10.00000000000000000, 68.67312586194995561, 35.91791733033500122 ) ) ;
#64884=AXIS2_PLACEMENT_3D ( 'NONE', #27080, #66938, #33848 ) ;
#64893=DIRECTION ( 'NONE',  ( -1.000000000000000000, 0.000000000000000000, 0.000000000000000000 ) ) ;
#64894=VERTEX_POINT ( 'NONE', #20723 ) ;
#64911=CARTESIAN_POINT ( 'NONE',  ( 10.00000000000000000, -62.20884554313985149, -46.21855187248698371 ) ) ;
#64913=FACE_OUTER_BOUND ( 'NONE', #54294, .T. ) ;
#64915=CARTESIAN_POINT ( 'NONE',  ( 10.00000000000000000, -75.11725578898466438, -2.956366410621452001 ) ) ;
#64921=ORIENTED_EDGE ( 'NONE', *, *, #15449, .T. ) ;
#64935=LINE ( 'NONE', #32166, #34707 ) ;
#64946=EDGE_CURVE ( 'NONE', #4178, #464, #59478, .T. ) ;
#64961=ORIENTED_EDGE ( 'NONE', *, *, #66239, .T. ) ;
#64965=CARTESIAN_POINT ( 'NONE',  ( 10.00000000000000000, -75.11764819372145041, 29.05362095685286761 ) ) ;
#64966=AXIS2_PLACEMENT_3D ( 'NONE', #14828, #66714, #53957 ) ;
#64972=DIRECTION ( 'NONE',  ( 0.000000000000000000, 0.000000000000000000, 1.000000000000000000 ) ) ;
#64974=DIRECTION ( 'NONE',  ( -1.000000000000000000, 0.000000000000000000, 0.000000000000000000 ) ) ;
#64975=FACE_OUTER_BOUND ( 'NONE', #63559, .T. ) ;
#64976=DIRECTION ( 'NONE',  ( -1.000000000000000000, 0.000000000000000000, 0.000000000000000000 ) ) ;
#64978=DIRECTION ( 'NONE',  ( 0.000000000000000000, 0.000000000000000000, 1.000000000000000000 ) ) ;
#64988=CIRCLE ( 'NONE', #3760, 31.99999999999999289 ) ;
#64989=AXIS2_PLACEMENT_3D ( 'NONE', #6717, #52569, #1121 ) ;
#65000=ORIENTED_EDGE ( 'NONE', *, *, #41577, .T. ) ;
#65006=EDGE_LOOP ( 'NONE', ( #72044, #47256, #3631, #49352 ) ) ;
#65018=CARTESIAN_POINT ( 'NONE',  ( 0.000000000000000000, 0.000000000000000000, 0.000000000000000000 ) ) ;
#65020=EDGE_CURVE ( 'NONE', #67983, #50757, #62836, .T. ) ;
#65026=CARTESIAN_POINT ( 'NONE',  ( 10.00000000000000000, -62.20884554314051940, 46.21855187248608132 ) ) ;
#65027=EDGE_LOOP ( 'NONE', ( #7578, #39490, #43556, #40297 ) ) ;
#65042=DIRECTION ( 'NONE',  ( -1.000000000000000000, 0.000000000000000000, 0.000000000000000000 ) ) ;
#65043=EDGE_CURVE ( 'NONE', #72004, #10345, #15506, .T. ) ;
#65061=LINE ( 'NONE', #8645, #31241 ) ;
#65063=CARTESIAN_POINT ( 'NONE',  ( 10.00000000000000000, -58.39081064771713869, -50.95692526931392052 ) ) ;
#65094=ORIENTED_EDGE ( 'NONE', *, *, #52197, .F. ) ;
#65101=EDGE_LOOP ( 'NONE', ( #74269, #71016, #68355, #73015 ) ) ;
#65111=EDGE_LOOP ( 'NONE', ( #44031, #36248, #8998, #40044 ) ) ;
#65113=VERTEX_POINT ( 'NONE', #45535 ) ;
#65118=VERTEX_POINT ( 'NONE', #21449 ) ;
#65122=ORIENTED_EDGE ( 'NONE', *, *, #15334, .T. ) ;
#65141=DIRECTION ( 'NONE',  ( 0.000000000000000000, -0.3090169943749548898, 0.9510565162951511997 ) ) ;
#65142=LINE ( 'NONE', #59126, #20027 ) ;
#65159=FACE_OUTER_BOUND ( 'NONE', #9401, .T. ) ;
#65176=CARTESIAN_POINT ( 'NONE',  ( 10.00000000000000000, 68.26794271651307611, -31.47745569255064169 ) ) ;
#65184=DIRECTION ( 'NONE',  ( -1.000000000000000000, -0.000000000000000000, 0.000000000000000000 ) ) ;
#65189=VERTEX_POINT ( 'NONE', #57915 ) ;
#65194=VERTEX_POINT ( 'NONE', #64657 ) ;
#65198=VERTEX_POINT ( 'NONE', #53375 ) ;
#65203=ORIENTED_EDGE ( 'NONE', *, *, #43471, .T. ) ;
#65213=DIRECTION ( 'NONE',  ( -1.000000000000000000, -0.000000000000000000, 0.000000000000000000 ) ) ;
#65233=ORIENTED_EDGE ( 'NONE', *, *, #65449, .F. ) ;
#65235=ORIENTED_EDGE ( 'NONE', *, *, #41769, .F. ) ;
#65237=CARTESIAN_POINT ( 'NONE',  ( 10.00000000000000000, 0.000000000000000000, 0.000000000000000000 ) ) ;
#65239=DIRECTION ( 'NONE',  ( -1.000000000000000000, 0.000000000000000000, 0.000000000000000000 ) ) ;
#65240=CYLINDRICAL_SURFACE ( 'NONE', #52936, 31.99999999999999289 ) ;
#65248=CIRCLE ( 'NONE', #13594, 31.99999999999999289 ) ;
#65254=DIRECTION ( 'NONE',  ( 0.000000000000000000, 0.3090169943749482839, -0.9510565162951533091 ) ) ;
#65290=DIRECTION ( 'NONE',  ( -1.000000000000000000, 0.000000000000000000, 0.000000000000000000 ) ) ;
#65311=EDGE_CURVE ( 'NONE', #14991, #62129, #52955, .T. ) ;
#65338=DIRECTION ( 'NONE',  ( 0.000000000000000000, -0.9510565162951500895, -0.3090169943749581649 ) ) ;
#65345=CIRCLE ( 'NONE', #36559, 82.00000000000000000 ) ;
#65347=EDGE_CURVE ( 'NONE', #19224, #70328, #31313, .T. ) ;
#65359=CARTESIAN_POINT ( 'NONE',  ( 0.000000000000000000, 16.00000000000000000, 2.500000000000000000 ) ) ;
#65360=CARTESIAN_POINT ( 'NONE',  ( 5.000000000000000000, 64.81221759200417409, -50.23322058963276504 ) ) ;
#65363=ADVANCED_FACE ( 'NONE', ( #49205 ), #60869, .T. ) ;
#65372=DIRECTION ( 'NONE',  ( -1.000000000000000000, -0.000000000000000000, 0.000000000000000000 ) ) ;
#65384=EDGE_LOOP ( 'NONE', ( #56022, #15053, #33552, #30660 ) ) ;
#65399=ORIENTED_EDGE ( 'NONE', *, *, #71287, .T. ) ;
#65407=ORIENTED_EDGE ( 'NONE', *, *, #33505, .T. ) ;
#65424=CARTESIAN_POINT ( 'NONE',  ( 0.000000000000000000, -81.96053171279901051, -2.543863470249246195 ) ) ;
#65428=DIRECTION ( 'NONE',  ( 0.000000000000000000, 0.9238795325112877377, -0.3826834323650873948 ) ) ;
#65431=DIRECTION ( 'NONE',  ( -1.000000000000000000, -0.000000000000000000, -0.000000000000000000 ) ) ;
#65433=DIRECTION ( 'NONE',  ( -1.000000000000000000, 0.000000000000000000, 0.000000000000000000 ) ) ;
#65436=UNCERTAINTY_MEASURE_WITH_UNIT (LENGTH_MEASURE( 1.000000000000000082E-05 ), #44088, 'distance_accuracy_value', 'NONE');
#65444=DIRECTION ( 'NONE',  ( -1.000000000000000000, -0.000000000000000000, 0.000000000000000000 ) ) ;
#65449=EDGE_CURVE ( 'NONE', #43589, #19072, #38682, .T. ) ;
#65451=AXIS2_PLACEMENT_3D ( 'NONE', #40205, #23649, #6373 ) ;
#65460=DIRECTION ( 'NONE',  ( -1.000000000000000000, 0.000000000000000000, 0.000000000000000000 ) ) ;
#65467=VERTEX_POINT ( 'NONE', #67251 ) ;
#65470=EDGE_CURVE ( 'NONE', #68435, #60775, #70911, .T. ) ;
#65474=AXIS2_PLACEMENT_3D ( 'NONE', #18986, #47573, #59601 ) ;
#65484=DIRECTION ( 'NONE',  ( -1.000000000000000000, -0.000000000000000000, -0.000000000000000000 ) ) ;
#65490=CARTESIAN_POINT ( 'NONE',  ( 10.00000000000000000, 5.256550761633969060, -77.32052557432835727 ) ) ;
#65496=DIRECTION ( 'NONE',  ( 0.000000000000000000, 0.07845909572783793529, 0.9969173337331285190 ) ) ;
#65502=EDGE_LOOP ( 'NONE', ( #9418, #36935, #32436, #3647 ) ) ;
#65504=DIRECTION ( 'NONE',  ( -1.000000000000000000, 0.000000000000000000, 0.000000000000000000 ) ) ;
#65514=ORIENTED_EDGE ( 'NONE', *, *, #74325, .T. ) ;
#65525=AXIS2_PLACEMENT_3D ( 'NONE', #19712, #54677, #61058 ) ;
#65528=CYLINDRICAL_SURFACE ( 'NONE', #51475, 77.49899999999999523 ) ;
#65535=DIRECTION ( 'NONE',  ( -1.000000000000000000, -0.000000000000000000, -0.000000000000000000 ) ) ;
#65536=EDGE_CURVE ( 'NONE', #5511, #68580, #60207, .T. ) ;
#65537=DIRECTION ( 'NONE',  ( 1.000000000000000000, 0.000000000000000000, 0.000000000000000000 ) ) ;
#65540=ORIENTED_EDGE ( 'NONE', *, *, #34616, .F. ) ;
#65542=CARTESIAN_POINT ( 'NONE',  ( 0.000000000000000000, 50.23322058963348979, 64.81221759200361987 ) ) ;
#65544=DIRECTION ( 'NONE',  ( -1.000000000000000000, -0.000000000000000000, -0.000000000000000000 ) ) ;
#65548=EDGE_CURVE ( 'NONE', #30219, #14528, #8573, .T. ) ;
#65549=CARTESIAN_POINT ( 'NONE',  ( 10.00000000000000000, -77.19088730480528682, 6.903761155837488062 ) ) ;
#65561=ORIENTED_EDGE ( 'NONE', *, *, #39195, .T. ) ;
#65563=ORIENTED_EDGE ( 'NONE', *, *, #21526, .F. ) ;
#65594=CARTESIAN_POINT ( 'NONE',  ( 0.000000000000000000, -77.19088730480528682, 6.903761155837488062 ) ) ;
#65597=ORIENTED_EDGE ( 'NONE', *, *, #46415, .T. ) ;
#65599=CYLINDRICAL_SURFACE ( 'NONE', #49239, 32.00000000000000000 ) ;
#65604=DIRECTION ( 'NONE',  ( 0.000000000000000000, -0.7071067811865537900, 0.7071067811865413555 ) ) ;
#65616=AXIS2_PLACEMENT_3D ( 'NONE', #13236, #42555, #36164 ) ;
#65617=EDGE_CURVE ( 'NONE', #49569, #14685, #64988, .T. ) ;
#65623=DIRECTION ( 'NONE',  ( 0.000000000000000000, -0.9969173337331287410, 0.07845909572783495156 ) ) ;
#65631=FACE_OUTER_BOUND ( 'NONE', #19013, .T. ) ;
#65643=VERTEX_POINT ( 'NONE', #35618 ) ;
#65650=CIRCLE ( 'NONE', #23637, 77.49899999999999523 ) ;
#65655=VERTEX_POINT ( 'NONE', #12687 ) ;
#65662=CARTESIAN_POINT ( 'NONE',  ( 5.000000000000000000, 46.11716303203284184, -67.80270845531839541 ) ) ;
#65667=EDGE_CURVE ( 'NONE', #48290, #15280, #70969, .T. ) ;
#65668=EDGE_LOOP ( 'NONE', ( #54133, #5170, #27665, #54717 ) ) ;
#65682=CARTESIAN_POINT ( 'NONE',  ( 0.000000000000000000, 65.59268652807263322, -36.72794159290169347 ) ) ;
#65683=ORIENTED_EDGE ( 'NONE', *, *, #39338, .F. ) ;
#65690=FACE_OUTER_BOUND ( 'NONE', #23126, .T. ) ;
#65695=EDGE_LOOP ( 'NONE', ( #3437, #60954, #55680, #16117 ) ) ;
#65697=EDGE_CURVE ( 'NONE', #53602, #24570, #43429, .T. ) ;
#65699=DIRECTION ( 'NONE',  ( 0.000000000000000000, 0.000000000000000000, 1.000000000000000000 ) ) ;
#65700=CARTESIAN_POINT ( 'NONE',  ( 0.000000000000000000, 0.000000000000000000, 0.000000000000000000 ) ) ;
#65704=CARTESIAN_POINT ( 'NONE',  ( 0.000000000000000000, 51.29473840253317718, -63.97538442413369353 ) ) ;
#65708=CARTESIAN_POINT ( 'NONE',  ( 0.000000000000000000, 0.000000000000000000, 0.000000000000000000 ) ) ;
#65713=AXIS2_PLACEMENT_3D ( 'NONE', #40990, #64292, #51890 ) ;
#65719=AXIS2_PLACEMENT_3D ( 'NONE', #55061, #3593, #43806 ) ;
#65720=DIRECTION ( 'NONE',  ( -1.000000000000000000, -0.000000000000000000, -0.000000000000000000 ) ) ;
#65737=ORIENTED_EDGE ( 'NONE', *, *, #71030, .T. ) ;
#65740=ORIENTED_EDGE ( 'NONE', *, *, #16824, .F. ) ;
#65758=EDGE_CURVE ( 'NONE', #30795, #21162, #67378, .T. ) ;
#65759=DIRECTION ( 'NONE',  ( -1.000000000000000000, 0.000000000000000000, 0.000000000000000000 ) ) ;
#65760=ORIENTED_EDGE ( 'NONE', *, *, #16710, .T. ) ;
#65768=CARTESIAN_POINT ( 'NONE',  ( -10.00000000000000000, 0.000000000000000000, 0.000000000000000000 ) ) ;
#65782=ADVANCED_FACE ( 'NONE', ( #13791 ), #20560, .T. ) ;
#65783=CARTESIAN_POINT ( 'NONE',  ( 10.00000000000000000, 0.000000000000000000, 0.000000000000000000 ) ) ;
#65786=DIRECTION ( 'NONE',  ( -1.000000000000000000, 0.000000000000000000, 0.000000000000000000 ) ) ;
#65792=CARTESIAN_POINT ( 'NONE',  ( 10.00000000000000000, -46.54456581323762521, -59.03342792756313884 ) ) ;
#65794=CARTESIAN_POINT ( 'NONE',  ( 5.000000000000000000, 55.16347631943042984, 60.67117009219156643 ) ) ;
#65797=AXIS2_PLACEMENT_3D ( 'NONE', #48962, #48609, #71893 ) ;
#65804=CARTESIAN_POINT ( 'NONE',  ( 10.00000000000000000, -62.50329211542465657, 41.76937507738766442 ) ) ;
#65811=CIRCLE ( 'NONE', #31018, 12.50000000000000000 ) ;
#65817=DIRECTION ( 'NONE',  ( -1.000000000000000000, 0.000000000000000000, 0.000000000000000000 ) ) ;
#65826=ORIENTED_EDGE ( 'NONE', *, *, #63324, .F. ) ;
#65832=VECTOR ( 'NONE', #1618, 1000.000000000000000 ) ;
#65836=LINE ( 'NONE', #21816, #48477 ) ;
#65839=LINE ( 'NONE', #14325, #68934 ) ;
#65844=ORIENTED_EDGE ( 'NONE', *, *, #17455, .F. ) ;
#65846=DIRECTION ( 'NONE',  ( 0.000000000000000000, 0.000000000000000000, -1.000000000000000000 ) ) ;
#65859=EDGE_CURVE ( 'NONE', #60921, #23922, #14570, .T. ) ;
#65869=EDGE_CURVE ( 'NONE', #16005, #31772, #31368, .T. ) ;
#65876=CYLINDRICAL_SURFACE ( 'NONE', #40439, 82.00000000000000000 ) ;
#65878=AXIS2_PLACEMENT_3D ( 'NONE', #35821, #58776, #53130 ) ;
#65883=FACE_OUTER_BOUND ( 'NONE', #11368, .T. ) ;
#65884=ORIENTED_EDGE ( 'NONE', *, *, #46330, .T. ) ;
#65886=ORIENTED_EDGE ( 'NONE', *, *, #43550, .F. ) ;
#65890=CARTESIAN_POINT ( 'NONE',  ( 10.00000000000000000, 71.91182617369189245, 28.89263327155772743 ) ) ;
#65901=LINE ( 'NONE', #3131, #57369 ) ;
#65904=DIRECTION ( 'NONE',  ( 0.000000000000000000, 1.000000000000000000, 0.000000000000000000 ) ) ;
#65905=DIRECTION ( 'NONE',  ( 0.000000000000000000, 0.000000000000000000, 1.000000000000000000 ) ) ;
#65906=FACE_OUTER_BOUND ( 'NONE', #4983, .T. ) ;
#65911=EDGE_CURVE ( 'NONE', #52257, #7708, #73377, .T. ) ;
#65917=DIRECTION ( 'NONE',  ( 0.000000000000000000, 0.000000000000000000, 1.000000000000000000 ) ) ;
#65924=ORIENTED_EDGE ( 'NONE', *, *, #23333, .T. ) ;
#65932=ORIENTED_EDGE ( 'NONE', *, *, #32341, .F. ) ;
#65943=EDGE_LOOP ( 'NONE', ( #66134, #1612, #51955, #38933 ) ) ;
#65945=VERTEX_POINT ( 'NONE', #46002 ) ;
#65960=ADVANCED_FACE ( 'NONE', ( #68566 ), #73807, .T. ) ;
#65963=EDGE_CURVE ( 'NONE', #34327, #16195, #41512, .T. ) ;
#65979=DIRECTION ( 'NONE',  ( -1.000000000000000000, 0.000000000000000000, 0.000000000000000000 ) ) ;
#65980=EDGE_LOOP ( 'NONE', ( #61319, #34786, #62233, #36956 ) ) ;
#65983=DIRECTION ( 'NONE',  ( 0.000000000000000000, 0.3090169943749410120, 0.9510565162951556406 ) ) ;
#65986=DIRECTION ( 'NONE',  ( 0.000000000000000000, 0.000000000000000000, 1.000000000000000000 ) ) ;
#65990=EDGE_LOOP ( 'NONE', ( #31178, #52895, #22033, #58511 ) ) ;
#65994=ADVANCED_FACE ( 'NONE', ( #39618 ), #9272, .T. ) ;
#65999=LINE ( 'NONE', #20493, #62963 ) ;
#66000=CARTESIAN_POINT ( 'NONE',  ( 0.000000000000000000, -8.840884882375609877, 74.65374052328647281 ) ) ;
#66008=DIRECTION ( 'NONE',  ( 0.000000000000000000, 0.000000000000000000, 1.000000000000000000 ) ) ;
#66012=CIRCLE ( 'NONE', #28804, 31.99999999999999289 ) ;
#66013=AXIS2_PLACEMENT_3D ( 'NONE', #68151, #4645, #56514 ) ;
#66018=ORIENTED_EDGE ( 'NONE', *, *, #38718, .F. ) ;
#66024=LINE ( 'NONE', #36321, #889 ) ;
#66025=CARTESIAN_POINT ( 'NONE',  ( 0.000000000000000000, -21.60688246758642705, 79.10210256391360417 ) ) ;
#66035=ORIENTED_EDGE ( 'NONE', *, *, #20175, .T. ) ;
#66036=VECTOR ( 'NONE', #67825, 1000.000000000000000 ) ;
#66041=EDGE_CURVE ( 'NONE', #5572, #39383, #39103, .T. ) ;
#66056=CARTESIAN_POINT ( 'NONE',  ( 10.00000000000000000, -79.10210256391353312, -21.60688246758667574 ) ) ;
#66065=CIRCLE ( 'NONE', #48018, 31.99999999999998934 ) ;
#66079=DIRECTION ( 'NONE',  ( -1.000000000000000000, -0.000000000000000000, -0.000000000000000000 ) ) ;
#66081=CARTESIAN_POINT ( 'NONE',  ( 10.00000000000000000, 74.65374052328660071, -8.840884882374309583 ) ) ;
#66089=DIRECTION ( 'NONE',  ( -1.000000000000000000, 0.000000000000000000, -0.000000000000000000 ) ) ;
#66093=CARTESIAN_POINT ( 'NONE',  ( 0.000000000000000000, 77.19088730480532945, -6.903761155836913410 ) ) ;
#66103=DIRECTION ( 'NONE',  ( -1.000000000000000000, 0.000000000000000000, -0.000000000000000000 ) ) ;
#66109=EDGE_LOOP ( 'NONE', ( #19218, #74223, #36173, #42573 ) ) ;
#66113=CARTESIAN_POINT ( 'NONE',  ( 5.000000000000002665, -34.94270380257586339, -74.18225833017926618 ) ) ;
#66114=DIRECTION ( 'NONE',  ( -1.000000000000000000, 0.000000000000000000, -0.000000000000000000 ) ) ;
#66134=ORIENTED_EDGE ( 'NONE', *, *, #42219, .T. ) ;
#66141=VECTOR ( 'NONE', #66089, 1000.000000000000000 ) ;
#66142=CARTESIAN_POINT ( 'NONE',  ( 10.00000000000000000, 0.000000000000000000, 77.49899999999999523 ) ) ;
#66143=ORIENTED_EDGE ( 'NONE', *, *, #15958, .T. ) ;
#66144=AXIS2_PLACEMENT_3D ( 'NONE', #47201, #58112, #70114 ) ;
#66153=EDGE_CURVE ( 'NONE', #42089, #32443, #35502, .T. ) ;
#66167=AXIS2_PLACEMENT_3D ( 'NONE', #53948, #60335, #64861 ) ;
#66179=CARTESIAN_POINT ( 'NONE',  ( 10.00000000000000000, -67.80270845531921964, 46.11716303203163392 ) ) ;
#66184=CARTESIAN_POINT ( 'NONE',  ( 10.00000000000000000, 0.000000000000000000, 0.000000000000000000 ) ) ;
#66187=DIRECTION ( 'NONE',  ( 0.000000000000000000, 0.000000000000000000, 1.000000000000000000 ) ) ;
#66190=EDGE_CURVE ( 'NONE', #25525, #52624, #41824, .T. ) ;
#66219=CARTESIAN_POINT ( 'NONE',  ( 10.00000000000000000, 75.11764819372142199, 2.946379043147685728 ) ) ;
#66220=VERTEX_POINT ( 'NONE', #3114 ) ;
#66225=ORIENTED_EDGE ( 'NONE', *, *, #25206, .F. ) ;
#66231=DIRECTION ( 'NONE',  ( 1.000000000000000000, 0.000000000000000000, 0.000000000000000000 ) ) ;
#66239=EDGE_CURVE ( 'NONE', #62527, #991, #3843, .T. ) ;
#66241=EDGE_CURVE ( 'NONE', #47803, #56493, #42947, .T. ) ;
#66246=FACE_OUTER_BOUND ( 'NONE', #61860, .T. ) ;
#66250=AXIS2_PLACEMENT_3D ( 'NONE', #58286, #28592, #12780 ) ;
#66253=DIRECTION ( 'NONE',  ( 0.000000000000000000, 0.000000000000000000, 1.000000000000000000 ) ) ;
#66255=AXIS2_PLACEMENT_3D ( 'NONE', #37230, #42865, #59051 ) ;
#66259=LINE ( 'NONE', #65890, #62028 ) ;
#66264=FACE_OUTER_BOUND ( 'NONE', #48897, .T. ) ;
#66268=LINE ( 'NONE', #1396, #40075 ) ;
#66270=CIRCLE ( 'NONE', #48230, 77.49900000000002365 ) ;
#66279=CARTESIAN_POINT ( 'NONE',  ( 5.000000000000000000, -55.16347631943085617, 60.67117009219118273 ) ) ;
#66286=DIRECTION ( 'NONE',  ( -1.000000000000000000, -0.000000000000000000, 0.000000000000000000 ) ) ;
#66287=EDGE_CURVE ( 'NONE', #991, #31033, #17532, .T. ) ;
#66294=ORIENTED_EDGE ( 'NONE', *, *, #44760, .T. ) ;
#66297=CIRCLE ( 'NONE', #12244, 77.49900000000000944 ) ;
#66304=VERTEX_POINT ( 'NONE', #43332 ) ;
#66307=VERTEX_POINT ( 'NONE', #26379 ) ;
#66310=ORIENTED_EDGE ( 'NONE', *, *, #53073, .F. ) ;
#66321=ORIENTED_EDGE ( 'NONE', *, *, #65617, .T. ) ;
#66326=DIRECTION ( 'NONE',  ( -1.000000000000000000, 0.000000000000000000, 0.000000000000000000 ) ) ;
#66330=CYLINDRICAL_SURFACE ( 'NONE', #38262, 31.99999999999998579 ) ;
#66332=FACE_OUTER_BOUND ( 'NONE', #65695, .T. ) ;
#66342=FACE_OUTER_BOUND ( 'NONE', #46243, .T. ) ;
#66345=LINE ( 'NONE', #60699, #70262 ) ;
#66347=CARTESIAN_POINT ( 'NONE',  ( 10.00000000000000000, 0.000000000000000000, 0.000000000000000000 ) ) ;
#66348=ORIENTED_EDGE ( 'NONE', *, *, #56377, .T. ) ;
#66351=FACE_OUTER_BOUND ( 'NONE', #22768, .T. ) ;
#66352=CYLINDRICAL_SURFACE ( 'NONE', #25497, 82.00000000000000000 ) ;
#66353=FACE_OUTER_BOUND ( 'NONE', #57532, .T. ) ;
#66354=FACE_OUTER_BOUND ( 'NONE', #31418, .T. ) ;
#66358=CARTESIAN_POINT ( 'NONE',  ( 10.00000000000000000, 62.50884508063427347, 41.76106447765511831 ) ) ;
#66360=CIRCLE ( 'NONE', #60351, 82.00000000000000000 ) ;
#66366=DIRECTION ( 'NONE',  ( -1.000000000000000000, 0.000000000000000000, 0.000000000000000000 ) ) ;
#66368=CIRCLE ( 'NONE', #35177, 77.49900000000000944 ) ;
#66379=CIRCLE ( 'NONE', #25512, 77.49900000000000944 ) ;
#66382=EDGE_CURVE ( 'NONE', #70074, #3369, #71504, .T. ) ;
#66384=ORIENTED_EDGE ( 'NONE', *, *, #22404, .T. ) ;
#66386=EDGE_LOOP ( 'NONE', ( #17481, #31912, #64403, #51312 ) ) ;
#66394=FACE_OUTER_BOUND ( 'NONE', #28009, .T. ) ;
#66395=CARTESIAN_POINT ( 'NONE',  ( 0.000000000000000000, 16.00000000000000000, -2.500000000000000000 ) ) ;
#66404=VERTEX_POINT ( 'NONE', #62853 ) ;
#66406=EDGE_CURVE ( 'NONE', #33112, #12032, #9145, .T. ) ;
#66408=AXIS2_PLACEMENT_3D ( 'NONE', #9316, #71348, #25868 ) ;
#66411=LINE ( 'NONE', #65662, #32993 ) ;
#66417=DIRECTION ( 'NONE',  ( -1.000000000000000000, -0.000000000000000000, 0.000000000000000000 ) ) ;
#66420=VECTOR ( 'NONE', #31047, 1000.000000000000000 ) ;
#66426=DIRECTION ( 'NONE',  ( -1.000000000000000000, -0.000000000000000000, 0.000000000000000000 ) ) ;
#66429=VERTEX_POINT ( 'NONE', #45170 ) ;
#66441=DIRECTION ( 'NONE',  ( 0.000000000000000000, -0.07845909572785220165, 0.9969173337331274087 ) ) ;
#66448=DIRECTION ( 'NONE',  ( 0.000000000000000000, -0.3090169943749548342, 0.9510565162951510887 ) ) ;
#66453=VECTOR ( 'NONE', #21388, 1000.000000000000000 ) ;
#66464=ADVANCED_FACE ( 'NONE', ( #51161 ), #16585, .T. ) ;
#66471=AXIS2_PLACEMENT_3D ( 'NONE', #49874, #32951, #37876 ) ;
#66475=EDGE_CURVE ( 'NONE', #9910, #22755, #40389, .T. ) ;
#66478=DIRECTION ( 'NONE',  ( 0.000000000000000000, 0.5224985647159441360, 0.8526401643540951758 ) ) ;
#66487=DIRECTION ( 'NONE',  ( 0.000000000000000000, -0.3090169943749349613, -0.9510565162951576390 ) ) ;
#66489=EDGE_CURVE ( 'NONE', #44617, #33112, #67723, .T. ) ;
#66491=CARTESIAN_POINT ( 'NONE',  ( 10.00000000000000000, -76.41127070299280888, 12.93880638057289012 ) ) ;
#66492=ORIENTED_EDGE ( 'NONE', *, *, #31715, .T. ) ;
#66501=DIRECTION ( 'NONE',  ( 0.000000000000000000, 0.000000000000000000, 1.000000000000000000 ) ) ;
#66512=ORIENTED_EDGE ( 'NONE', *, *, #23037, .T. ) ;
#66516=VECTOR ( 'NONE', #8966, 1000.000000000000000 ) ;
#66521=ORIENTED_EDGE ( 'NONE', *, *, #10625, .F. ) ;
#66524=LINE ( 'NONE', #10479, #15245 ) ;
#66526=DIRECTION ( 'NONE',  ( 0.000000000000000000, 0.000000000000000000, 1.000000000000000000 ) ) ;
#66533=CARTESIAN_POINT ( 'NONE',  ( 10.00000000000000000, 55.38113227695858143, -54.21277698773617715 ) ) ;
#66544=EDGE_CURVE ( 'NONE', #36499, #71482, #46355, .T. ) ;
#66546=FACE_OUTER_BOUND ( 'NONE', #51782, .T. ) ;
#66547=ADVANCED_FACE ( 'NONE', ( #6072 ), #13161, .T. ) ;
#66548=DIRECTION ( 'NONE',  ( 0.000000000000000000, -0.1564344650402381132, 0.9876883405951365491 ) ) ;
#66556=DIRECTION ( 'NONE',  ( -1.000000000000000000, -0.000000000000000000, 0.000000000000000000 ) ) ;
#66557=CIRCLE ( 'NONE', #57016, 31.99999999999999289 ) ;
#66572=DIRECTION ( 'NONE',  ( -1.000000000000000000, 0.000000000000000000, 0.000000000000000000 ) ) ;
#66586=ORIENTED_EDGE ( 'NONE', *, *, #10771, .F. ) ;
#66593=LINE ( 'NONE', #26359, #63108 ) ;
#66603=ORIENTED_EDGE ( 'NONE', *, *, #70319, .T. ) ;
#66607=CARTESIAN_POINT ( 'NONE',  ( 0.000000000000000000, 0.000000000000000000, 77.49899999999999523 ) ) ;
#66614=CIRCLE ( 'NONE', #24641, 31.99999999999999289 ) ;
#66630=AXIS2_PLACEMENT_3D ( 'NONE', #65176, #41489, #47868 ) ;
#66645=DIRECTION ( 'NONE',  ( -1.000000000000000000, 0.000000000000000000, 0.000000000000000000 ) ) ;
#66648=DIRECTION ( 'NONE',  ( 0.000000000000000000, 0.000000000000000000, -1.000000000000000000 ) ) ;
#66649=ORIENTED_EDGE ( 'NONE', *, *, #20041, .F. ) ;
#66653=ORIENTED_EDGE ( 'NONE', *, *, #21513, .F. ) ;
#66662=ORIENTED_EDGE ( 'NONE', *, *, #64171, .F. ) ;
#66672=CARTESIAN_POINT ( 'NONE',  ( 10.00000000000000000, 75.11764819372149304, -2.946379043146603482 ) ) ;
#66675=ORIENTED_EDGE ( 'NONE', *, *, #57804, .T. ) ;
#66685=CIRCLE ( 'NONE', #7854, 82.00000000000000000 ) ;
#66698=AXIS2_PLACEMENT_3D ( 'NONE', #31732, #9178, #32470 ) ;
#66703=VERTEX_POINT ( 'NONE', #12055 ) ;
#66714=DIRECTION ( 'NONE',  ( -1.000000000000000000, 0.000000000000000000, 0.000000000000000000 ) ) ;
#66716=ORIENTED_EDGE ( 'NONE', *, *, #47975, .T. ) ;
#66720=DIRECTION ( 'NONE',  ( 0.000000000000000000, 0.5224985647159500202, -0.8526401643540915121 ) ) ;
#66721=DIRECTION ( 'NONE',  ( -1.000000000000000000, 0.000000000000000000, -0.000000000000000000 ) ) ;
#66732=CARTESIAN_POINT ( 'NONE',  ( 0.000000000000000000, -63.18004540532994184, -44.88180994100446952 ) ) ;
#66737=EDGE_CURVE ( 'NONE', #10962, #69749, #9004, .T. ) ;
#66740=CIRCLE ( 'NONE', #51165, 31.99999999999999645 ) ;
#66743=ORIENTED_EDGE ( 'NONE', *, *, #30529, .T. ) ;
#66761=ORIENTED_EDGE ( 'NONE', *, *, #67204, .T. ) ;
#66762=EDGE_LOOP ( 'NONE', ( #29651, #63853, #31453, #61299 ) ) ;
#66763=CARTESIAN_POINT ( 'NONE',  ( 0.000000000000000000, -74.65491531819111515, 23.16904090965678975 ) ) ;
#66782=DIRECTION ( 'NONE',  ( -1.000000000000000000, -0.000000000000000000, 0.000000000000000000 ) ) ;
#66788=CIRCLE ( 'NONE', #3223, 77.49899999999999523 ) ;
#66790=CIRCLE ( 'NONE', #27154, 77.49899999999999523 ) ;
#66794=VECTOR ( 'NONE', #7171, 1000.000000000000000 ) ;
#66796=DIRECTION ( 'NONE',  ( -1.000000000000000000, -0.000000000000000000, 0.000000000000000000 ) ) ;
#66801=ORIENTED_EDGE ( 'NONE', *, *, #14163, .T. ) ;
#66805=CARTESIAN_POINT ( 'NONE',  ( 10.00000000000000000, 0.000000000000000000, 0.000000000000000000 ) ) ;
#66821=EDGE_CURVE ( 'NONE', #44951, #70845, #59438, .T. ) ;
#66831=AXIS2_PLACEMENT_3D ( 'NONE', #7943, #30864, #14692 ) ;
#66839=CIRCLE ( 'NONE', #29632, 31.99999999999999645 ) ;
#66843=CARTESIAN_POINT ( 'NONE',  ( 10.00000000000000000, 28.89263327155850902, -71.91182617369157981 ) ) ;
#66850=CARTESIAN_POINT ( 'NONE',  ( 10.00000000000000000, 0.000000000000000000, 0.000000000000000000 ) ) ;
#66855=CIRCLE ( 'NONE', #15230, 31.99999999999999289 ) ;
#66857=CARTESIAN_POINT ( 'NONE',  ( 0.000000000000000000, 73.73191006444572793, -14.66109333815486515 ) ) ;
#66864=DIRECTION ( 'NONE',  ( -1.000000000000000000, 0.000000000000000000, 0.000000000000000000 ) ) ;
#66867=EDGE_LOOP ( 'NONE', ( #62507, #15252, #23859, #56061 ) ) ;
#66894=CARTESIAN_POINT ( 'NONE',  ( 10.00000000000000000, -62.50884508063453637, 41.76106447765467777 ) ) ;
#66898=CIRCLE ( 'NONE', #51279, 77.49900000000000944 ) ;
#66901=CARTESIAN_POINT ( 'NONE',  ( 10.00000000000000000, 55.16347631943129670, -60.67117009219074220 ) ) ;
#66904=CARTESIAN_POINT ( 'NONE',  ( 0.000000000000000000, 65.58780272294129077, -36.73666225445822420 ) ) ;
#66910=DIRECTION ( 'NONE',  ( -1.000000000000000000, -0.000000000000000000, -0.000000000000000000 ) ) ;
#66911=DIRECTION ( 'NONE',  ( 0.000000000000000000, 0.000000000000000000, 1.000000000000000000 ) ) ;
#66913=EDGE_LOOP ( 'NONE', ( #42661, #57713, #56131, #12749 ) ) ;
#66915=CARTESIAN_POINT ( 'NONE',  ( 10.00000000000000000, -59.03961581697432592, 46.53671651293927880 ) ) ;
#66923=ORIENTED_EDGE ( 'NONE', *, *, #39666, .T. ) ;
#66930=DIRECTION ( 'NONE',  ( 0.000000000000000000, 0.000000000000000000, -1.000000000000000000 ) ) ;
#66934=CYLINDRICAL_SURFACE ( 'NONE', #3261, 77.49899999999999523 ) ;
#66936=CARTESIAN_POINT ( 'NONE',  ( 10.00000000000000000, 20.41045688087824317, 72.35160999960824313 ) ) ;
#66938=DIRECTION ( 'NONE',  ( -1.000000000000000000, -0.000000000000000000, -0.000000000000000000 ) ) ;
#66940=EDGE_LOOP ( 'NONE', ( #23296, #24715, #60830, #29869 ) ) ;
#66941=ADVANCED_FACE ( 'NONE', ( #50333 ), #34163, .T. ) ;
#66958=CIRCLE ( 'NONE', #40568, 32.00000000000000000 ) ;
#66965=CARTESIAN_POINT ( 'NONE',  ( 10.00000000000000000, 20.40083707022987625, -72.35432306680462489 ) ) ;
#66979=FACE_BOUND ( 'NONE', #627, .T. ) ;
#66997=VERTEX_POINT ( 'NONE', #10483 ) ;
#67013=EDGE_CURVE ( 'NONE', #15750, #49569, #33791, .T. ) ;
#67016=FACE_OUTER_BOUND ( 'NONE', #12574, .T. ) ;
#67020=VERTEX_POINT ( 'NONE', #52553 ) ;
#67036=ORIENTED_EDGE ( 'NONE', *, *, #28185, .T. ) ;
#67040=CIRCLE ( 'NONE', #20232, 31.99999999999999289 ) ;
#67045=CARTESIAN_POINT ( 'NONE',  ( 10.00000000000000000, 0.000000000000000000, 0.000000000000000000 ) ) ;
#67066=AXIS2_PLACEMENT_3D ( 'NONE', #23029, #12097, #7205 ) ;
#67075=DIRECTION ( 'NONE',  ( 0.000000000000000000, 0.000000000000000000, 1.000000000000000000 ) ) ;
#67079=ORIENTED_EDGE ( 'NONE', *, *, #22178, .F. ) ;
#67092=AXIS2_PLACEMENT_3D ( 'NONE', #66904, #15775, #20671 ) ;
#67096=DIRECTION ( 'NONE',  ( -1.000000000000000000, 0.000000000000000000, 0.000000000000000000 ) ) ;
#67108=AXIS2_PLACEMENT_3D ( 'NONE', #72965, #67348, #15849 ) ;
#67111=CIRCLE ( 'NONE', #69483, 32.00000000000000000 ) ;
#67115=AXIS2_PLACEMENT_3D ( 'NONE', #47700, #1519, #71725 ) ;
#67120=DIRECTION ( 'NONE',  ( -1.000000000000000000, 0.000000000000000000, 0.000000000000000000 ) ) ;
#67126=EDGE_CURVE ( 'NONE', #4935, #53602, #12698, .T. ) ;
#67128=ORIENTED_EDGE ( 'NONE', *, *, #3147, .T. ) ;
#67129=ORIENTED_EDGE ( 'NONE', *, *, #22178, .T. ) ;
#67132=DIRECTION ( 'NONE',  ( 0.000000000000000000, -0.9238795325112821866, -0.3826834323651006065 ) ) ;
#67151=CARTESIAN_POINT ( 'NONE',  ( 10.00000000000000000, -41.19522573413780009, 65.64334221924896440 ) ) ;
#67163=ADVANCED_FACE ( 'NONE', ( #5988 ), #28894, .T. ) ;
#67164=FACE_OUTER_BOUND ( 'NONE', #1838, .T. ) ;
#67167=CARTESIAN_POINT ( 'NONE',  ( 10.00000000000000000, 0.000000000000000000, 0.000000000000000000 ) ) ;
#67184=AXIS2_PLACEMENT_3D ( 'NONE', #71794, #49979, #43632 ) ;
#67190=VERTEX_POINT ( 'NONE', #64965 ) ;
#67197=CARTESIAN_POINT ( 'NONE',  ( 0.000000000000000000, -40.65526001592565564, -71.21200624218839437 ) ) ;
#67201=AXIS2_PLACEMENT_3D ( 'NONE', #30912, #59885, #4504 ) ;
#67204=EDGE_CURVE ( 'NONE', #38641, #21124, #40226, .T. ) ;
#67206=EDGE_CURVE ( 'NONE', #56916, #35888, #25839, .T. ) ;
#67209=DIRECTION ( 'NONE',  ( -1.000000000000000000, 0.000000000000000000, 0.000000000000000000 ) ) ;
#67221=VECTOR ( 'NONE', #39230, 1000.000000000000000 ) ;
#67223=DIRECTION ( 'NONE',  ( -1.000000000000000000, -0.000000000000000000, 0.000000000000000000 ) ) ;
#67224=AXIS2_PLACEMENT_3D ( 'NONE', #36518, #65484, #14330 ) ;
#67226=CARTESIAN_POINT ( 'NONE',  ( 5.000000000000000000, -51.29473840253177741, -63.97538442413482329 ) ) ;
#67230=ORIENTED_EDGE ( 'NONE', *, *, #69590, .T. ) ;
#67232=ORIENTED_EDGE ( 'NONE', *, *, #30457, .T. ) ;
#67242=DIRECTION ( 'NONE',  ( -1.000000000000000000, 0.000000000000000000, -0.000000000000000000 ) ) ;
#67243=LINE ( 'NONE', #51427, #55289 ) ;
#67246=EDGE_CURVE ( 'NONE', #45326, #33698, #48395, .T. ) ;
#67247=EDGE_CURVE ( 'NONE', #13514, #10345, #19448, .T. ) ;
#67250=ORIENTED_EDGE ( 'NONE', *, *, #68867, .F. ) ;
#67251=CARTESIAN_POINT ( 'NONE',  ( 0.000000000000000000, 40.65526001592612459, 71.21200624218811015 ) ) ;
#67256=ORIENTED_EDGE ( 'NONE', *, *, #16964, .T. ) ;
#67263=CARTESIAN_POINT ( 'NONE',  ( 0.000000000000000000, 0.000000000000000000, 0.000000000000000000 ) ) ;
#67281=AXIS2_PLACEMENT_3D ( 'NONE', #36443, #2281, #59761 ) ;
#67282=DIRECTION ( 'NONE',  ( 0.000000000000000000, 0.000000000000000000, 1.000000000000000000 ) ) ;
#67294=ORIENTED_EDGE ( 'NONE', *, *, #55783, .F. ) ;
#67306=ORIENTED_EDGE ( 'NONE', *, *, #14772, .F. ) ;
#67310=EDGE_LOOP ( 'NONE', ( #63006, #29588, #52542, #9504 ) ) ;
#67311=CARTESIAN_POINT ( 'NONE',  ( 0.000000000000000000, -80.28980883073769803, 16.65972982744906261 ) ) ;
#67315=ADVANCED_FACE ( 'NONE', ( #59312 ), #7807, .T. ) ;
#67317=DIRECTION ( 'NONE',  ( 1.000000000000000000, -0.000000000000000000, -0.000000000000000000 ) ) ;
#67318=ORIENTED_EDGE ( 'NONE', *, *, #616, .F. ) ;
#67324=AXIS2_PLACEMENT_3D ( 'NONE', #53200, #1738, #12231 ) ;
#67325=EDGE_CURVE ( 'NONE', #47328, #34710, #53486, .T. ) ;
#67330=ORIENTED_EDGE ( 'NONE', *, *, #1893, .F. ) ;
#67346=CARTESIAN_POINT ( 'NONE',  ( 0.000000000000000000, 0.000000000000000000, 0.000000000000000000 ) ) ;
#67348=DIRECTION ( 'NONE',  ( -1.000000000000000000, -0.000000000000000000, 0.000000000000000000 ) ) ;
#67349=ORIENTED_EDGE ( 'NONE', *, *, #64410, .F. ) ;
#67358=CARTESIAN_POINT ( 'NONE',  ( 5.000000000000002665, -80.28980883073769803, 16.65972982744906261 ) ) ;
#67359=CIRCLE ( 'NONE', #60138, 77.49899999999999523 ) ;
#67361=CIRCLE ( 'NONE', #33772, 31.99999999999999289 ) ;
#67377=CIRCLE ( 'NONE', #36201, 31.99999999999999289 ) ;
#67378=CIRCLE ( 'NONE', #37409, 31.99999999999999645 ) ;
#67382=VERTEX_POINT ( 'NONE', #10772 ) ;
#67386=ADVANCED_FACE ( 'NONE', ( #34071 ), #27691, .T. ) ;
#67389=EDGE_LOOP ( 'NONE', ( #40227, #28862, #29483, #54901 ) ) ;
#67393=DIRECTION ( 'NONE',  ( -1.000000000000000000, -0.000000000000000000, 0.000000000000000000 ) ) ;
#67397=DIRECTION ( 'NONE',  ( -1.000000000000000000, -0.000000000000000000, -0.000000000000000000 ) ) ;
#67406=ORIENTED_EDGE ( 'NONE', *, *, #73991, .F. ) ;
#67409=AXIS2_PLACEMENT_3D ( 'NONE', #9823, #32741, #49302 ) ;
#67416=EDGE_CURVE ( 'NONE', #63089, #26612, #15100, .T. ) ;
#67439=DIRECTION ( 'NONE',  ( -1.000000000000000000, -0.000000000000000000, -0.000000000000000000 ) ) ;
#67449=CARTESIAN_POINT ( 'NONE',  ( 10.00000000000000000, 51.02545421589324803, 55.20638768913779870 ) ) ;
#67458=DIRECTION ( 'NONE',  ( -1.000000000000000000, 0.000000000000000000, 0.000000000000000000 ) ) ;
#67471=DIRECTION ( 'NONE',  ( -1.000000000000000000, -0.000000000000000000, -0.000000000000000000 ) ) ;
#67479=VERTEX_POINT ( 'NONE', #5891 ) ;
#67490=ORIENTED_EDGE ( 'NONE', *, *, #19345, .T. ) ;
#67495=EDGE_CURVE ( 'NONE', #49393, #39290, #40451, .T. ) ;
#67497=DIRECTION ( 'NONE',  ( -1.000000000000000000, 0.000000000000000000, -0.000000000000000000 ) ) ;
#67502=ORIENTED_EDGE ( 'NONE', *, *, #63332, .F. ) ;
#67509=DIRECTION ( 'NONE',  ( 0.000000000000000000, 0.000000000000000000, 1.000000000000000000 ) ) ;
#67529=DIRECTION ( 'NONE',  ( -1.000000000000000000, -0.000000000000000000, -0.000000000000000000 ) ) ;
#67532=ORIENTED_EDGE ( 'NONE', *, *, #41261, .F. ) ;
#67538=DIRECTION ( 'NONE',  ( -1.000000000000000000, -0.000000000000000000, -0.000000000000000000 ) ) ;
#67549=CARTESIAN_POINT ( 'NONE',  ( 10.00000000000000000, 8.830959090342393125, 74.65491531819122883 ) ) ;
#67560=DIRECTION ( 'NONE',  ( -1.000000000000000000, -0.000000000000000000, -0.000000000000000000 ) ) ;
#67564=ORIENTED_EDGE ( 'NONE', *, *, #73427, .T. ) ;
#67567=LINE ( 'NONE', #58841, #69571 ) ;
#67572=EDGE_CURVE ( 'NONE', #72495, #2787, #60738, .T. ) ;
#67580=EDGE_CURVE ( 'NONE', #10345, #34939, #66685, .T. ) ;
#67585=DIRECTION ( 'NONE',  ( -1.000000000000000000, 0.000000000000000000, 0.000000000000000000 ) ) ;
#67590=DIRECTION ( 'NONE',  ( 1.000000000000000000, 0.000000000000000000, 0.000000000000000000 ) ) ;
#67591=ORIENTED_EDGE ( 'NONE', *, *, #46496, .T. ) ;
#67626=VERTEX_POINT ( 'NONE', #29158 ) ;
#67632=DIRECTION ( 'NONE',  ( -1.000000000000000000, 0.000000000000000000, 0.000000000000000000 ) ) ;
#67647=AXIS2_PLACEMENT_3D ( 'NONE', #13576, #36145, #1249 ) ;
#67648=CARTESIAN_POINT ( 'NONE',  ( 0.000000000000000000, 0.000000000000000000, 0.000000000000000000 ) ) ;
#67652=CARTESIAN_POINT ( 'NONE',  ( 10.00000000000000000, 26.02418014898310261, 70.52718814184268581 ) ) ;
#67657=DIRECTION ( 'NONE',  ( -1.000000000000000000, -0.000000000000000000, -0.000000000000000000 ) ) ;
#67664=CARTESIAN_POINT ( 'NONE',  ( 0.000000000000000000, -71.87247863392443037, 39.47590169984818687 ) ) ;
#67667=EDGE_CURVE ( 'NONE', #63002, #10732, #58861, .T. ) ;
#67673=ORIENTED_EDGE ( 'NONE', *, *, #32763, .T. ) ;
#67684=CARTESIAN_POINT ( 'NONE',  ( 50.00005079999999680, 1.530808498934191521E-15, -12.50000000000000000 ) ) ;
#67699=ORIENTED_EDGE ( 'NONE', *, *, #46042, .F. ) ;
#67706=ORIENTED_EDGE ( 'NONE', *, *, #55496, .F. ) ;
#67707=CARTESIAN_POINT ( 'NONE',  ( 10.00000000000000000, -2.543863470247802905, -81.96053171279903893 ) ) ;
#67717=DIRECTION ( 'NONE',  ( 1.000000000000000000, 0.000000000000000000, 0.000000000000000000 ) ) ;
#67718=DIRECTION ( 'NONE',  ( -1.000000000000000000, -0.000000000000000000, 0.000000000000000000 ) ) ;
#67723=LINE ( 'NONE', #44427, #54775 ) ;
#67726=EDGE_CURVE ( 'NONE', #17422, #21235, #66740, .T. ) ;
#67739=CARTESIAN_POINT ( 'NONE',  ( 10.00000000000000000, -28.89263327155797967, 71.91182617369179297 ) ) ;
#67745=CARTESIAN_POINT ( 'NONE',  ( 0.000000000000000000, 74.65491531819118620, 23.16904090965733332 ) ) ;
#67751=DIRECTION ( 'NONE',  ( -1.000000000000000000, 0.000000000000000000, 0.000000000000000000 ) ) ;
#67752=ORIENTED_EDGE ( 'NONE', *, *, #61650, .F. ) ;
#67753=CARTESIAN_POINT ( 'NONE',  ( 0.000000000000000000, -78.73519480814971416, 22.90783923731600069 ) ) ;
#67754=CARTESIAN_POINT ( 'NONE',  ( 0.000000000000000000, -31.47745569255189224, 68.26794271651249346 ) ) ;
#67757=VECTOR ( 'NONE', #74022, 1000.000000000000000 ) ;
#67763=EDGE_CURVE ( 'NONE', #46797, #71305, #45175, .T. ) ;
#67768=CARTESIAN_POINT ( 'NONE',  ( 10.00000000000000000, -26.01480285779785362, -70.53064760720343429 ) ) ;
#67772=EDGE_LOOP ( 'NONE', ( #64037, #73624, #2068, #52317 ) ) ;
#67777=ORIENTED_EDGE ( 'NONE', *, *, #57597, .F. ) ;
#67780=ORIENTED_EDGE ( 'NONE', *, *, #46764, .F. ) ;
#67782=CARTESIAN_POINT ( 'NONE',  ( 10.00000000000000000, 74.18225833017937987, -34.94270380257560049 ) ) ;
#67783=CYLINDRICAL_SURFACE ( 'NONE', #18921, 77.49899999999999523 ) ;
#67790=VECTOR ( 'NONE', #18388, 1000.000000000000000 ) ;
#67796=CARTESIAN_POINT ( 'NONE',  ( 10.00000000000000000, 34.44570377933598593, 69.42325613327452061 ) ) ;
#67809=DIRECTION ( 'NONE',  ( 0.000000000000000000, 0.000000000000000000, 1.000000000000000000 ) ) ;
#67825=DIRECTION ( 'NONE',  ( -1.000000000000000000, 0.000000000000000000, 0.000000000000000000 ) ) ;
#67850=CIRCLE ( 'NONE', #31820, 82.00000000000000000 ) ;
#67854=CYLINDRICAL_SURFACE ( 'NONE', #40676, 31.99999999999999289 ) ;
#67859=ORIENTED_EDGE ( 'NONE', *, *, #33411, .F. ) ;
#67862=ORIENTED_EDGE ( 'NONE', *, *, #67325, .T. ) ;
#67865=ORIENTED_EDGE ( 'NONE', *, *, #17994, .T. ) ;
#67881=VECTOR ( 'NONE', #43803, 1000.000000000000000 ) ;
#67882=CARTESIAN_POINT ( 'NONE',  ( 5.000000000000000000, -67.80270845531921964, 46.11716303203163392 ) ) ;
#67885=FACE_OUTER_BOUND ( 'NONE', #34585, .T. ) ;
#67886=EDGE_CURVE ( 'NONE', #45326, #34583, #28352, .T. ) ;
#67903=LINE ( 'NONE', #39333, #61311 ) ;
#67904=ORIENTED_EDGE ( 'NONE', *, *, #13982, .F. ) ;
#67905=DIRECTION ( 'NONE',  ( -1.000000000000000000, -0.000000000000000000, -0.000000000000000000 ) ) ;
#67932=DIRECTION ( 'NONE',  ( 0.000000000000000000, 0.000000000000000000, -1.000000000000000000 ) ) ;
#67935=AXIS2_PLACEMENT_3D ( 'NONE', #910, #41102, #13618 ) ;
#67941=CARTESIAN_POINT ( 'NONE',  ( 10.00000000000000000, -76.41127070299262414, -12.93880638057396304 ) ) ;
#67948=DIRECTION ( 'NONE',  ( 0.000000000000000000, 0.000000000000000000, 1.000000000000000000 ) ) ;
#67951=ORIENTED_EDGE ( 'NONE', *, *, #4721, .T. ) ;
#67952=ORIENTED_EDGE ( 'NONE', *, *, #49704, .T. ) ;
#67967=CARTESIAN_POINT ( 'NONE',  ( 0.000000000000000000, 0.000000000000000000, 0.000000000000000000 ) ) ;
#67980=CARTESIAN_POINT ( 'NONE',  ( 5.000000000000002665, 2.543863470249527303, -81.96053171279901051 ) ) ;
#67983=VERTEX_POINT ( 'NONE', #23090 ) ;
#67989=ORIENTED_EDGE ( 'NONE', *, *, #28854, .T. ) ;
#67993=AXIS2_PLACEMENT_3D ( 'NONE', #42894, #60559, #31959 ) ;
#67994=ORIENTED_EDGE ( 'NONE', *, *, #71768, .T. ) ;
#68004=DIRECTION ( 'NONE',  ( 0.000000000000000000, 0.9510565162951523099, 0.3090169943749513926 ) ) ;
#68006=CYLINDRICAL_SURFACE ( 'NONE', #19480, 32.00000000000000000 ) ;
#68022=AXIS2_PLACEMENT_3D ( 'NONE', #26736, #55319, #33116 ) ;
#68026=DIRECTION ( 'NONE',  ( 0.000000000000000000, -0.9876883405951359940, -0.1564344650402420267 ) ) ;
#68037=DIRECTION ( 'NONE',  ( -1.000000000000000000, -0.000000000000000000, -0.000000000000000000 ) ) ;
#68055=ORIENTED_EDGE ( 'NONE', *, *, #2771, .T. ) ;
#68056=CARTESIAN_POINT ( 'NONE',  ( 10.00000000000000000, 54.21277698773675979, 55.38113227695801299 ) ) ;
#68063=CIRCLE ( 'NONE', #54861, 31.99999999999999645 ) ;
#68064=ORIENTED_EDGE ( 'NONE', *, *, #32516, .T. ) ;
#68073=AXIS2_PLACEMENT_3D ( 'NONE', #40206, #63889, #46219 ) ;
#68075=AXIS2_PLACEMENT_3D ( 'NONE', #18229, #30605, #12585 ) ;
#68083=AXIS2_PLACEMENT_3D ( 'NONE', #473, #46300, #40660 ) ;
#68084=ORIENTED_EDGE ( 'NONE', *, *, #22354, .F. ) ;
#68087=ORIENTED_EDGE ( 'NONE', *, *, #53406, .F. ) ;
#68095=CARTESIAN_POINT ( 'NONE',  ( 0.000000000000000000, 66.50666863322055633, -39.78640506895536078 ) ) ;
#68096=AXIS2_PLACEMENT_3D ( 'NONE', #26521, #31046, #2888 ) ;
#68114=DIRECTION ( 'NONE',  ( 0.000000000000000000, -0.9723699203976740035, -0.2334453638559160216 ) ) ;
#68116=ORIENTED_EDGE ( 'NONE', *, *, #9582, .F. ) ;
#68123=LINE ( 'NONE', #73375, #24600 ) ;
#68129=ORIENTED_EDGE ( 'NONE', *, *, #19751, .T. ) ;
#68132=ORIENTED_EDGE ( 'NONE', *, *, #57472, .T. ) ;
#68137=ORIENTED_EDGE ( 'NONE', *, *, #37157, .F. ) ;
#68138=CARTESIAN_POINT ( 'NONE',  ( 10.00000000000000000, -74.18225833017864090, -34.94270380257719211 ) ) ;
#68140=VECTOR ( 'NONE', #73581, 1000.000000000000000 ) ;
#68151=CARTESIAN_POINT ( 'NONE',  ( 10.00000000000000000, 74.65491531819105830, 8.830959090343693418 ) ) ;
#68178=DIRECTION ( 'NONE',  ( 0.000000000000000000, 0.000000000000000000, 1.000000000000000000 ) ) ;
#68184=EDGE_CURVE ( 'NONE', #7708, #70437, #33173, .T. ) ;
#68197=DIRECTION ( 'NONE',  ( -1.000000000000000000, -0.000000000000000000, -0.000000000000000000 ) ) ;
#68199=CARTESIAN_POINT ( 'NONE',  ( 10.00000000000000000, 81.50828551894225882, 8.966570791700975818 ) ) ;
#68204=CARTESIAN_POINT ( 'NONE',  ( 0.000000000000000000, -77.16300072079641836, -27.74655509720751567 ) ) ;
#68224=ORIENTED_EDGE ( 'NONE', *, *, #50828, .F. ) ;
#68230=AXIS2_PLACEMENT_3D ( 'NONE', #73079, #44912, #10683 ) ;
#68235=EDGE_CURVE ( 'NONE', #23492, #17876, #48794, .T. ) ;
#68236=ORIENTED_EDGE ( 'NONE', *, *, #14699, .F. ) ;
#68237=ORIENTED_EDGE ( 'NONE', *, *, #62510, .F. ) ;
#68244=DIRECTION ( 'NONE',  ( 0.000000000000000000, 0.000000000000000000, -1.000000000000000000 ) ) ;
#68247=LINE ( 'NONE', #21626, #52573 ) ;
#68259=CARTESIAN_POINT ( 'NONE',  ( 10.00000000000000000, -80.28980883073744224, -16.65972982745018882 ) ) ;
#68261=EDGE_CURVE ( 'NONE', #4576, #33591, #42794, .T. ) ;
#68282=EDGE_CURVE ( 'NONE', #70758, #11833, #63214, .T. ) ;
#68291=ORIENTED_EDGE ( 'NONE', *, *, #301, .F. ) ;
#68292=AXIS2_PLACEMENT_3D ( 'NONE', #12575, #5847, #46806 ) ;
#68316=AXIS2_PLACEMENT_3D ( 'NONE', #15419, #66572, #45129 ) ;
#68326=EDGE_CURVE ( 'NONE', #11648, #26342, #66790, .T. ) ;
#68331=FACE_OUTER_BOUND ( 'NONE', #27098, .T. ) ;
#68348=CARTESIAN_POINT ( 'NONE',  ( 10.00000000000000000, 0.000000000000000000, 0.000000000000000000 ) ) ;
#68349=VECTOR ( 'NONE', #44742, 1000.000000000000000 ) ;
#68355=ORIENTED_EDGE ( 'NONE', *, *, #66041, .T. ) ;
#68366=CIRCLE ( 'NONE', #46732, 31.99999999999999289 ) ;
#68370=DIRECTION ( 'NONE',  ( 0.000000000000000000, 0.000000000000000000, 1.000000000000000000 ) ) ;
#68371=VERTEX_POINT ( 'NONE', #62398 ) ;
#68379=ORIENTED_EDGE ( 'NONE', *, *, #44659, .F. ) ;
#68388=ORIENTED_EDGE ( 'NONE', *, *, #52349, .F. ) ;
#68390=CARTESIAN_POINT ( 'NONE',  ( 0.000000000000000000, -66.50666863322028632, 39.78640506895582973 ) ) ;
#68401=LINE ( 'NONE', #16891, #24282 ) ;
#68409=DIRECTION ( 'NONE',  ( -1.000000000000000000, -0.000000000000000000, 0.000000000000000000 ) ) ;
#68421=AXIS2_PLACEMENT_3D ( 'NONE', #5118, #61880, #56233 ) ;
#68426=ORIENTED_EDGE ( 'NONE', *, *, #39248, .T. ) ;
#68429=ORIENTED_EDGE ( 'NONE', *, *, #60727, .F. ) ;
#68435=VERTEX_POINT ( 'NONE', #32908 ) ;
#68439=DIRECTION ( 'NONE',  ( 1.000000000000000000, 0.000000000000000000, 0.000000000000000000 ) ) ;
#68451=CIRCLE ( 'NONE', #2429, 31.99999999999999645 ) ;
#68455=CYLINDRICAL_SURFACE ( 'NONE', #41453, 82.00000000000000000 ) ;
#68456=ORIENTED_EDGE ( 'NONE', *, *, #40080, .T. ) ;
#68457=ORIENTED_EDGE ( 'NONE', *, *, #21301, .T. ) ;
#68460=CARTESIAN_POINT ( 'NONE',  ( 0.000000000000000000, -59.46389618801999433, 49.70050353004867816 ) ) ;
#68464=CARTESIAN_POINT ( 'NONE',  ( 0.000000000000000000, -64.81221759200379040, 50.23322058963324110 ) ) ;
#68469=FACE_OUTER_BOUND ( 'NONE', #19803, .T. ) ;
#68480=CIRCLE ( 'NONE', #24036, 31.99999999999999289 ) ;
#68485=CARTESIAN_POINT ( 'NONE',  ( 0.000000000000000000, 81.96053171279902472, -2.543863470248670211 ) ) ;
#68488=CARTESIAN_POINT ( 'NONE',  ( 10.00000000000000000, 0.000000000000000000, 0.000000000000000000 ) ) ;
#68489=CARTESIAN_POINT ( 'NONE',  ( -10.00000000000000000, 0.000000000000000000, 0.000000000000000000 ) ) ;
#68503=CARTESIAN_POINT ( 'NONE',  ( 10.00000000000000000, 31.47745569255237896, -68.26794271651228030 ) ) ;
#68505=CARTESIAN_POINT ( 'NONE',  ( 0.000000000000000000, -24.73286445877653961, -73.44644590900085745 ) ) ;
#68526=DIRECTION ( 'NONE',  ( -1.000000000000000000, 0.000000000000000000, 0.000000000000000000 ) ) ;
#68530=LINE ( 'NONE', #29024, #72813 ) ;
#68531=EDGE_CURVE ( 'NONE', #19857, #47239, #4396, .T. ) ;
#68558=DIRECTION ( 'NONE',  ( -1.000000000000000000, 0.000000000000000000, -0.000000000000000000 ) ) ;
#68559=DIRECTION ( 'NONE',  ( 0.000000000000000000, -0.8526401643540859610, -0.5224985647159591240 ) ) ;
#68562=DIRECTION ( 'NONE',  ( -1.000000000000000000, 0.000000000000000000, 0.000000000000000000 ) ) ;
#68566=FACE_OUTER_BOUND ( 'NONE', #51681, .T. ) ;
#68580=VERTEX_POINT ( 'NONE', #40416 ) ;
#68585=DIRECTION ( 'NONE',  ( -1.000000000000000000, 0.000000000000000000, -0.000000000000000000 ) ) ;
#68587=AXIS2_PLACEMENT_3D ( 'NONE', #56350, #50317, #44706 ) ;
#68590=DIRECTION ( 'NONE',  ( -1.000000000000000000, 0.000000000000000000, 0.000000000000000000 ) ) ;
#68592=AXIS2_PLACEMENT_3D ( 'NONE', #30738, #59705, #13083 ) ;
#68596=CARTESIAN_POINT ( 'NONE',  ( 0.000000000000000000, 14.66109333815460225, 73.73191006444577056 ) ) ;
#68597=VERTEX_POINT ( 'NONE', #4751 ) ;
#68602=DIRECTION ( 'NONE',  ( 0.000000000000000000, 0.000000000000000000, -1.000000000000000000 ) ) ;
#68624=ORIENTED_EDGE ( 'NONE', *, *, #47975, .F. ) ;
#68648=ORIENTED_EDGE ( 'NONE', *, *, #65617, .F. ) ;
#68651=CARTESIAN_POINT ( 'NONE',  ( 10.00000000000000000, 17.28742895386191236, -75.54627589209927407 ) ) ;
#68658=ORIENTED_EDGE ( 'NONE', *, *, #34652, .T. ) ;
#68664=ORIENTED_EDGE ( 'NONE', *, *, #70191, .T. ) ;
#68667=AXIS2_PLACEMENT_3D ( 'NONE', #63483, #11960, #367 ) ;
#68671=EDGE_CURVE ( 'NONE', #52624, #23895, #24865, .T. ) ;
#68677=DIRECTION ( 'NONE',  ( 0.000000000000000000, 0.2334453638558991184, 0.9723699203976781114 ) ) ;
#68690=AXIS2_PLACEMENT_3D ( 'NONE', #67346, #43691, #22228 ) ;
#68695=ORIENTED_EDGE ( 'NONE', *, *, #31668, .F. ) ;
#68701=ADVANCED_FACE ( 'NONE', ( #67885 ), #51322, .T. ) ;
#68702=ADVANCED_FACE ( 'NONE', ( #23501 ), #12943, .T. ) ;
#68716=CIRCLE ( 'NONE', #55507, 31.99999999999999289 ) ;
#68733=AXIS2_PLACEMENT_3D ( 'NONE', #49119, #55131, #20556 ) ;
#68763=CARTESIAN_POINT ( 'NONE',  ( 0.000000000000000000, -46.53671651293991118, 59.03961581697383565 ) ) ;
#68768=EDGE_CURVE ( 'NONE', #28823, #32140, #32045, .T. ) ;
#68773=DIRECTION ( 'NONE',  ( -1.000000000000000000, 0.000000000000000000, 0.000000000000000000 ) ) ;
#68782=AXIS2_PLACEMENT_3D ( 'NONE', #74331, #67209, #5561 ) ;
#68788=CYLINDRICAL_SURFACE ( 'NONE', #65451, 32.00000000000000000 ) ;
#68790=AXIS2_PLACEMENT_3D ( 'NONE', #45275, #68197, #16693 ) ;
#68809=VERTEX_POINT ( 'NONE', #18592 ) ;
#68813=FACE_OUTER_BOUND ( 'NONE', #69369, .T. ) ;
#68815=DIRECTION ( 'NONE',  ( -1.000000000000000000, 0.000000000000000000, 0.000000000000000000 ) ) ;
#68816=EDGE_LOOP ( 'NONE', ( #12334, #31791, #13508, #55581 ) ) ;
#68818=ORIENTED_EDGE ( 'NONE', *, *, #22344, .T. ) ;
#68822=ORIENTED_EDGE ( 'NONE', *, *, #38128, .T. ) ;
#68823=CIRCLE ( 'NONE', #15995, 77.49899999999999523 ) ;
#68833=VERTEX_POINT ( 'NONE', #62007 ) ;
#68836=EDGE_LOOP ( 'NONE', ( #20507, #48214, #12363, #29885 ) ) ;
#68845=DIRECTION ( 'NONE',  ( 0.000000000000000000, 0.000000000000000000, 1.000000000000000000 ) ) ;
#68852=FACE_OUTER_BOUND ( 'NONE', #50772, .T. ) ;
#68856=EDGE_CURVE ( 'NONE', #49560, #31776, #36833, .T. ) ;
#68865=EDGE_CURVE ( 'NONE', #55001, #56348, #71652, .T. ) ;
#68867=EDGE_CURVE ( 'NONE', #38604, #8405, #45291, .T. ) ;
#68877=CARTESIAN_POINT ( 'NONE',  ( 10.00000000000000000, 31.46837873495072913, -68.27212725128242710 ) ) ;
#68888=ORIENTED_EDGE ( 'NONE', *, *, #36061, .T. ) ;
#68896=ADVANCED_FACE ( 'NONE', ( #23179 ), #69039, .T. ) ;
#68897=ORIENTED_EDGE ( 'NONE', *, *, #11299, .F. ) ;
#68904=EDGE_LOOP ( 'NONE', ( #55851, #22294, #13950, #33890 ) ) ;
#68909=CARTESIAN_POINT ( 'NONE',  ( 0.000000000000000000, -8.830959090342926032, 74.65491531819115778 ) ) ;
#68917=VERTEX_POINT ( 'NONE', #57019 ) ;
#68930=DIRECTION ( 'NONE',  ( 0.000000000000000000, 0.000000000000000000, 1.000000000000000000 ) ) ;
#68934=VECTOR ( 'NONE', #71825, 1000.000000000000000 ) ;
#68942=VECTOR ( 'NONE', #49184, 1000.000000000000000 ) ;
#68952=DIRECTION ( 'NONE',  ( -1.000000000000000000, 0.000000000000000000, -0.000000000000000000 ) ) ;
#68961=DIRECTION ( 'NONE',  ( 0.000000000000000000, 0.000000000000000000, 1.000000000000000000 ) ) ;
#68974=CARTESIAN_POINT ( 'NONE',  ( 10.00000000000000000, -59.46389618801928378, -49.70050353004953791 ) ) ;
#68975=AXIS2_PLACEMENT_3D ( 'NONE', #43205, #60847, #31519 ) ;
#68980=VERTEX_POINT ( 'NONE', #36660 ) ;
#68981=AXIS2_PLACEMENT_3D ( 'NONE', #18668, #70913, #29569 ) ;
#68988=EDGE_LOOP ( 'NONE', ( #5109, #40624, #58239, #23133 ) ) ;
#68989=EDGE_CURVE ( 'NONE', #21157, #7122, #19367, .T. ) ;
#69004=ORIENTED_EDGE ( 'NONE', *, *, #28718, .T. ) ;
#69008=VERTEX_POINT ( 'NONE', #13358 ) ;
#69037=DIRECTION ( 'NONE',  ( 0.000000000000000000, 0.000000000000000000, -1.000000000000000000 ) ) ;
#69039=CYLINDRICAL_SURFACE ( 'NONE', #63259, 32.00000000000000000 ) ;
#69041=CARTESIAN_POINT ( 'NONE',  ( 10.00000000000000000, -46.21855187248673502, 62.20884554314003623 ) ) ;
#69042=DIRECTION ( 'NONE',  ( -1.000000000000000000, 0.000000000000000000, 0.000000000000000000 ) ) ;
#69048=AXIS2_PLACEMENT_3D ( 'NONE', #9637, #69908, #72409 ) ;
#69058=ORIENTED_EDGE ( 'NONE', *, *, #16645, .T. ) ;
#69063=DIRECTION ( 'NONE',  ( -1.000000000000000000, 0.000000000000000000, 0.000000000000000000 ) ) ;
#69066=ORIENTED_EDGE ( 'NONE', *, *, #12947, .T. ) ;
#69067=ORIENTED_EDGE ( 'NONE', *, *, #34645, .T. ) ;
#69072=CARTESIAN_POINT ( 'NONE',  ( 0.000000000000000000, 0.000000000000000000, 0.000000000000000000 ) ) ;
#69075=EDGE_CURVE ( 'NONE', #41590, #36758, #52466, .T. ) ;
#69079=VERTEX_POINT ( 'NONE', #25392 ) ;
#69085=ADVANCED_FACE ( 'NONE', ( #20103 ), #71975, .T. ) ;
#69096=EDGE_CURVE ( 'NONE', #65189, #46694, #32119, .T. ) ;
#69123=DIRECTION ( 'NONE',  ( 1.000000000000000000, -0.000000000000000000, 0.000000000000000000 ) ) ;
#69125=VERTEX_POINT ( 'NONE', #72352 ) ;
#69128=CARTESIAN_POINT ( 'NONE',  ( -10.00000000000000000, 0.000000000000000000, 0.000000000000000000 ) ) ;
#69135=CARTESIAN_POINT ( 'NONE',  ( 10.00000000000000000, -8.840884882374576037, -74.65374052328658649 ) ) ;
#69138=DIRECTION ( 'NONE',  ( 0.000000000000000000, -0.3090169943749548898, 0.9510565162951511997 ) ) ;
#69141=EDGE_CURVE ( 'NONE', #3975, #29598, #51319, .T. ) ;
#69146=CARTESIAN_POINT ( 'NONE',  ( 0.000000000000000000, 20.41045688087930898, -72.35160999960793049 ) ) ;
#69151=CARTESIAN_POINT ( 'NONE',  ( 10.00000000000000000, 75.11725578898467859, 2.956366410620910656 ) ) ;
#69159=EDGE_LOOP ( 'NONE', ( #2243, #8706, #4742, #24623 ) ) ;
#69167=DIRECTION ( 'NONE',  ( -1.000000000000000000, 0.000000000000000000, 0.000000000000000000 ) ) ;
#69181=VERTEX_POINT ( 'NONE', #14841 ) ;
#69187=DIRECTION ( 'NONE',  ( 0.000000000000000000, -0.9969173337331270757, -0.07845909572785580988 ) ) ;
#69190=ORIENTED_EDGE ( 'NONE', *, *, #69867, .T. ) ;
#69198=CARTESIAN_POINT ( 'NONE',  ( 0.000000000000000000, 0.000000000000000000, 0.000000000000000000 ) ) ;
#69200=ORIENTED_EDGE ( 'NONE', *, *, #51278, .F. ) ;
#69202=DIRECTION ( 'NONE',  ( -1.000000000000000000, -0.000000000000000000, 0.000000000000000000 ) ) ;
#69206=DIRECTION ( 'NONE',  ( 0.000000000000000000, 0.000000000000000000, -1.000000000000000000 ) ) ;
#69208=EDGE_CURVE ( 'NONE', #35339, #72850, #74127, .T. ) ;
#69215=DIRECTION ( 'NONE',  ( 0.000000000000000000, 0.9969173337331276308, 0.07845909572784864894 ) ) ;
#69223=CARTESIAN_POINT ( 'NONE',  ( 10.00000000000000000, -72.35432306680498016, 20.40083707022857951 ) ) ;
#69254=ORIENTED_EDGE ( 'NONE', *, *, #27061, .F. ) ;
#69258=EDGE_CURVE ( 'NONE', #47069, #2989, #2153, .T. ) ;
#69259=ORIENTED_EDGE ( 'NONE', *, *, #9260, .F. ) ;
#69262=ORIENTED_EDGE ( 'NONE', *, *, #6539, .F. ) ;
#69267=VERTEX_POINT ( 'NONE', #23094 ) ;
#69273=DIRECTION ( 'NONE',  ( 0.000000000000000000, -0.9238795325112821866, -0.3826834323651006065 ) ) ;
#69276=CARTESIAN_POINT ( 'NONE',  ( -10.00000000000000000, 0.000000000000000000, 0.000000000000000000 ) ) ;
#69283=ORIENTED_EDGE ( 'NONE', *, *, #4156, .T. ) ;
#69291=CARTESIAN_POINT ( 'NONE',  ( 10.00000000000000178, 0.000000000000000000, 0.000000000000000000 ) ) ;
#69298=DIRECTION ( 'NONE',  ( -1.000000000000000000, 0.000000000000000000, 0.000000000000000000 ) ) ;
#69306=VECTOR ( 'NONE', #52622, 1000.000000000000000 ) ;
#69311=LINE ( 'NONE', #17797, #50071 ) ;
#69326=ORIENTED_EDGE ( 'NONE', *, *, #27418, .F. ) ;
#69333=EDGE_CURVE ( 'NONE', #11928, #72369, #44143, .T. ) ;
#69338=CARTESIAN_POINT ( 'NONE',  ( 0.000000000000000000, 73.72996012237440766, 14.67089635893739619 ) ) ;
#69340=EDGE_LOOP ( 'NONE', ( #56562, #35520, #63161, #53641 ) ) ;
#69366=EDGE_LOOP ( 'NONE', ( #20229, #27555, #45803, #69713 ) ) ;
#69369=EDGE_LOOP ( 'NONE', ( #39770, #68379, #33470, #33542 ) ) ;
#69370=EDGE_CURVE ( 'NONE', #72558, #72136, #10314, .T. ) ;
#69377=CARTESIAN_POINT ( 'NONE',  ( 0.000000000000000000, 31.46837873495072913, -68.27212725128242710 ) ) ;
#69380=CIRCLE ( 'NONE', #28574, 77.49899999999999523 ) ;
#69396=FACE_OUTER_BOUND ( 'NONE', #30047, .T. ) ;
#69403=DIRECTION ( 'NONE',  ( 0.000000000000000000, 0.3826834323650907810, -0.9238795325112864054 ) ) ;
#69414=LINE ( 'NONE', #65549, #38461 ) ;
#69419=VECTOR ( 'NONE', #59837, 1000.000000000000000 ) ;
#69431=CYLINDRICAL_SURFACE ( 'NONE', #8673, 82.00000000000000000 ) ;
#69433=DIRECTION ( 'NONE',  ( 0.000000000000000000, -0.4539904997395541875, 0.8910065241883642351 ) ) ;
#69435=ORIENTED_EDGE ( 'NONE', *, *, #31331, .T. ) ;
#69436=ORIENTED_EDGE ( 'NONE', *, *, #73226, .T. ) ;
#69438=EDGE_LOOP ( 'NONE', ( #55282, #17577, #44569, #11128 ) ) ;
#69451=ORIENTED_EDGE ( 'NONE', *, *, #18930, .F. ) ;
#69458=AXIS2_PLACEMENT_3D ( 'NONE', #12529, #29077, #24921 ) ;
#69477=CARTESIAN_POINT ( 'NONE',  ( 0.000000000000000000, 0.8261519478441983200, -77.49459641780885022 ) ) ;
#69483=AXIS2_PLACEMENT_3D ( 'NONE', #17295, #63547, #63182 ) ;
#69484=CARTESIAN_POINT ( 'NONE',  ( 0.000000000000000000, -33.71516098798685590, -74.74816331893465815 ) ) ;
#69486=CARTESIAN_POINT ( 'NONE',  ( -10.00000000000000000, 0.000000000000000000, 0.000000000000000000 ) ) ;
#69488=CARTESIAN_POINT ( 'NONE',  ( 10.00000000000000000, 75.54627589209970040, -17.28742895386005785 ) ) ;
#69496=DIRECTION ( 'NONE',  ( 0.000000000000000000, 0.000000000000000000, 1.000000000000000000 ) ) ;
#69503=CIRCLE ( 'NONE', #1124, 31.99999999999999289 ) ;
#69505=VERTEX_POINT ( 'NONE', #12894 ) ;
#69508=CYLINDRICAL_SURFACE ( 'NONE', #29874, 31.99999999999998579 ) ;
#69509=AXIS2_PLACEMENT_3D ( 'NONE', #22759, #33259, #3983 ) ;
#69512=CARTESIAN_POINT ( 'NONE',  ( 10.00000000000000000, 80.28980883073779751, -16.65972982744850839 ) ) ;
#69517=CARTESIAN_POINT ( 'NONE',  ( 50.00005079999999680, 0.000000000000000000, 0.000000000000000000 ) ) ;
#69519=EDGE_CURVE ( 'NONE', #27817, #70179, #69311, .T. ) ;
#69526=AXIS2_PLACEMENT_3D ( 'NONE', #25677, #66645, #15127 ) ;
#69530=EDGE_CURVE ( 'NONE', #39290, #4576, #3326, .T. ) ;
#69532=ORIENTED_EDGE ( 'NONE', *, *, #30466, .F. ) ;
#69541=ORIENTED_EDGE ( 'NONE', *, *, #8196, .T. ) ;
#69543=EDGE_CURVE ( 'NONE', #24805, #2169, #60268, .T. ) ;
#69548=EDGE_CURVE ( 'NONE', #71438, #4362, #8749, .T. ) ;
#69552=DIRECTION ( 'NONE',  ( -1.000000000000000000, -0.000000000000000000, 0.000000000000000000 ) ) ;
#69553=ORIENTED_EDGE ( 'NONE', *, *, #18737, .T. ) ;
#69559=ORIENTED_EDGE ( 'NONE', *, *, #14772, .T. ) ;
#69567=CYLINDRICAL_SURFACE ( 'NONE', #17625, 77.49899999999999523 ) ;
#69570=CIRCLE ( 'NONE', #1198, 31.99999999999999289 ) ;
#69571=VECTOR ( 'NONE', #30987, 1000.000000000000000 ) ;
#69572=AXIS2_PLACEMENT_3D ( 'NONE', #25636, #42203, #42565 ) ;
#69580=CARTESIAN_POINT ( 'NONE',  ( 0.000000000000000000, 0.000000000000000000, 0.000000000000000000 ) ) ;
#69590=EDGE_CURVE ( 'NONE', #17276, #43589, #71752, .T. ) ;
#69601=CARTESIAN_POINT ( 'NONE',  ( 10.00000000000000000, 73.44644590900061587, 24.73286445877730699 ) ) ;
#69602=CYLINDRICAL_SURFACE ( 'NONE', #38250, 77.49899999999999523 ) ;
#69616=ORIENTED_EDGE ( 'NONE', *, *, #54069, .T. ) ;
#69619=ADVANCED_FACE ( 'NONE', ( #59516 ), #14382, .T. ) ;
#69622=ORIENTED_EDGE ( 'NONE', *, *, #18105, .F. ) ;
#69625=ORIENTED_EDGE ( 'NONE', *, *, #664, .F. ) ;
#69639=CARTESIAN_POINT ( 'NONE',  ( 10.00000000000000000, -15.33399622253540251, 80.55351364060582853 ) ) ;
#69649=EDGE_LOOP ( 'NONE', ( #1329, #52537, #45531, #35599 ) ) ;
#69652=ORIENTED_EDGE ( 'NONE', *, *, #66544, .F. ) ;
#69661=DIRECTION ( 'NONE',  ( 0.000000000000000000, 0.000000000000000000, -1.000000000000000000 ) ) ;
#69662=CIRCLE ( 'NONE', #24050, 31.99999999999998579 ) ;
#69664=ORIENTED_EDGE ( 'NONE', *, *, #44379, .F. ) ;
#69667=LINE ( 'NONE', #17426, #18698 ) ;
#69681=VECTOR ( 'NONE', #65759, 1000.000000000000000 ) ;
#69689=CARTESIAN_POINT ( 'NONE',  ( -10.00000000000000000, 0.000000000000000000, 0.000000000000000000 ) ) ;
#69707=EDGE_CURVE ( 'NONE', #25328, #17282, #63363, .T. ) ;
#69711=DIRECTION ( 'NONE',  ( -1.000000000000000000, -0.000000000000000000, 0.000000000000000000 ) ) ;
#69713=ORIENTED_EDGE ( 'NONE', *, *, #19924, .T. ) ;
#69738=CARTESIAN_POINT ( 'NONE',  ( 0.000000000000000000, -80.55351364060599906, 15.33399622253456585 ) ) ;
#69743=ORIENTED_EDGE ( 'NONE', *, *, #73152, .T. ) ;
#69749=VERTEX_POINT ( 'NONE', #61367 ) ;
#69750=EDGE_CURVE ( 'NONE', #49474, #29034, #15359, .T. ) ;
#69766=CARTESIAN_POINT ( 'NONE',  ( 10.00000000000000000, 0.000000000000000000, 0.000000000000000000 ) ) ;
#69782=ORIENTED_EDGE ( 'NONE', *, *, #24809, .F. ) ;
#69786=DIRECTION ( 'NONE',  ( 0.000000000000000000, 0.000000000000000000, -1.000000000000000000 ) ) ;
#69794=DIRECTION ( 'NONE',  ( 0.000000000000000000, 0.000000000000000000, 1.000000000000000000 ) ) ;
#69799=ORIENTED_EDGE ( 'NONE', *, *, #72700, .T. ) ;
#69801=ORIENTED_EDGE ( 'NONE', *, *, #71131, .F. ) ;
#69825=DIRECTION ( 'NONE',  ( -1.000000000000000000, 0.000000000000000000, 0.000000000000000000 ) ) ;
#69830=ADVANCED_FACE ( 'NONE', ( #6804 ), #24468, .T. ) ;
#69834=CARTESIAN_POINT ( 'NONE',  ( 0.000000000000000000, 23.16143007188532366, -73.95703589263949596 ) ) ;
#69852=DIRECTION ( 'NONE',  ( -1.000000000000000000, 0.000000000000000000, 0.000000000000000000 ) ) ;
#69867=EDGE_CURVE ( 'NONE', #1870, #66997, #6938, .T. ) ;
#69873=AXIS2_PLACEMENT_3D ( 'NONE', #6357, #40193, #29257 ) ;
#69881=EDGE_LOOP ( 'NONE', ( #31486, #1453, #49106, #4597 ) ) ;
#69886=CIRCLE ( 'NONE', #29104, 31.99999999999999289 ) ;
#69889=AXIS2_PLACEMENT_3D ( 'NONE', #37390, #48287, #71944 ) ;
#69897=DIRECTION ( 'NONE',  ( -1.000000000000000000, 0.000000000000000000, 0.000000000000000000 ) ) ;
#69898=CARTESIAN_POINT ( 'NONE',  ( 10.00000000000000000, 68.67312586195046720, -35.91791733033402068 ) ) ;
#69899=ADVANCED_FACE ( 'NONE', ( #23724 ), #24832, .T. ) ;
#69903=ORIENTED_EDGE ( 'NONE', *, *, #26337, .F. ) ;
#69908=DIRECTION ( 'NONE',  ( -1.000000000000000000, 0.000000000000000000, 0.000000000000000000 ) ) ;
#69918=CARTESIAN_POINT ( 'NONE',  ( 10.00000000000000000, 0.000000000000000000, 0.000000000000000000 ) ) ;
#69921=CARTESIAN_POINT ( 'NONE',  ( 0.000000000000000000, -46.21855187248673502, 62.20884554314003623 ) ) ;
#69924=CARTESIAN_POINT ( 'NONE',  ( 10.00000000000000000, -72.35432306680498016, 20.40083707022857951 ) ) ;
#69925=CYLINDRICAL_SURFACE ( 'NONE', #9194, 82.00000000000000000 ) ;
#69942=DIRECTION ( 'NONE',  ( 0.000000000000000000, 0.000000000000000000, 1.000000000000000000 ) ) ;
#69958=CARTESIAN_POINT ( 'NONE',  ( 5.000000000000002665, -29.01471420065507090, -76.69515212746047439 ) ) ;
#69968=PRODUCT_DEFINITION_FORMATION_WITH_SPECIFIED_SOURCE ( 'ANY', '', #27159, .NOT_KNOWN. ) ;
#69969=EDGE_LOOP ( 'NONE', ( #1708, #71793, #40397, #6776 ) ) ;
#69970=DIRECTION ( 'NONE',  ( -1.000000000000000000, -0.000000000000000000, -0.000000000000000000 ) ) ;
#69973=AXIS2_PLACEMENT_3D ( 'NONE', #48978, #14404, #2799 ) ;
#69974=ORIENTED_EDGE ( 'NONE', *, *, #45943, .T. ) ;
#69988=ORIENTED_EDGE ( 'NONE', *, *, #2782, .F. ) ;
#69989=VECTOR ( 'NONE', #9007, 1000.000000000000000 ) ;
#69999=EDGE_CURVE ( 'NONE', #16263, #4375, #49007, .T. ) ;
#70008=LINE ( 'NONE', #19619, #46774 ) ;
#70011=CYLINDRICAL_SURFACE ( 'NONE', #17630, 31.99999999999999289 ) ;
#70013=DIRECTION ( 'NONE',  ( 0.000000000000000000, 0.000000000000000000, 1.000000000000000000 ) ) ;
#70027=CARTESIAN_POINT ( 'NONE',  ( 0.000000000000000000, -2.946379043145784582, -75.11764819372150725 ) ) ;
#70034=CIRCLE ( 'NONE', #37635, 77.49899999999999523 ) ;
#70043=AXIS2_PLACEMENT_3D ( 'NONE', #7552, #48507, #25939 ) ;
#70049=CYLINDRICAL_SURFACE ( 'NONE', #34644, 82.00000000000000000 ) ;
#70061=CIRCLE ( 'NONE', #12434, 77.49900000000000944 ) ;
#70068=CIRCLE ( 'NONE', #60493, 31.99999999999999289 ) ;
#70074=VERTEX_POINT ( 'NONE', #50251 ) ;
#70081=DIRECTION ( 'NONE',  ( -1.000000000000000000, 0.000000000000000000, 0.000000000000000000 ) ) ;
#70085=DIRECTION ( 'NONE',  ( 0.000000000000000000, 0.1564344650402312020, -0.9876883405951376593 ) ) ;
#70109=ORIENTED_EDGE ( 'NONE', *, *, #58078, .T. ) ;
#70110=EDGE_CURVE ( 'NONE', #57325, #50561, #58616, .T. ) ;
#70112=CYLINDRICAL_SURFACE ( 'NONE', #8113, 31.99999999999998579 ) ;
#70114=DIRECTION ( 'NONE',  ( 0.000000000000000000, 0.000000000000000000, -1.000000000000000000 ) ) ;
#70118=CARTESIAN_POINT ( 'NONE',  ( 5.000000000000000000, -27.74655509720725988, 77.16300072079653205 ) ) ;
#70124=CARTESIAN_POINT ( 'NONE',  ( 0.000000000000000000, -72.35160999960801576, -20.41045688087902121 ) ) ;
#70125=DIRECTION ( 'NONE',  ( 0.000000000000000000, 0.000000000000000000, 1.000000000000000000 ) ) ;
#70127=DIRECTION ( 'NONE',  ( -1.000000000000000000, 0.000000000000000000, 0.000000000000000000 ) ) ;
#70134=ORIENTED_EDGE ( 'NONE', *, *, #60885, .F. ) ;
#70166=DIRECTION ( 'NONE',  ( 0.000000000000000000, 0.000000000000000000, 1.000000000000000000 ) ) ;
#70179=VERTEX_POINT ( 'NONE', #51747 ) ;
#70181=DIRECTION ( 'NONE',  ( 0.000000000000000000, 0.000000000000000000, 1.000000000000000000 ) ) ;
#70184=VERTEX_POINT ( 'NONE', #23188 ) ;
#70187=AXIS2_PLACEMENT_3D ( 'NONE', #57431, #45424, #33752 ) ;
#70190=DIRECTION ( 'NONE',  ( -1.000000000000000000, 0.000000000000000000, 0.000000000000000000 ) ) ;
#70191=EDGE_CURVE ( 'NONE', #41093, #47282, #32205, .T. ) ;
#70207=DIRECTION ( 'NONE',  ( 0.000000000000000000, 0.000000000000000000, 1.000000000000000000 ) ) ;
#70215=AXIS2_PLACEMENT_3D ( 'NONE', #13701, #24989, #41545 ) ;
#70219=AXIS2_PLACEMENT_3D ( 'NONE', #45285, #23814, #40005 ) ;
#70225=ADVANCED_FACE ( 'NONE', ( #63414 ), #40852, .T. ) ;
#70231=ORIENTED_EDGE ( 'NONE', *, *, #59933, .F. ) ;
#70238=VERTEX_POINT ( 'NONE', #55350 ) ;
#70243=FACE_OUTER_BOUND ( 'NONE', #73488, .T. ) ;
#70244=ORIENTED_EDGE ( 'NONE', *, *, #15956, .T. ) ;
#70255=DIRECTION ( 'NONE',  ( 0.000000000000000000, 0.07845909572784530439, -0.9969173337331279638 ) ) ;
#70260=EDGE_CURVE ( 'NONE', #688, #66304, #5836, .T. ) ;
#70262=VECTOR ( 'NONE', #15185, 1000.000000000000000 ) ;
#70266=CARTESIAN_POINT ( 'NONE',  ( 5.000000000000002665, -8.966570791700153364, -81.50828551894237251 ) ) ;
#70270=VERTEX_POINT ( 'NONE', #21127 ) ;
#70271=CARTESIAN_POINT ( 'NONE',  ( 10.00000000000000000, 81.90746397400394585, -3.894527615416976118 ) ) ;
#70283=ORIENTED_EDGE ( 'NONE', *, *, #38868, .F. ) ;
#70301=VECTOR ( 'NONE', #14047, 1000.000000000000000 ) ;
#70304=CARTESIAN_POINT ( 'NONE',  ( 10.00000000000000000, -41.76106447765533147, 62.50884508063410294 ) ) ;
#70306=AXIS2_PLACEMENT_3D ( 'NONE', #4068, #35745, #13558 ) ;
#70314=DIRECTION ( 'NONE',  ( 1.000000000000000000, 0.000000000000000000, 0.000000000000000000 ) ) ;
#70316=DIRECTION ( 'NONE',  ( 1.000000000000000000, 0.000000000000000000, 0.000000000000000000 ) ) ;
#70317=LINE ( 'NONE', #18822, #46228 ) ;
#70319=EDGE_CURVE ( 'NONE', #46797, #5511, #38060, .T. ) ;
#70320=CYLINDRICAL_SURFACE ( 'NONE', #35548, 77.49899999999999523 ) ;
#70322=CARTESIAN_POINT ( 'NONE',  ( 10.00000000000000000, 0.000000000000000000, 0.000000000000000000 ) ) ;
#70328=VERTEX_POINT ( 'NONE', #60989 ) ;
#70353=CARTESIAN_POINT ( 'NONE',  ( 10.00000000000000000, 24.73286445877808148, -73.44644590900034586 ) ) ;
#70355=CIRCLE ( 'NONE', #21148, 82.00000000000000000 ) ;
#70357=DIRECTION ( 'NONE',  ( -1.000000000000000000, -0.000000000000000000, -0.000000000000000000 ) ) ;
#70368=VECTOR ( 'NONE', #55236, 1000.000000000000000 ) ;
#70372=DIRECTION ( 'NONE',  ( 0.000000000000000000, 0.000000000000000000, 1.000000000000000000 ) ) ;
#70373=CARTESIAN_POINT ( 'NONE',  ( 0.000000000000000000, -59.75363087400113926, 56.15606465354937882 ) ) ;
#70379=DIRECTION ( 'NONE',  ( -1.000000000000000000, 0.000000000000000000, 0.000000000000000000 ) ) ;
#70397=DIRECTION ( 'NONE',  ( 0.000000000000000000, 0.8090169943749446757, 0.5877852522924769119 ) ) ;
#70403=VERTEX_POINT ( 'NONE', #56846 ) ;
#70420=ORIENTED_EDGE ( 'NONE', *, *, #20392, .T. ) ;
#70421=EDGE_CURVE ( 'NONE', #29098, #5845, #45945, .T. ) ;
#70437=VERTEX_POINT ( 'NONE', #39554 ) ;
#70439=DIRECTION ( 'NONE',  ( 0.000000000000000000, 0.000000000000000000, -1.000000000000000000 ) ) ;
#70443=VECTOR ( 'NONE', #20990, 1000.000000000000000 ) ;
#70444=DIRECTION ( 'NONE',  ( -1.000000000000000000, -0.000000000000000000, -0.000000000000000000 ) ) ;
#70464=DIRECTION ( 'NONE',  ( 1.000000000000000000, -0.000000000000000000, -0.000000000000000000 ) ) ;
#70485=CARTESIAN_POINT ( 'NONE',  ( 10.00000000000000000, 0.000000000000000000, 0.000000000000000000 ) ) ;
#70490=LINE ( 'NONE', #42328, #51830 ) ;
#70516=DIRECTION ( 'NONE',  ( -1.000000000000000000, 0.000000000000000000, -0.000000000000000000 ) ) ;
#70517=FACE_OUTER_BOUND ( 'NONE', #56954, .T. ) ;
#70519=CARTESIAN_POINT ( 'NONE',  ( 10.00000000000000000, 77.32052557432841411, 5.256550761633138613 ) ) ;
#70525=DIRECTION ( 'NONE',  ( 0.000000000000000000, 0.9510565162951523099, 0.3090169943749513926 ) ) ;
#70528=AXIS2_PLACEMENT_3D ( 'NONE', #63257, #68526, #45601 ) ;
#70539=CYLINDRICAL_SURFACE ( 'NONE', #27822, 31.99999999999999289 ) ;
#70555=DIRECTION ( 'NONE',  ( 0.000000000000000000, 0.000000000000000000, -1.000000000000000000 ) ) ;
#70574=DIRECTION ( 'NONE',  ( 0.000000000000000000, 0.2334453638558990629, 0.9723699203976782224 ) ) ;
#70579=DIRECTION ( 'NONE',  ( 1.000000000000000000, 0.000000000000000000, 0.000000000000000000 ) ) ;
#70584=CIRCLE ( 'NONE', #62194, 77.49899999999999523 ) ;
#70595=CARTESIAN_POINT ( 'NONE',  ( 10.00000000000000000, -77.19088730480518734, -6.903761155838607166 ) ) ;
#70598=VERTEX_POINT ( 'NONE', #18100 ) ;
#70612=CARTESIAN_POINT ( 'NONE',  ( 0.000000000000000000, -51.02545421589285723, -55.20638768913812555 ) ) ;
#70617=ADVANCED_FACE ( 'NONE', ( #18819 ), #6456, .T. ) ;
#70618=AXIS2_PLACEMENT_3D ( 'NONE', #20000, #30542, #36931 ) ;
#70629=VERTEX_POINT ( 'NONE', #848 ) ;
#70634=AXIS2_PLACEMENT_3D ( 'NONE', #66000, #49051, #60722 ) ;
#70648=VERTEX_POINT ( 'NONE', #69601 ) ;
#70663=CARTESIAN_POINT ( 'NONE',  ( 0.000000000000000000, 80.55351364060589958, 15.33399622253511829 ) ) ;
#70668=ADVANCED_FACE ( 'NONE', ( #48879 ), #42887, .T. ) ;
#70670=CARTESIAN_POINT ( 'NONE',  ( 0.000000000000000000, 71.27951684758026829, 30.41916302227139113 ) ) ;
#70675=CARTESIAN_POINT ( 'NONE',  ( 10.00000000000000000, 8.840884882376133902, -74.65374052328640175 ) ) ;
#70686=FACE_OUTER_BOUND ( 'NONE', #14011, .T. ) ;
#70690=AXIS2_PLACEMENT_3D ( 'NONE', #25519, #31157, #54108 ) ;
#70692=DIRECTION ( 'NONE',  ( 0.000000000000000000, 0.000000000000000000, 1.000000000000000000 ) ) ;
#70694=CIRCLE ( 'NONE', #16688, 82.00000000000000000 ) ;
#70708=ORIENTED_EDGE ( 'NONE', *, *, #18191, .F. ) ;
#70710=ORIENTED_EDGE ( 'NONE', *, *, #67495, .F. ) ;
#70714=FACE_OUTER_BOUND ( 'NONE', #13707, .T. ) ;
#70715=CYLINDRICAL_SURFACE ( 'NONE', #28452, 31.99999999999999289 ) ;
#70716=AXIS2_PLACEMENT_3D ( 'NONE', #12493, #35431, #24163 ) ;
#70721=CARTESIAN_POINT ( 'NONE',  ( 0.000000000000000000, 0.000000000000000000, 0.000000000000000000 ) ) ;
#70723=CIRCLE ( 'NONE', #69509, 77.49899999999999523 ) ;
#70724=VERTEX_POINT ( 'NONE', #54168 ) ;
#70726=CIRCLE ( 'NONE', #6100, 31.99999999999998934 ) ;
#70747=CARTESIAN_POINT ( 'NONE',  ( 10.00000000000000000, -66.50666863321973210, -39.78640506895676765 ) ) ;
#70751=AXIS2_PLACEMENT_3D ( 'NONE', #19892, #10102, #33026 ) ;
#70758=VERTEX_POINT ( 'NONE', #48513 ) ;
#70770=CARTESIAN_POINT ( 'NONE',  ( 10.00000000000000000, 0.000000000000000000, 77.49899999999999523 ) ) ;
#70780=LINE ( 'NONE', #7639, #59309 ) ;
#70788=CYLINDRICAL_SURFACE ( 'NONE', #6529, 77.49899999999999523 ) ;
#70791=CARTESIAN_POINT ( 'NONE',  ( 10.00000000000000000, 0.000000000000000000, 0.000000000000000000 ) ) ;
#70793=CYLINDRICAL_SURFACE ( 'NONE', #44484, 31.99999999999999289 ) ;
#70796=EDGE_CURVE ( 'NONE', #32443, #38641, #20680, .T. ) ;
#70805=DIRECTION ( 'NONE',  ( -1.000000000000000000, 0.000000000000000000, -0.000000000000000000 ) ) ;
#70812=CIRCLE ( 'NONE', #42, 32.00000000000000000 ) ;
#70817=CARTESIAN_POINT ( 'NONE',  ( 10.00000000000000000, 0.000000000000000000, 0.000000000000000000 ) ) ;
#70825=CARTESIAN_POINT ( 'NONE',  ( 5.000000000000002665, -74.18225833017913828, 34.94270380257611919 ) ) ;
#70844=CARTESIAN_POINT ( 'NONE',  ( 5.000000000000002665, -39.47590169984897557, 71.87247863392401825 ) ) ;
#70845=VERTEX_POINT ( 'NONE', #4150 ) ;
#70848=ORIENTED_EDGE ( 'NONE', *, *, #49233, .F. ) ;
#70849=EDGE_CURVE ( 'NONE', #20435, #28882, #61653, .T. ) ;
#70863=DIRECTION ( 'NONE',  ( 1.000000000000000000, -0.000000000000000000, 0.000000000000000000 ) ) ;
#70875=EDGE_CURVE ( 'NONE', #56348, #68435, #16523, .T. ) ;
#70889=VERTEX_POINT ( 'NONE', #27046 ) ;
#70892=FACE_OUTER_BOUND ( 'NONE', #14909, .T. ) ;
#70896=DIRECTION ( 'NONE',  ( 0.000000000000000000, 0.000000000000000000, 1.000000000000000000 ) ) ;
#70908=VERTEX_POINT ( 'NONE', #27421 ) ;
#70909=CARTESIAN_POINT ( 'NONE',  ( 10.00000000000000000, 0.000000000000000000, 0.000000000000000000 ) ) ;
#70911=CIRCLE ( 'NONE', #38518, 82.00000000000000000 ) ;
#70913=DIRECTION ( 'NONE',  ( -1.000000000000000000, 0.000000000000000000, -0.000000000000000000 ) ) ;
#70915=DIRECTION ( 'NONE',  ( 0.000000000000000000, 0.000000000000000000, 1.000000000000000000 ) ) ;
#70929=ORIENTED_EDGE ( 'NONE', *, *, #72115, .T. ) ;
#70930=CARTESIAN_POINT ( 'NONE',  ( 0.000000000000000000, -76.66974797899844418, 11.30684508768314522 ) ) ;
#70933=ADVANCED_FACE ( 'NONE', ( #38721 ), #10138, .T. ) ;
#70944=CIRCLE ( 'NONE', #25345, 82.00000000000000000 ) ;
#70946=CARTESIAN_POINT ( 'NONE',  ( 10.00000000000000000, 18.89407956138256139, 75.16055320797038064 ) ) ;
#70953=CARTESIAN_POINT ( 'NONE',  ( 10.00000000000000000, -35.91791733033525702, 68.67312586194982771 ) ) ;
#70957=DIRECTION ( 'NONE',  ( 0.000000000000000000, 0.000000000000000000, 1.000000000000000000 ) ) ;
#70969=CIRCLE ( 'NONE', #39760, 31.99999999999998934 ) ;
#70976=DIRECTION ( 'NONE',  ( 1.000000000000000000, 0.000000000000000000, 0.000000000000000000 ) ) ;
#70979=ORIENTED_EDGE ( 'NONE', *, *, #49325, .T. ) ;
#70982=DIRECTION ( 'NONE',  ( -1.000000000000000000, 0.000000000000000000, 0.000000000000000000 ) ) ;
#70990=AXIS2_PLACEMENT_3D ( 'NONE', #69135, #51087, #45469 ) ;
#70994=LINE ( 'NONE', #8219, #41341 ) ;
#71010=EDGE_CURVE ( 'NONE', #34381, #50235, #29274, .T. ) ;
#71016=ORIENTED_EDGE ( 'NONE', *, *, #25114, .F. ) ;
#71021=CARTESIAN_POINT ( 'NONE',  ( 10.00000000000000000, 0.000000000000000000, 0.000000000000000000 ) ) ;
#71024=ORIENTED_EDGE ( 'NONE', *, *, #66406, .T. ) ;
#71026=CARTESIAN_POINT ( 'NONE',  ( 10.00000000000000000, 0.000000000000000000, 0.000000000000000000 ) ) ;
#71027=ORIENTED_EDGE ( 'NONE', *, *, #55184, .T. ) ;
#71030=EDGE_CURVE ( 'NONE', #3728, #68597, #41309, .T. ) ;
#71033=CARTESIAN_POINT ( 'NONE',  ( 10.00000000000000000, 77.16300072079661732, 27.74655509720697921 ) ) ;
#71040=ADVANCED_FACE ( 'NONE', ( #24389 ), #18732, .T. ) ;
#71042=EDGE_CURVE ( 'NONE', #73588, #17434, #47949, .T. ) ;
#71044=CYLINDRICAL_SURFACE ( 'NONE', #21470, 31.99999999999998579 ) ;
#71048=VECTOR ( 'NONE', #58656, 1000.000000000000000 ) ;
#71053=DIRECTION ( 'NONE',  ( 0.000000000000000000, -0.6494480483301739993, -0.7604059656000392575 ) ) ;
#71061=DIRECTION ( 'NONE',  ( -1.000000000000000000, -0.000000000000000000, 0.000000000000000000 ) ) ;
#71062=CARTESIAN_POINT ( 'NONE',  ( 0.000000000000000000, 22.90783923731741112, -78.73519480814930205 ) ) ;
#71066=ORIENTED_EDGE ( 'NONE', *, *, #73213, .T. ) ;
#71067=CARTESIAN_POINT ( 'NONE',  ( 0.000000000000000000, 0.000000000000000000, 0.000000000000000000 ) ) ;
#71074=EDGE_LOOP ( 'NONE', ( #57367, #62281, #64532, #14613 ) ) ;
#71075=DIRECTION ( 'NONE',  ( -1.000000000000000000, -0.000000000000000000, -0.000000000000000000 ) ) ;
#71086=EDGE_LOOP ( 'NONE', ( #29740, #38086, #27875, #49845 ) ) ;
#71087=DIRECTION ( 'NONE',  ( -1.000000000000000000, 0.000000000000000000, 0.000000000000000000 ) ) ;
#71089=VERTEX_POINT ( 'NONE', #8582 ) ;
#71090=DIRECTION ( 'NONE',  ( 0.000000000000000000, 0.000000000000000000, -1.000000000000000000 ) ) ;
#71092=ADVANCED_FACE ( 'NONE', ( #2613 ), #2969, .T. ) ;
#71098=ORIENTED_EDGE ( 'NONE', *, *, #56100, .F. ) ;
#71131=EDGE_CURVE ( 'NONE', #21230, #69181, #37115, .T. ) ;
#71134=CARTESIAN_POINT ( 'NONE',  ( 10.00000000000000000, 0.000000000000000000, 0.000000000000000000 ) ) ;
#71141=DIRECTION ( 'NONE',  ( 1.000000000000000000, -0.000000000000000000, -0.000000000000000000 ) ) ;
#71144=CARTESIAN_POINT ( 'NONE',  ( 0.000000000000000000, -14.67089635893764665, 73.72996012237435082 ) ) ;
#71155=FACE_OUTER_BOUND ( 'NONE', #46264, .T. ) ;
#71159=DIRECTION ( 'NONE',  ( 0.000000000000000000, 0.000000000000000000, 1.000000000000000000 ) ) ;
#71170=EDGE_CURVE ( 'NONE', #58503, #49949, #58738, .T. ) ;
#71179=EDGE_LOOP ( 'NONE', ( #44308, #42356, #40149, #44863 ) ) ;
#71183=ORIENTED_EDGE ( 'NONE', *, *, #59032, .T. ) ;
#71187=LINE ( 'NONE', #70825, #70301 ) ;
#71191=DIRECTION ( 'NONE',  ( 1.000000000000000000, -0.000000000000000000, 0.000000000000000000 ) ) ;
#71202=CYLINDRICAL_SURFACE ( 'NONE', #35489, 31.99999999999999289 ) ;
#71222=VERTEX_POINT ( 'NONE', #42421 ) ;
#71224=CIRCLE ( 'NONE', #35226, 77.49899999999998101 ) ;
#71225=CIRCLE ( 'NONE', #54440, 82.00000000000000000 ) ;
#71232=DIRECTION ( 'NONE',  ( 0.000000000000000000, 0.000000000000000000, 1.000000000000000000 ) ) ;
#71248=AXIS2_PLACEMENT_3D ( 'NONE', #31669, #47859, #18545 ) ;
#71250=ADVANCED_FACE ( 'NONE', ( #48789 ), #19108, .F. ) ;
#71252=CIRCLE ( 'NONE', #38872, 77.49899999999999523 ) ;
#71254=ORIENTED_EDGE ( 'NONE', *, *, #27324, .T. ) ;
#71258=DIRECTION ( 'NONE',  ( 0.000000000000000000, -0.2334453638559127742, 0.9723699203976748917 ) ) ;
#71260=CIRCLE ( 'NONE', #7640, 31.99999999999999289 ) ;
#71268=ORIENTED_EDGE ( 'NONE', *, *, #62822, .T. ) ;
#71276=DIRECTION ( 'NONE',  ( -1.000000000000000000, 0.000000000000000000, -0.000000000000000000 ) ) ;
#71285=VERTEX_POINT ( 'NONE', #39375 ) ;
#71287=EDGE_CURVE ( 'NONE', #2959, #14681, #45603, .T. ) ;
#71289=DIRECTION ( 'NONE',  ( -1.000000000000000000, 0.000000000000000000, 0.000000000000000000 ) ) ;
#71294=VERTEX_POINT ( 'NONE', #72812 ) ;
#71295=FACE_OUTER_BOUND ( 'NONE', #26959, .T. ) ;
#71305=VERTEX_POINT ( 'NONE', #72454 ) ;
#71316=LINE ( 'NONE', #9287, #66141 ) ;
#71320=CIRCLE ( 'NONE', #38926, 82.00000000000000000 ) ;
#71327=AXIS2_PLACEMENT_3D ( 'NONE', #8486, #54350, #25767 ) ;
#71336=EDGE_CURVE ( 'NONE', #20435, #71438, #29951, .T. ) ;
#71342=ORIENTED_EDGE ( 'NONE', *, *, #41662, .T. ) ;
#71343=DIRECTION ( 'NONE',  ( 1.000000000000000000, 0.000000000000000000, -0.000000000000000000 ) ) ;
#71347=ADVANCED_FACE ( 'NONE', ( #27331 ), #73945, .T. ) ;
#71348=DIRECTION ( 'NONE',  ( -1.000000000000000000, -0.000000000000000000, 0.000000000000000000 ) ) ;
#71349=VERTEX_POINT ( 'NONE', #50268 ) ;
#71353=ORIENTED_EDGE ( 'NONE', *, *, #72872, .F. ) ;
#71357=CARTESIAN_POINT ( 'NONE',  ( 10.00000000000000000, 0.000000000000000000, 0.000000000000000000 ) ) ;
#71358=VECTOR ( 'NONE', #4092, 1000.000000000000000 ) ;
#71359=DIRECTION ( 'NONE',  ( 0.000000000000000000, 0.000000000000000000, 1.000000000000000000 ) ) ;
#71373=CIRCLE ( 'NONE', #19755, 31.99999999999999289 ) ;
#71377=CARTESIAN_POINT ( 'NONE',  ( 10.00000000000000000, 30.41916302227113178, 71.27951684758036777 ) ) ;
#71381=CIRCLE ( 'NONE', #34207, 82.00000000000000000 ) ;
#71385=ORIENTED_EDGE ( 'NONE', *, *, #7456, .T. ) ;
#71389=ORIENTED_EDGE ( 'NONE', *, *, #43736, .T. ) ;
#71390=EDGE_CURVE ( 'NONE', #42798, #32631, #1691, .T. ) ;
#71401=CARTESIAN_POINT ( 'NONE',  ( 0.000000000000000000, -68.67312586194971402, -35.91791733033549860 ) ) ;
#71404=CYLINDRICAL_SURFACE ( 'NONE', #56564, 77.49899999999999523 ) ;
#71410=CARTESIAN_POINT ( 'NONE',  ( 0.000000000000000000, -73.72996012237449293, 14.67089635893687571 ) ) ;
#71424=DIRECTION ( 'NONE',  ( 0.000000000000000000, 0.000000000000000000, -1.000000000000000000 ) ) ;
#71427=DIRECTION ( 'NONE',  ( 0.000000000000000000, 0.000000000000000000, 1.000000000000000000 ) ) ;
#71429=ADVANCED_FACE ( 'NONE', ( #7657 ), #13292, .T. ) ;
#71438=VERTEX_POINT ( 'NONE', #8025 ) ;
#71442=VERTEX_POINT ( 'NONE', #34463 ) ;
#71468=CIRCLE ( 'NONE', #55882, 77.49900000000002365 ) ;
#71475=EDGE_LOOP ( 'NONE', ( #15137, #58849, #67490, #65760 ) ) ;
#71482=VERTEX_POINT ( 'NONE', #28827 ) ;
#71487=DIRECTION ( 'NONE',  ( -1.000000000000000000, -0.000000000000000000, 0.000000000000000000 ) ) ;
#71488=DIRECTION ( 'NONE',  ( 0.000000000000000000, 0.000000000000000000, 1.000000000000000000 ) ) ;
#71496=FACE_OUTER_BOUND ( 'NONE', #12196, .T. ) ;
#71504=CIRCLE ( 'NONE', #31900, 82.00000000000000000 ) ;
#71508=VECTOR ( 'NONE', #55413, 1000.000000000000000 ) ;
#71511=CARTESIAN_POINT ( 'NONE',  ( 10.00000000000000000, 41.19522573413731692, 65.64334221924924861 ) ) ;
#71514=CARTESIAN_POINT ( 'NONE',  ( 0.000000000000000000, 0.000000000000000000, 0.000000000000000000 ) ) ;
#71524=CARTESIAN_POINT ( 'NONE',  ( 10.00000000000000000, 0.000000000000000000, 0.000000000000000000 ) ) ;
#71536=CARTESIAN_POINT ( 'NONE',  ( 0.000000000000000000, 0.000000000000000000, 0.000000000000000000 ) ) ;
#71538=ORIENTED_EDGE ( 'NONE', *, *, #63346, .T. ) ;
#71550=ORIENTED_EDGE ( 'NONE', *, *, #6083, .T. ) ;
#71559=ORIENTED_EDGE ( 'NONE', *, *, #4124, .F. ) ;
#71563=EDGE_CURVE ( 'NONE', #73763, #69008, #9576, .T. ) ;
#71568=CARTESIAN_POINT ( 'NONE',  ( 5.000000000000000000, -67.80270845531855173, -46.11716303203261447 ) ) ;
#71571=CARTESIAN_POINT ( 'NONE',  ( 0.000000000000000000, 17.28742895386084655, 75.54627589209950145 ) ) ;
#71580=CARTESIAN_POINT ( 'NONE',  ( 0.000000000000000000, 81.90746397400393164, -3.894527615416986333 ) ) ;
#71590=DIRECTION ( 'NONE',  ( 0.000000000000000000, 0.7604059656000276002, 0.6494480483301877660 ) ) ;
#71610=FACE_OUTER_BOUND ( 'NONE', #5206, .T. ) ;
#71620=CYLINDRICAL_SURFACE ( 'NONE', #42528, 82.00000000000000000 ) ;
#71624=DIRECTION ( 'NONE',  ( -1.000000000000000000, 0.000000000000000000, -0.000000000000000000 ) ) ;
#71629=AXIS2_PLACEMENT_3D ( 'NONE', #51796, #52523, #51416 ) ;
#71630=ORIENTED_EDGE ( 'NONE', *, *, #616, .T. ) ;
#71631=DIRECTION ( 'NONE',  ( -1.000000000000000000, 0.000000000000000000, -0.000000000000000000 ) ) ;
#71634=DIRECTION ( 'NONE',  ( -1.000000000000000000, -0.000000000000000000, 0.000000000000000000 ) ) ;
#71637=DIRECTION ( 'NONE',  ( 0.000000000000000000, 0.000000000000000000, 1.000000000000000000 ) ) ;
#71652=CIRCLE ( 'NONE', #11604, 31.99999999999999289 ) ;
#71660=AXIS2_PLACEMENT_3D ( 'NONE', #4890, #43615, #15015 ) ;
#71668=DIRECTION ( 'NONE',  ( -1.000000000000000000, -0.000000000000000000, -0.000000000000000000 ) ) ;
#71670=ORIENTED_EDGE ( 'NONE', *, *, #36505, .F. ) ;
#71673=EDGE_LOOP ( 'NONE', ( #65563, #62810, #67232, #31658 ) ) ;
#71681=EDGE_LOOP ( 'NONE', ( #60942, #31121, #20516, #29845 ) ) ;
#71689=CARTESIAN_POINT ( 'NONE',  ( 0.000000000000000000, -26.01480285779885904, 70.53064760720306481 ) ) ;
#71693=CARTESIAN_POINT ( 'NONE',  ( 0.000000000000000000, 0.000000000000000000, 0.000000000000000000 ) ) ;
#71694=FACE_OUTER_BOUND ( 'NONE', #9934, .T. ) ;
#71697=AXIS2_PLACEMENT_3D ( 'NONE', #39112, #21423, #61672 ) ;
#71700=EDGE_CURVE ( 'NONE', #32622, #70629, #49223, .T. ) ;
#71709=DIRECTION ( 'NONE',  ( 0.000000000000000000, 0.000000000000000000, 1.000000000000000000 ) ) ;
#71710=ADVANCED_FACE ( 'NONE', ( #18795 ), #2300, .T. ) ;
#71713=AXIS2_PLACEMENT_3D ( 'NONE', #38554, #34292, #45966 ) ;
#71719=CARTESIAN_POINT ( 'NONE',  ( 10.00000000000000000, 51.03279382321166224, -55.19960302592011914 ) ) ;
#71725=DIRECTION ( 'NONE',  ( 0.000000000000000000, -0.3090169943749349613, -0.9510565162951576390 ) ) ;
#71726=ORIENTED_EDGE ( 'NONE', *, *, #29628, .T. ) ;
#71738=VERTEX_POINT ( 'NONE', #41735 ) ;
#71750=CIRCLE ( 'NONE', #24922, 31.99999999999999289 ) ;
#71752=CIRCLE ( 'NONE', #12940, 31.99999999999998934 ) ;
#71766=DIRECTION ( 'NONE',  ( 0.000000000000000000, 0.000000000000000000, 1.000000000000000000 ) ) ;
#71768=EDGE_CURVE ( 'NONE', #57845, #26721, #52841, .T. ) ;
#71774=CARTESIAN_POINT ( 'NONE',  ( 0.000000000000000000, 46.11716303203284184, -67.80270845531839541 ) ) ;
#71775=ADVANCED_FACE ( 'NONE', ( #24819 ), #64678, .T. ) ;
#71782=CIRCLE ( 'NONE', #27344, 31.99999999999999289 ) ;
#71792=ADVANCED_FACE ( 'NONE', ( #1565 ), #19904, .T. ) ;
#71793=ORIENTED_EDGE ( 'NONE', *, *, #16841, .T. ) ;
#71794=CARTESIAN_POINT ( 'NONE',  ( -10.00000000000000000, 0.000000000000000000, 0.000000000000000000 ) ) ;
#71797=CARTESIAN_POINT ( 'NONE',  ( 10.00000000000000000, -77.32052557432845674, 5.256550761632577284 ) ) ;
#71804=ORIENTED_EDGE ( 'NONE', *, *, #71899, .T. ) ;
#71806=EDGE_CURVE ( 'NONE', #3546, #67626, #65061, .T. ) ;
#71817=ORIENTED_EDGE ( 'NONE', *, *, #34062, .T. ) ;
#71819=CIRCLE ( 'NONE', #46622, 31.99999999999998579 ) ;
#71825=DIRECTION ( 'NONE',  ( -1.000000000000000000, -0.000000000000000000, 0.000000000000000000 ) ) ;
#71837=CARTESIAN_POINT ( 'NONE',  ( 10.00000000000000000, 41.76106447765489094, 62.50884508063442269 ) ) ;
#71840=VERTEX_POINT ( 'NONE', #64314 ) ;
#71846=VERTEX_POINT ( 'NONE', #35717 ) ;
#71860=DIRECTION ( 'NONE',  ( 1.000000000000000000, 0.000000000000000000, 0.000000000000000000 ) ) ;
#71862=VERTEX_POINT ( 'NONE', #25528 ) ;
#71874=CYLINDRICAL_SURFACE ( 'NONE', #67201, 77.49899999999999523 ) ;
#71880=DIRECTION ( 'NONE',  ( 0.000000000000000000, -0.8526401643540971742, 0.5224985647159409163 ) ) ;
#71882=LINE ( 'NONE', #25665, #30130 ) ;
#71887=EDGE_CURVE ( 'NONE', #57102, #32622, #49936, .T. ) ;
#71893=DIRECTION ( 'NONE',  ( 0.000000000000000000, 0.000000000000000000, 1.000000000000000000 ) ) ;
#71899=EDGE_CURVE ( 'NONE', #73400, #60921, #26261, .T. ) ;
#71900=DIRECTION ( 'NONE',  ( 0.000000000000000000, 0.000000000000000000, 1.000000000000000000 ) ) ;
#71903=FACE_OUTER_BOUND ( 'NONE', #61932, .T. ) ;
#71905=ORIENTED_EDGE ( 'NONE', *, *, #66241, .T. ) ;
#71906=FACE_OUTER_BOUND ( 'NONE', #17955, .T. ) ;
#71909=CIRCLE ( 'NONE', #67092, 31.99999999999998579 ) ;
#71913=ORIENTED_EDGE ( 'NONE', *, *, #4032, .T. ) ;
#71920=ORIENTED_EDGE ( 'NONE', *, *, #38527, .T. ) ;
#71925=ORIENTED_EDGE ( 'NONE', *, *, #22571, .F. ) ;
#71927=ORIENTED_EDGE ( 'NONE', *, *, #19114, .F. ) ;
#71940=CIRCLE ( 'NONE', #47910, 82.00000000000000000 ) ;
#71941=DIRECTION ( 'NONE',  ( 0.000000000000000000, 1.000000000000000000, 3.491481338843133355E-15 ) ) ;
#71942=CIRCLE ( 'NONE', #34713, 77.49899999999999523 ) ;
#71944=DIRECTION ( 'NONE',  ( 0.000000000000000000, 0.000000000000000000, 1.000000000000000000 ) ) ;
#71952=DIRECTION ( 'NONE',  ( 0.000000000000000000, 0.000000000000000000, 1.000000000000000000 ) ) ;
#71958=ADVANCED_FACE ( 'NONE', ( #37196 ), #54117, .T. ) ;
#71960=EDGE_CURVE ( 'NONE', #59828, #503, #1248, .T. ) ;
#71961=CARTESIAN_POINT ( 'NONE',  ( 10.00000000000000000, -74.65491531819111515, -8.830959090343204920 ) ) ;
#71964=FACE_OUTER_BOUND ( 'NONE', #53908, .T. ) ;
#71965=DIRECTION ( 'NONE',  ( -1.000000000000000000, -0.000000000000000000, -0.000000000000000000 ) ) ;
#71971=AXIS2_PLACEMENT_3D ( 'NONE', #38770, #72956, #9821 ) ;
#71973=LINE ( 'NONE', #72699, #22264 ) ;
#71975=CYLINDRICAL_SURFACE ( 'NONE', #934, 82.00000000000000000 ) ;
#71977=CARTESIAN_POINT ( 'NONE',  ( 10.00000000000000000, 49.70050353004889132, 59.46389618801982380 ) ) ;
#71979=DIRECTION ( 'NONE',  ( 1.000000000000000000, -0.000000000000000000, -0.000000000000000000 ) ) ;
#71982=DIRECTION ( 'NONE',  ( 0.000000000000000000, 0.000000000000000000, 1.000000000000000000 ) ) ;
#71995=EDGE_CURVE ( 'NONE', #72558, #23616, #42052, .T. ) ;
#71997=CIRCLE ( 'NONE', #1221, 82.00000000000000000 ) ;
#71998=CIRCLE ( 'NONE', #45631, 77.49899999999999523 ) ;
#72001=DIRECTION ( 'NONE',  ( -1.000000000000000000, 0.000000000000000000, 0.000000000000000000 ) ) ;
#72004=VERTEX_POINT ( 'NONE', #72852 ) ;
#72018=ORIENTED_EDGE ( 'NONE', *, *, #37251, .F. ) ;
#72027=EDGE_CURVE ( 'NONE', #36877, #10469, #59755, .T. ) ;
#72044=ORIENTED_EDGE ( 'NONE', *, *, #65536, .F. ) ;
#72055=DIRECTION ( 'NONE',  ( -1.000000000000000000, -0.000000000000000000, 0.000000000000000000 ) ) ;
#72060=ADVANCED_FACE ( 'NONE', ( #22122 ), #61984, .T. ) ;
#72063=DIRECTION ( 'NONE',  ( -1.000000000000000000, 0.000000000000000000, 0.000000000000000000 ) ) ;
#72088=DIRECTION ( 'NONE',  ( 0.000000000000000000, 0.000000000000000000, 1.000000000000000000 ) ) ;
#72089=VECTOR ( 'NONE', #54594, 1000.000000000000000 ) ;
#72098=CARTESIAN_POINT ( 'NONE',  ( 0.000000000000000000, 62.20884554314086046, -46.21855187248561236 ) ) ;
#72106=ORIENTED_EDGE ( 'NONE', *, *, #16385, .T. ) ;
#72115=EDGE_CURVE ( 'NONE', #45142, #42699, #4859, .T. ) ;
#72116=VERTEX_POINT ( 'NONE', #10464 ) ;
#72117=CARTESIAN_POINT ( 'NONE',  ( 0.000000000000000000, -56.15606465355001120, 59.75363087400055662 ) ) ;
#72118=DIRECTION ( 'NONE',  ( 0.000000000000000000, 0.000000000000000000, 1.000000000000000000 ) ) ;
#72120=LINE ( 'NONE', #67980, #70443 ) ;
#72127=VECTOR ( 'NONE', #37009, 1000.000000000000000 ) ;
#72128=DIRECTION ( 'NONE',  ( 0.000000000000000000, -0.8090169943749532244, 0.5877852522924652545 ) ) ;
#72130=CARTESIAN_POINT ( 'NONE',  ( 0.000000000000000000, 34.44570377933598593, 69.42325613327452061 ) ) ;
#72133=ORIENTED_EDGE ( 'NONE', *, *, #59610, .T. ) ;
#72135=DIRECTION ( 'NONE',  ( -1.000000000000000000, -0.000000000000000000, -0.000000000000000000 ) ) ;
#72136=VERTEX_POINT ( 'NONE', #11569 ) ;
#72158=EDGE_CURVE ( 'NONE', #33464, #36312, #70726, .T. ) ;
#72159=DIRECTION ( 'NONE',  ( -1.000000000000000000, -0.000000000000000000, 0.000000000000000000 ) ) ;
#72162=EDGE_CURVE ( 'NONE', #64812, #43566, #67243, .T. ) ;
#72165=CARTESIAN_POINT ( 'NONE',  ( 5.000000000000000000, 51.29473840253317718, -63.97538442413369353 ) ) ;
#72166=DIRECTION ( 'NONE',  ( 0.000000000000000000, 0.7071067811865487940, -0.7071067811865462405 ) ) ;
#72167=DIRECTION ( 'NONE',  ( 1.000000000000000000, -0.000000000000000000, 0.000000000000000000 ) ) ;
#72181=VECTOR ( 'NONE', #54390, 1000.000000000000000 ) ;
#72182=LINE ( 'NONE', #44002, #5546 ) ;
#72198=CARTESIAN_POINT ( 'NONE',  ( 0.000000000000000000, -35.91791733033525702, 68.67312586194982771 ) ) ;
#72201=CARTESIAN_POINT ( 'NONE',  ( 0.000000000000000000, -8.966570791701281351, 81.50828551894224461 ) ) ;
#72202=CARTESIAN_POINT ( 'NONE',  ( 0.000000000000000000, 0.000000000000000000, 0.000000000000000000 ) ) ;
#72204=CARTESIAN_POINT ( 'NONE',  ( 0.000000000000000000, 78.73519480814985627, -22.90783923731548910 ) ) ;
#72205=EDGE_LOOP ( 'NONE', ( #58631, #28201, #34508, #18476 ) ) ;
#72208=ORIENTED_EDGE ( 'NONE', *, *, #49829, .F. ) ;
#72229=CYLINDRICAL_SURFACE ( 'NONE', #68022, 32.00000000000000000 ) ;
#72239=CIRCLE ( 'NONE', #66255, 31.99999999999998934 ) ;
#72241=CARTESIAN_POINT ( 'NONE',  ( 0.000000000000000000, -18.89407956138310496, 75.16055320797023853 ) ) ;
#72244=AXIS2_PLACEMENT_3D ( 'NONE', #30988, #53944, #2482 ) ;
#72251=DIRECTION ( 'NONE',  ( 0.000000000000000000, -0.9510565162951565288, 0.3090169943749384029 ) ) ;
#72254=DIRECTION ( 'NONE',  ( -1.000000000000000000, 0.000000000000000000, 0.000000000000000000 ) ) ;
#72256=CARTESIAN_POINT ( 'NONE',  ( 5.000000000000000000, -77.16300072079681627, 27.74655509720641078 ) ) ;
#72257=CARTESIAN_POINT ( 'NONE',  ( 10.00000000000000000, -31.46837873494930093, -68.27212725128309501 ) ) ;
#72262=CARTESIAN_POINT ( 'NONE',  ( 10.00000000000000000, 75.54627589209970040, -17.28742895386005785 ) ) ;
#72265=CARTESIAN_POINT ( 'NONE',  ( 10.00000000000000000, -39.78640506895559525, -66.50666863322042843 ) ) ;
#72272=CARTESIAN_POINT ( 'NONE',  ( 0.000000000000000000, 6.903761155837774943, 77.19088730480525840 ) ) ;
#72273=ORIENTED_EDGE ( 'NONE', *, *, #35256, .T. ) ;
#72287=EDGE_CURVE ( 'NONE', #61965, #71862, #52166, .T. ) ;
#72299=EDGE_CURVE ( 'NONE', #11546, #23616, #1821, .T. ) ;
#72302=FACE_OUTER_BOUND ( 'NONE', #43842, .T. ) ;
#72305=ORIENTED_EDGE ( 'NONE', *, *, #25902, .T. ) ;
#72325=DIRECTION ( 'NONE',  ( 0.000000000000000000, 0.000000000000000000, 1.000000000000000000 ) ) ;
#72327=DIRECTION ( 'NONE',  ( 0.000000000000000000, 0.000000000000000000, 1.000000000000000000 ) ) ;
#72332=ADVANCED_FACE ( 'NONE', ( #13425 ), #29227, .F. ) ;
#72338=CARTESIAN_POINT ( 'NONE',  ( 10.00000000000000000, 0.000000000000000000, 0.000000000000000000 ) ) ;
#72352=CARTESIAN_POINT ( 'NONE',  ( 0.000000000000000000, 76.41127070299290835, -12.93880638057231991 ) ) ;
#72366=VECTOR ( 'NONE', #54144, 1000.000000000000000 ) ;
#72367=AXIS2_PLACEMENT_3D ( 'NONE', #10956, #33881, #74097 ) ;
#72369=VERTEX_POINT ( 'NONE', #13784 ) ;
#72372=CARTESIAN_POINT ( 'NONE',  ( 10.00000000000000000, 46.54456581323805153, 59.03342792756280488 ) ) ;
#72382=EDGE_CURVE ( 'NONE', #10842, #9979, #39693, .T. ) ;
#72393=DIRECTION ( 'NONE',  ( -1.000000000000000000, 0.000000000000000000, -0.000000000000000000 ) ) ;
#72395=PLANE ( 'NONE',  #20378 ) ;
#72396=EDGE_CURVE ( 'NONE', #15358, #6553, #47941, .T. ) ;
#72400=ORIENTED_EDGE ( 'NONE', *, *, #66382, .F. ) ;
#72407=CIRCLE ( 'NONE', #20946, 31.99999999999999645 ) ;
#72409=DIRECTION ( 'NONE',  ( 0.000000000000000000, 0.000000000000000000, 1.000000000000000000 ) ) ;
#72412=CARTESIAN_POINT ( 'NONE',  ( 10.00000000000000000, 0.000000000000000000, 0.000000000000000000 ) ) ;
#72415=AXIS2_PLACEMENT_3D ( 'NONE', #24368, #40930, #70207 ) ;
#72416=ADVANCED_FACE ( 'NONE', ( #14158 ), #59669, .T. ) ;
#72429=DIRECTION ( 'NONE',  ( 0.000000000000000000, 0.000000000000000000, 1.000000000000000000 ) ) ;
#72433=DIRECTION ( 'NONE',  ( -1.000000000000000000, 0.000000000000000000, 0.000000000000000000 ) ) ;
#72435=CARTESIAN_POINT ( 'NONE',  ( 0.000000000000000000, -69.42325613327415113, -34.44570377933673200 ) ) ;
#72437=DIRECTION ( 'NONE',  ( 1.000000000000000000, 0.000000000000000000, 0.000000000000000000 ) ) ;
#72447=AXIS2_PLACEMENT_3D ( 'NONE', #9972, #38927, #9611 ) ;
#72448=DIRECTION ( 'NONE',  ( -1.000000000000000000, 0.000000000000000000, 0.000000000000000000 ) ) ;
#72454=CARTESIAN_POINT ( 'NONE',  ( 10.00000000000000000, -41.19522573413687638, -65.64334221924953283 ) ) ;
#72457=AXIS2_PLACEMENT_3D ( 'NONE', #23541, #35190, #36292 ) ;
#72462=EDGE_CURVE ( 'NONE', #24570, #278, #37852, .T. ) ;
#72489=CYLINDRICAL_SURFACE ( 'NONE', #16370, 12.50000000000000000 ) ;
#72495=VERTEX_POINT ( 'NONE', #49117 ) ;
#72508=EDGE_LOOP ( 'NONE', ( #864, #33364, #40243, #59686 ) ) ;
#72511=DIRECTION ( 'NONE',  ( -1.000000000000000000, 0.000000000000000000, 0.000000000000000000 ) ) ;
#72512=DIRECTION ( 'NONE',  ( -1.000000000000000000, -0.000000000000000000, -0.000000000000000000 ) ) ;
#72538=EDGE_CURVE ( 'NONE', #36312, #57978, #67903, .T. ) ;
#72541=ORIENTED_EDGE ( 'NONE', *, *, #8139, .T. ) ;
#72553=DIRECTION ( 'NONE',  ( -1.000000000000000000, 0.000000000000000000, -0.000000000000000000 ) ) ;
#72558=VERTEX_POINT ( 'NONE', #4770 ) ;
#72559=CARTESIAN_POINT ( 'NONE',  ( 0.000000000000000000, 70.52718814184294160, -26.02418014898236720 ) ) ;
#72561=ORIENTED_EDGE ( 'NONE', *, *, #58749, .T. ) ;
#72562=FACE_OUTER_BOUND ( 'NONE', #22242, .T. ) ;
#72563=DIRECTION ( 'NONE',  ( -1.000000000000000000, 0.000000000000000000, -0.000000000000000000 ) ) ;
#72590=CARTESIAN_POINT ( 'NONE',  ( 10.00000000000000000, 73.44644590900061587, 24.73286445877730699 ) ) ;
#72604=CIRCLE ( 'NONE', #19809, 82.00000000000000000 ) ;
#72611=CARTESIAN_POINT ( 'NONE',  ( 0.000000000000000000, -44.88180994100329713, -63.18004540533077318 ) ) ;
#72612=DIRECTION ( 'NONE',  ( -1.000000000000000000, 0.000000000000000000, 0.000000000000000000 ) ) ;
#72613=DIRECTION ( 'NONE',  ( 0.000000000000000000, 0.9510565162951546414, -0.3090169943749446202 ) ) ;
#72632=LINE ( 'NONE', #31686, #42707 ) ;
#72634=CIRCLE ( 'NONE', #10236, 77.49899999999999523 ) ;
#72648=ORIENTED_EDGE ( 'NONE', *, *, #10467, .T. ) ;
#72650=ORIENTED_EDGE ( 'NONE', *, *, #57597, .T. ) ;
#72653=CARTESIAN_POINT ( 'NONE',  ( 10.00000000000000000, 0.000000000000000000, 0.000000000000000000 ) ) ;
#72663=CARTESIAN_POINT ( 'NONE',  ( 10.00000000000000000, 36.73666225445988687, -65.58780272294035285 ) ) ;
#72665=DIRECTION ( 'NONE',  ( -1.000000000000000000, 0.000000000000000000, -0.000000000000000000 ) ) ;
#72680=AXIS2_PLACEMENT_3D ( 'NONE', #43034, #14447, #54313 ) ;
#72689=DIRECTION ( 'NONE',  ( 0.000000000000000000, 0.000000000000000000, 1.000000000000000000 ) ) ;
#72691=LINE ( 'NONE', #15575, #62797 ) ;
#72699=CARTESIAN_POINT ( 'NONE',  ( 10.00000000000000000, 66.50666863322055633, -39.78640506895536078 ) ) ;
#72700=EDGE_CURVE ( 'NONE', #37771, #60557, #70008, .T. ) ;
#72701=CARTESIAN_POINT ( 'NONE',  ( -10.00000000000000000, 0.000000000000000000, 0.000000000000000000 ) ) ;
#72711=DIRECTION ( 'NONE',  ( -1.000000000000000000, 0.000000000000000000, 0.000000000000000000 ) ) ;
#72713=EDGE_CURVE ( 'NONE', #38392, #45539, #13159, .T. ) ;
#72728=EDGE_CURVE ( 'NONE', #38655, #54641, #27534, .T. ) ;
#72729=EDGE_CURVE ( 'NONE', #503, #23895, #56383, .T. ) ;
#72748=VERTEX_POINT ( 'NONE', #70747 ) ;
#72753=DIRECTION ( 'NONE',  ( 0.000000000000000000, 0.000000000000000000, -1.000000000000000000 ) ) ;
#72757=ORIENTED_EDGE ( 'NONE', *, *, #18987, .F. ) ;
#72765=CARTESIAN_POINT ( 'NONE',  ( 10.00000000000000000, 16.65972982745046238, -80.28980883073739960 ) ) ;
#72773=AXIS2_PLACEMENT_3D ( 'NONE', #29399, #34686, #23416 ) ;
#72777=CARTESIAN_POINT ( 'NONE',  ( -10.00000000000000000, 0.000000000000000000, 0.000000000000000000 ) ) ;
#72782=ORIENTED_EDGE ( 'NONE', *, *, #13660, .T. ) ;
#72784=ORIENTED_EDGE ( 'NONE', *, *, #23352, .F. ) ;
#72785=EDGE_CURVE ( 'NONE', #5647, #12010, #35793, .T. ) ;
#72788=ADVANCED_FACE ( 'NONE', ( #7248 ), #58369, .T. ) ;
#72789=CARTESIAN_POINT ( 'NONE',  ( 10.00000000000000000, 41.76937507738788469, 62.50329211542452157 ) ) ;
#72791=CARTESIAN_POINT ( 'NONE',  ( 5.000000000000002665, -16.65972982744877484, -80.28980883073775487 ) ) ;
#72795=EDGE_CURVE ( 'NONE', #65945, #5973, #43181, .T. ) ;
#72796=CARTESIAN_POINT ( 'NONE',  ( 0.000000000000000000, -51.29473840253270112, 63.97538442413407012 ) ) ;
#72806=EDGE_CURVE ( 'NONE', #11119, #9632, #36175, .T. ) ;
#72810=CARTESIAN_POINT ( 'NONE',  ( 10.00000000000000000, -36.73666225445940370, 65.58780272294062286 ) ) ;
#72811=CIRCLE ( 'NONE', #5625, 31.99999999999999289 ) ;
#72812=CARTESIAN_POINT ( 'NONE',  ( 0.000000000000000000, -73.95703589263958122, -23.16143007188506431 ) ) ;
#72813=VECTOR ( 'NONE', #34295, 1000.000000000000000 ) ;
#72815=EDGE_CURVE ( 'NONE', #4680, #9035, #30524, .T. ) ;
#72822=CYLINDRICAL_SURFACE ( 'NONE', #14030, 31.99999999999999289 ) ;
#72824=LINE ( 'NONE', #26605, #73757 ) ;
#72830=DIRECTION ( 'NONE',  ( -1.000000000000000000, 0.000000000000000000, 0.000000000000000000 ) ) ;
#72831=ORIENTED_EDGE ( 'NONE', *, *, #6036, .F. ) ;
#72838=LINE ( 'NONE', #67226, #34145 ) ;
#72841=CIRCLE ( 'NONE', #41739, 77.49900000000000944 ) ;
#72844=EDGE_LOOP ( 'NONE', ( #37189, #65000, #30618, #67865 ) ) ;
#72850=VERTEX_POINT ( 'NONE', #60958 ) ;
#72852=CARTESIAN_POINT ( 'NONE',  ( 0.000000000000000000, 54.21277698773752718, -55.38113227695725271 ) ) ;
#72853=ORIENTED_EDGE ( 'NONE', *, *, #73939, .T. ) ;
#72859=EDGE_LOOP ( 'NONE', ( #54912, #18643, #10047, #62640 ) ) ;
#72865=DIRECTION ( 'NONE',  ( -1.000000000000000000, -0.000000000000000000, 0.000000000000000000 ) ) ;
#72872=EDGE_CURVE ( 'NONE', #52624, #48290, #10755, .T. ) ;
#72874=VECTOR ( 'NONE', #62468, 1000.000000000000000 ) ;
#72882=CARTESIAN_POINT ( 'NONE',  ( 10.00000000000000000, 65.59268652807210742, 36.72794159290264560 ) ) ;
#72887=EDGE_CURVE ( 'NONE', #24570, #72748, #62404, .T. ) ;
#72893=EDGE_CURVE ( 'NONE', #11217, #52914, #29945, .T. ) ;
#72901=EDGE_CURVE ( 'NONE', #29598, #63684, #3588, .T. ) ;
#72912=CIRCLE ( 'NONE', #8108, 31.99999999999999289 ) ;
#72923=AXIS2_PLACEMENT_3D ( 'NONE', #74112, #34261, #57208 ) ;
#72934=ORIENTED_EDGE ( 'NONE', *, *, #54598, .F. ) ;
#72952=EDGE_CURVE ( 'NONE', #73705, #39929, #15582, .T. ) ;
#72956=DIRECTION ( 'NONE',  ( -1.000000000000000000, -0.000000000000000000, 0.000000000000000000 ) ) ;
#72957=VERTEX_POINT ( 'NONE', #25386 ) ;
#72959=CARTESIAN_POINT ( 'NONE',  ( 10.00000000000000000, -72.35432306680469594, -20.40083707022958848 ) ) ;
#72962=ADVANCED_FACE ( 'NONE', ( #38135 ), #61072, .T. ) ;
#72963=FACE_OUTER_BOUND ( 'NONE', #768, .T. ) ;
#72964=CARTESIAN_POINT ( 'NONE',  ( 10.00000000000000000, 14.66109333815564852, -73.73191006444555740 ) ) ;
#72965=CARTESIAN_POINT ( 'NONE',  ( 10.00000000000000000, 0.000000000000000000, 0.000000000000000000 ) ) ;
#72970=DIRECTION ( 'NONE',  ( 0.000000000000000000, 0.7604059656000276002, 0.6494480483301876550 ) ) ;
#72981=CARTESIAN_POINT ( 'NONE',  ( 0.000000000000000000, 77.16300072079660310, 27.74655509720696500 ) ) ;
#72994=ORIENTED_EDGE ( 'NONE', *, *, #72162, .F. ) ;
#73000=VECTOR ( 'NONE', #19306, 1000.000000000000000 ) ;
#73012=ORIENTED_EDGE ( 'NONE', *, *, #73303, .T. ) ;
#73015=ORIENTED_EDGE ( 'NONE', *, *, #61781, .T. ) ;
#73017=ORIENTED_EDGE ( 'NONE', *, *, #26796, .F. ) ;
#73026=CIRCLE ( 'NONE', #65878, 77.49899999999999523 ) ;
#73034=CARTESIAN_POINT ( 'NONE',  ( 10.00000000000000000, 0.000000000000000000, 0.000000000000000000 ) ) ;
#73037=CARTESIAN_POINT ( 'NONE',  ( 0.000000000000000000, 74.18225833017888249, 34.94270380257665209 ) ) ;
#73039=CARTESIAN_POINT ( 'NONE',  ( 0.000000000000000000, 0.000000000000000000, 0.000000000000000000 ) ) ;
#73046=EDGE_LOOP ( 'NONE', ( #23940, #9349, #19774, #45693 ) ) ;
#73064=CIRCLE ( 'NONE', #32219, 82.00000000000000000 ) ;
#73065=AXIS2_PLACEMENT_3D ( 'NONE', #22255, #47046, #24474 ) ;
#73070=DIRECTION ( 'NONE',  ( 1.000000000000000000, 0.000000000000000000, 0.000000000000000000 ) ) ;
#73072=CARTESIAN_POINT ( 'NONE',  ( 10.00000000000000000, 14.67089635893713684, 73.72996012237443608 ) ) ;
#73078=CARTESIAN_POINT ( 'NONE',  ( 10.00000000000000000, -71.27951684758046724, 30.41916302227088309 ) ) ;
#73079=CARTESIAN_POINT ( 'NONE',  ( 0.000000000000000000, 31.46837873494978055, 68.27212725128286763 ) ) ;
#73081=DIRECTION ( 'NONE',  ( 0.000000000000000000, 0.000000000000000000, 1.000000000000000000 ) ) ;
#73093=DIRECTION ( 'NONE',  ( 0.000000000000000000, 0.000000000000000000, 1.000000000000000000 ) ) ;
#73103=ORIENTED_EDGE ( 'NONE', *, *, #74296, .T. ) ;
#73108=VECTOR ( 'NONE', #18709, 1000.000000000000000 ) ;
#73111=ORIENTED_EDGE ( 'NONE', *, *, #68671, .T. ) ;
#73118=ADVANCED_FACE ( 'NONE', ( #5432 ), #33223, .T. ) ;
#73119=AXIS2_PLACEMENT_3D ( 'NONE', #8111, #14113, #31037 ) ;
#73126=VERTEX_POINT ( 'NONE', #68199 ) ;
#73133=EDGE_CURVE ( 'NONE', #33517, #56683, #73452, .T. ) ;
#73151=FACE_OUTER_BOUND ( 'NONE', #38765, .T. ) ;
#73152=EDGE_CURVE ( 'NONE', #16336, #44625, #16818, .T. ) ;
#73162=DIRECTION ( 'NONE',  ( -1.000000000000000000, -0.000000000000000000, -0.000000000000000000 ) ) ;
#73178=CARTESIAN_POINT ( 'NONE',  ( 10.00000000000000000, 41.76106447765580043, -62.50884508063379741 ) ) ;
#73186=EDGE_CURVE ( 'NONE', #66703, #70184, #38439, .T. ) ;
#73191=ORIENTED_EDGE ( 'NONE', *, *, #42382, .T. ) ;
#73194=CARTESIAN_POINT ( 'NONE',  ( 10.00000000000000000, 59.46389618802034960, -49.70050353004825894 ) ) ;
#73198=CARTESIAN_POINT ( 'NONE',  ( 10.00000000000000000, -71.27951684758005513, -30.41916302227188851 ) ) ;
#73213=EDGE_CURVE ( 'NONE', #62512, #54897, #68451, .T. ) ;
#73221=CARTESIAN_POINT ( 'NONE',  ( 0.000000000000000000, 76.66974797899852945, -11.30684508768257679 ) ) ;
#73223=VERTEX_POINT ( 'NONE', #6886 ) ;
#73224=CARTESIAN_POINT ( 'NONE',  ( 10.00000000000000000, -17.28742895386139722, 75.54627589209937355 ) ) ;
#73226=EDGE_CURVE ( 'NONE', #50178, #46694, #36022, .T. ) ;
#73228=ORIENTED_EDGE ( 'NONE', *, *, #72887, .F. ) ;
#73230=ORIENTED_EDGE ( 'NONE', *, *, #67013, .T. ) ;
#73237=ORIENTED_EDGE ( 'NONE', *, *, #56753, .F. ) ;
#73240=CARTESIAN_POINT ( 'NONE',  ( 10.00000000000000000, 0.000000000000000000, 0.000000000000000000 ) ) ;
#73242=ORIENTED_EDGE ( 'NONE', *, *, #45434, .F. ) ;
#73270=DIRECTION ( 'NONE',  ( 0.000000000000000000, 0.000000000000000000, -1.000000000000000000 ) ) ;
#73273=EDGE_CURVE ( 'NONE', #24045, #26445, #13203, .T. ) ;
#73276=CIRCLE ( 'NONE', #1319, 31.99999999999999289 ) ;
#73282=AXIS2_PLACEMENT_3D ( 'NONE', #26042, #65544, #71900 ) ;
#73283=CARTESIAN_POINT ( 'NONE',  ( 10.00000000000000000, 16.00000000000000000, -2.500000000000000000 ) ) ;
#73291=FACE_OUTER_BOUND ( 'NONE', #30651, .T. ) ;
#73297=ORIENTED_EDGE ( 'NONE', *, *, #4766, .F. ) ;
#73303=EDGE_CURVE ( 'NONE', #67626, #43336, #22834, .T. ) ;
#73306=ORIENTED_EDGE ( 'NONE', *, *, #20456, .T. ) ;
#73326=ORIENTED_EDGE ( 'NONE', *, *, #50432, .F. ) ;
#73329=DIRECTION ( 'NONE',  ( -1.000000000000000000, -0.000000000000000000, 0.000000000000000000 ) ) ;
#73330=ADVANCED_FACE ( 'NONE', ( #65159 ), #71874, .T. ) ;
#73341=DIRECTION ( 'NONE',  ( -1.000000000000000000, -0.000000000000000000, -0.000000000000000000 ) ) ;
#73354=CARTESIAN_POINT ( 'NONE',  ( 10.00000000000000000, -77.32052557432837148, -5.256550761633697277 ) ) ;
#73357=DIRECTION ( 'NONE',  ( 1.000000000000000000, -0.000000000000000000, -0.000000000000000000 ) ) ;
#73361=LINE ( 'NONE', #27504, #62901 ) ;
#73367=DIRECTION ( 'NONE',  ( -1.000000000000000000, -0.000000000000000000, 0.000000000000000000 ) ) ;
#73375=CARTESIAN_POINT ( 'NONE',  ( 10.00000000000000000, -12.93880638057369659, 76.41127070299266677 ) ) ;
#73377=CIRCLE ( 'NONE', #4990, 32.00000000000000000 ) ;
#73381=EDGE_CURVE ( 'NONE', #63204, #37924, #17996, .T. ) ;
#73387=CARTESIAN_POINT ( 'NONE',  ( 10.00000000000000000, -22.90783923731686045, 78.73519480814947258 ) ) ;
#73400=VERTEX_POINT ( 'NONE', #70770 ) ;
#73404=CARTESIAN_POINT ( 'NONE',  ( 5.000000000000002665, 39.47590169984846398, 71.87247863392428826 ) ) ;
#73405=EDGE_CURVE ( 'NONE', #50832, #1159, #37263, .T. ) ;
#73408=ORIENTED_EDGE ( 'NONE', *, *, #19660, .F. ) ;
#73416=DIRECTION ( 'NONE',  ( -1.000000000000000000, -0.000000000000000000, -0.000000000000000000 ) ) ;
#73427=EDGE_CURVE ( 'NONE', #56348, #17276, #38498, .T. ) ;
#73433=DIRECTION ( 'NONE',  ( 0.000000000000000000, 0.000000000000000000, 1.000000000000000000 ) ) ;
#73440=CARTESIAN_POINT ( 'NONE',  ( 0.000000000000000000, 0.000000000000000000, 0.000000000000000000 ) ) ;
#73451=CARTESIAN_POINT ( 'NONE',  ( 10.00000000000000000, -75.11725578898466438, -2.956366410621452001 ) ) ;
#73452=LINE ( 'NONE', #74200, #66036 ) ;
#73457=CARTESIAN_POINT ( 'NONE',  ( 10.00000000000000000, 68.27212725128275395, 31.46837873495001503 ) ) ;
#73461=EDGE_CURVE ( 'NONE', #64387, #28018, #39685, .T. ) ;
#73469=CYLINDRICAL_SURFACE ( 'NONE', #47848, 32.00000000000000000 ) ;
#73472=ADVANCED_FACE ( 'NONE', ( #66264 ), #10119, .T. ) ;
#73478=FACE_OUTER_BOUND ( 'NONE', #34958, .T. ) ;
#73479=VERTEX_POINT ( 'NONE', #30546 ) ;
#73480=VECTOR ( 'NONE', #29489, 1000.000000000000000 ) ;
#73488=EDGE_LOOP ( 'NONE', ( #35316, #23166, #56359, #8101 ) ) ;
#73489=ORIENTED_EDGE ( 'NONE', *, *, #44136, .F. ) ;
#73499=EDGE_LOOP ( 'NONE', ( #58637, #72400, #27339, #47353 ) ) ;
#73544=CARTESIAN_POINT ( 'NONE',  ( 0.000000000000000000, -2.946379043146863719, 75.11764819372146462 ) ) ;
#73551=CARTESIAN_POINT ( 'NONE',  ( 10.00000000000000000, 71.91182617369230456, -28.89263327155667938 ) ) ;
#73552=CARTESIAN_POINT ( 'NONE',  ( 10.00000000000000000, 0.000000000000000000, 0.000000000000000000 ) ) ;
#73560=EDGE_CURVE ( 'NONE', #38392, #45747, #57710, .T. ) ;
#73570=AXIS2_PLACEMENT_3D ( 'NONE', #12554, #19669, #13295 ) ;
#73572=VERTEX_POINT ( 'NONE', #34532 ) ;
#73576=AXIS2_PLACEMENT_3D ( 'NONE', #67768, #4255, #56496 ) ;
#73581=DIRECTION ( 'NONE',  ( -1.000000000000000000, -0.000000000000000000, 0.000000000000000000 ) ) ;
#73585=DIRECTION ( 'NONE',  ( 0.000000000000000000, 0.000000000000000000, 1.000000000000000000 ) ) ;
#73587=AXIS2_PLACEMENT_3D ( 'NONE', #42859, #32668, #25925 ) ;
#73588=VERTEX_POINT ( 'NONE', #62010 ) ;
#73601=DIRECTION ( 'NONE',  ( -1.000000000000000000, 0.000000000000000000, -0.000000000000000000 ) ) ;
#73604=FACE_OUTER_BOUND ( 'NONE', #6962, .T. ) ;
#73615=ORIENTED_EDGE ( 'NONE', *, *, #42703, .F. ) ;
#73624=ORIENTED_EDGE ( 'NONE', *, *, #49206, .T. ) ;
#73625=DIRECTION ( 'NONE',  ( -1.000000000000000000, 0.000000000000000000, 0.000000000000000000 ) ) ;
#73626=DIRECTION ( 'NONE',  ( -1.000000000000000000, -0.000000000000000000, 0.000000000000000000 ) ) ;
#73652=EDGE_CURVE ( 'NONE', #65113, #59483, #42094, .T. ) ;
#73655=DIRECTION ( 'NONE',  ( 0.000000000000000000, 0.7604059656000322631, -0.6494480483301821039 ) ) ;
#73672=EDGE_LOOP ( 'NONE', ( #5844, #56245, #26768, #65407 ) ) ;
#73685=CARTESIAN_POINT ( 'NONE',  ( 10.00000000000000000, 0.000000000000000000, 0.000000000000000000 ) ) ;
#73687=ORIENTED_EDGE ( 'NONE', *, *, #1047, .T. ) ;
#73691=EDGE_CURVE ( 'NONE', #65118, #16263, #36374, .T. ) ;
#73692=ORIENTED_EDGE ( 'NONE', *, *, #61396, .F. ) ;
#73705=VERTEX_POINT ( 'NONE', #19458 ) ;
#73714=VECTOR ( 'NONE', #9538, 1000.000000000000000 ) ;
#73718=ORIENTED_EDGE ( 'NONE', *, *, #68989, .T. ) ;
#73719=DIRECTION ( 'NONE',  ( -1.000000000000000000, 0.000000000000000000, -0.000000000000000000 ) ) ;
#73720=DIRECTION ( 'NONE',  ( -1.000000000000000000, 0.000000000000000000, 0.000000000000000000 ) ) ;
#73723=CARTESIAN_POINT ( 'NONE',  ( 5.000000000000000000, -60.67117009219098378, -55.16347631943106933 ) ) ;
#73729=CARTESIAN_POINT ( 'NONE',  ( 10.00000000000000000, 0.000000000000000000, 0.000000000000000000 ) ) ;
#73737=EDGE_CURVE ( 'NONE', #1727, #25328, #25476, .T. ) ;
#73748=CIRCLE ( 'NONE', #62847, 32.00000000000000000 ) ;
#73749=AXIS2_PLACEMENT_3D ( 'NONE', #6190, #56582, #39654 ) ;
#73753=EDGE_LOOP ( 'NONE', ( #65844, #68457, #10770, #10084 ) ) ;
#73756=ORIENTED_EDGE ( 'NONE', *, *, #47117, .T. ) ;
#73757=VECTOR ( 'NONE', #8954, 1000.000000000000000 ) ;
#73763=VERTEX_POINT ( 'NONE', #14559 ) ;
#73767=EDGE_CURVE ( 'NONE', #63089, #41920, #26579, .T. ) ;
#73769=VERTEX_POINT ( 'NONE', #43892 ) ;
#73771=VERTEX_POINT ( 'NONE', #72435 ) ;
#73773=ORIENTED_EDGE ( 'NONE', *, *, #23006, .T. ) ;
#73779=ORIENTED_EDGE ( 'NONE', *, *, #39758, .F. ) ;
#73789=CARTESIAN_POINT ( 'NONE',  ( 0.000000000000000000, 0.000000000000000000, 0.000000000000000000 ) ) ;
#73803=CARTESIAN_POINT ( 'NONE',  ( 10.00000000000000000, 0.000000000000000000, 0.000000000000000000 ) ) ;
#73807=CYLINDRICAL_SURFACE ( 'NONE', #4298, 77.49899999999999523 ) ;
#73808=AXIS2_PLACEMENT_3D ( 'NONE', #67754, #62503, #50453 ) ;
#73819=DIRECTION ( 'NONE',  ( -1.000000000000000000, -0.000000000000000000, 0.000000000000000000 ) ) ;
#73820=DIRECTION ( 'NONE',  ( -1.000000000000000000, 0.000000000000000000, 0.000000000000000000 ) ) ;
#73826=CARTESIAN_POINT ( 'NONE',  ( 10.00000000000000000, 46.53671651293948486, 59.03961581697416250 ) ) ;
#73834=EDGE_CURVE ( 'NONE', #60600, #23124, #3734, .T. ) ;
#73838=VERTEX_POINT ( 'NONE', #20938 ) ;
#73842=CIRCLE ( 'NONE', #23411, 77.49899999999998101 ) ;
#73845=EDGE_CURVE ( 'NONE', #38841, #50744, #67359, .T. ) ;
#73848=DIRECTION ( 'NONE',  ( -1.000000000000000000, -0.000000000000000000, -0.000000000000000000 ) ) ;
#73856=EDGE_CURVE ( 'NONE', #68580, #45509, #49322, .T. ) ;
#73863=ORIENTED_EDGE ( 'NONE', *, *, #69999, .T. ) ;
#73875=CARTESIAN_POINT ( 'NONE',  ( 5.000000000000000000, -79.10210256391353312, -21.60688246758668640 ) ) ;
#73881=DIRECTION ( 'NONE',  ( 1.000000000000000000, 0.000000000000000000, 0.000000000000000000 ) ) ;
#73893=CARTESIAN_POINT ( 'NONE',  ( 10.00000000000000000, -73.95703589263958122, -23.16143007188506431 ) ) ;
#73900=CARTESIAN_POINT ( 'NONE',  ( 0.000000000000000000, -77.32052557432837148, -5.256550761633697277 ) ) ;
#73912=EDGE_LOOP ( 'NONE', ( #38124, #12233, #69664, #859 ) ) ;
#73917=DIRECTION ( 'NONE',  ( -1.000000000000000000, -0.000000000000000000, 0.000000000000000000 ) ) ;
#73918=CYLINDRICAL_SURFACE ( 'NONE', #6927, 31.99999999999998579 ) ;
#73926=DIRECTION ( 'NONE',  ( -1.000000000000000000, 0.000000000000000000, 0.000000000000000000 ) ) ;
#73929=EDGE_CURVE ( 'NONE', #43091, #60565, #51750, .T. ) ;
#73939=EDGE_CURVE ( 'NONE', #7213, #10916, #71316, .T. ) ;
#73940=EDGE_CURVE ( 'NONE', #71349, #42442, #60082, .T. ) ;
#73945=CYLINDRICAL_SURFACE ( 'NONE', #49168, 32.00000000000000000 ) ;
#73948=ORIENTED_EDGE ( 'NONE', *, *, #65470, .F. ) ;
#73961=ORIENTED_EDGE ( 'NONE', *, *, #26121, .T. ) ;
#73962=FACE_OUTER_BOUND ( 'NONE', #57538, .T. ) ;
#73964=DIRECTION ( 'NONE',  ( 0.000000000000000000, 0.000000000000000000, 1.000000000000000000 ) ) ;
#73972=VERTEX_POINT ( 'NONE', #28810 ) ;
#73973=CARTESIAN_POINT ( 'NONE',  ( 10.00000000000000000, 0.000000000000000000, 0.000000000000000000 ) ) ;
#73982=CYLINDRICAL_SURFACE ( 'NONE', #61712, 77.49899999999999523 ) ;
#73991=EDGE_CURVE ( 'NONE', #33698, #8597, #15738, .T. ) ;
#73992=CARTESIAN_POINT ( 'NONE',  ( 0.000000000000000000, 0.000000000000000000, 0.000000000000000000 ) ) ;
#73993=EDGE_CURVE ( 'NONE', #8951, #1496, #45763, .T. ) ;
#74001=CARTESIAN_POINT ( 'NONE',  ( 0.000000000000000000, -77.16300072079681627, 27.74655509720641078 ) ) ;
#74005=EDGE_CURVE ( 'NONE', #51313, #41146, #70944, .T. ) ;
#74020=DIRECTION ( 'NONE',  ( 1.000000000000000000, 0.000000000000000000, 0.000000000000000000 ) ) ;
#74022=DIRECTION ( 'NONE',  ( -1.000000000000000000, -0.000000000000000000, 0.000000000000000000 ) ) ;
#74049=EDGE_LOOP ( 'NONE', ( #62099, #15818, #45897, #6238 ) ) ;
#74061=DIRECTION ( 'NONE',  ( 0.000000000000000000, 0.9969173337331282969, -0.07845909572784179331 ) ) ;
#74062=VECTOR ( 'NONE', #69123, 1000.000000000000000 ) ;
#74065=VECTOR ( 'NONE', #63636, 1000.000000000000000 ) ;
#74066=ORIENTED_EDGE ( 'NONE', *, *, #5820, .T. ) ;
#74069=FACE_OUTER_BOUND ( 'NONE', #43545, .T. ) ;
#74073=AXIS2_PLACEMENT_3D ( 'NONE', #42207, #54585, #13250 ) ;
#74074=ORIENTED_EDGE ( 'NONE', *, *, #33530, .F. ) ;
#74087=CYLINDRICAL_SURFACE ( 'NONE', #37436, 31.99999999999999289 ) ;
#74088=DIRECTION ( 'NONE',  ( -1.000000000000000000, -0.000000000000000000, -0.000000000000000000 ) ) ;
#74093=DIRECTION ( 'NONE',  ( -1.000000000000000000, 0.000000000000000000, 0.000000000000000000 ) ) ;
#74095=CIRCLE ( 'NONE', #8032, 31.99999999999999289 ) ;
#74097=DIRECTION ( 'NONE',  ( 0.000000000000000000, 0.3826834323650907810, -0.9238795325112864054 ) ) ;
#74102=CYLINDRICAL_SURFACE ( 'NONE', #4979, 32.00000000000000000 ) ;
#74103=EDGE_CURVE ( 'NONE', #5866, #40399, #62681, .T. ) ;
#74112=CARTESIAN_POINT ( 'NONE',  ( 0.000000000000000000, 0.000000000000000000, 0.000000000000000000 ) ) ;
#74115=CARTESIAN_POINT ( 'NONE',  ( 0.000000000000000000, 0.000000000000000000, 0.000000000000000000 ) ) ;
#74121=CARTESIAN_POINT ( 'NONE',  ( 5.000000000000002665, 81.90746397400387480, 3.894527615418187150 ) ) ;
#74125=DIRECTION ( 'NONE',  ( 0.000000000000000000, 0.000000000000000000, 1.000000000000000000 ) ) ;
#74127=CIRCLE ( 'NONE', #65719, 32.00000000000000000 ) ;
#74132=ORIENTED_EDGE ( 'NONE', *, *, #34309, .T. ) ;
#74142=VERTEX_POINT ( 'NONE', #41206 ) ;
#74156=ORIENTED_EDGE ( 'NONE', *, *, #1936, .T. ) ;
#74161=CARTESIAN_POINT ( 'NONE',  ( 5.000000000000000000, -63.97538442413463855, 51.29473840253199768 ) ) ;
#74163=DIRECTION ( 'NONE',  ( -1.000000000000000000, 0.000000000000000000, -0.000000000000000000 ) ) ;
#74168=DIRECTION ( 'NONE',  ( -1.000000000000000000, 0.000000000000000000, -0.000000000000000000 ) ) ;
#74169=ADVANCED_FACE ( 'NONE', ( #35553 ), #58485, .T. ) ;
#74172=ORIENTED_EDGE ( 'NONE', *, *, #8569, .F. ) ;
#74182=AXIS2_PLACEMENT_3D ( 'NONE', #55896, #14180, #4410 ) ;
#74184=CARTESIAN_POINT ( 'NONE',  ( 0.000000000000000000, -55.38113227695820484, 54.21277698773656084 ) ) ;
#74190=EDGE_CURVE ( 'NONE', #71438, #70238, #37326, .T. ) ;
#74193=EDGE_CURVE ( 'NONE', #36080, #28680, #2128, .T. ) ;
#74200=CARTESIAN_POINT ( 'NONE',  ( 5.000000000000002665, 15.33399622253481986, 80.55351364060595643 ) ) ;
#74213=CIRCLE ( 'NONE', #14150, 77.49899999999999523 ) ;
#74216=DIRECTION ( 'NONE',  ( -1.000000000000000000, -0.000000000000000000, 0.000000000000000000 ) ) ;
#74217=ORIENTED_EDGE ( 'NONE', *, *, #15958, .F. ) ;
#74218=DIRECTION ( 'NONE',  ( 0.000000000000000000, 0.000000000000000000, 1.000000000000000000 ) ) ;
#74220=CARTESIAN_POINT ( 'NONE',  ( 0.000000000000000000, 81.34940948281337114, 10.30890764327411979 ) ) ;
#74223=ORIENTED_EDGE ( 'NONE', *, *, #69141, .T. ) ;
#74227=ORIENTED_EDGE ( 'NONE', *, *, #15604, .T. ) ;
#74229=CIRCLE ( 'NONE', #41821, 32.00000000000000000 ) ;
#74238=CARTESIAN_POINT ( 'NONE',  ( 10.00000000000000000, 2.946379043146343246, 75.11764819372150725 ) ) ;
#74255=DIRECTION ( 'NONE',  ( 0.000000000000000000, -1.000000000000000000, -1.040834085586084414E-14 ) ) ;
#74269=ORIENTED_EDGE ( 'NONE', *, *, #26728, .F. ) ;
#74277=DIRECTION ( 'NONE',  ( 0.000000000000000000, 0.000000000000000000, 1.000000000000000000 ) ) ;
#74278=CARTESIAN_POINT ( 'NONE',  ( 5.000000000000000000, 77.16300072079660310, 27.74655509720696855 ) ) ;
#74282=EDGE_CURVE ( 'NONE', #4552, #73705, #9580, .T. ) ;
#74293=AXIS2_PLACEMENT_3D ( 'NONE', #63508, #68409, #24019 ) ;
#74296=EDGE_CURVE ( 'NONE', #22189, #16005, #56590, .T. ) ;
#74322=CARTESIAN_POINT ( 'NONE',  ( 10.00000000000000000, 0.000000000000000000, 0.000000000000000000 ) ) ;
#74324=ORIENTED_EDGE ( 'NONE', *, *, #69075, .T. ) ;
#74325=EDGE_CURVE ( 'NONE', #24805, #35621, #31387, .T. ) ;
#74331=CARTESIAN_POINT ( 'NONE',  ( 0.000000000000000000, -59.03342792756231461, -46.54456581323868392 ) ) ;
#74332=EDGE_CURVE ( 'NONE', #38273, #37771, #13369, .T. ) ;
#74333=DIRECTION ( 'NONE',  ( 0.000000000000000000, -0.5877852522924625900, -0.8090169943749551118 ) ) ;
#74339=CIRCLE ( 'NONE', #22731, 31.99999999999999645 ) ;
ENDSEC;
END-ISO-10303-21;
